ISO-10303-21;
HEADER;
FILE_DESCRIPTION (('STEP AP214'),
    '1' );
FILE_NAME ('Aluminum Extrusions (T-Slot Profiles)_5537T808.step',
    '2026-10-09T16:01:55',
    ( '' ),
    ( '' ),
    'SwSTEP 2.0',
    'SolidWorks 2024',
    '' );
FILE_SCHEMA (( 'AUTOMOTIVE_DESIGN' ));
ENDSEC;

DATA;
#14=AXIS2_PLACEMENT_3D ( 'NONE', #25100, #35689, #34989 ) ;
#31=LINE ( 'NONE', #62705, #60565 ) ;
#35=SHAPE_REPRESENTATION ( 'Aluminum Extrusions (T-Slot Profiles)_5537T808', ( #45918 ), #47199 ) ;
#36=CARTESIAN_POINT ( 'NONE',  ( -11.99351654964679526, -7.826483450353362237, 455.0000000000000568 ) ) ;
#38=CARTESIAN_POINT ( 'NONE',  ( 4.201500623656003519, -4.740315990920191069, 195.0000000000000284 ) ) ;
#45=CARTESIAN_POINT ( 'NONE',  ( 6.006483450353353959, 5.993516549646629166, 195.0000000000000284 ) ) ;
#47=ADVANCED_FACE ( 'NONE', ( #64337 ), #37812, .F. ) ;
#48=CARTESIAN_POINT ( 'NONE',  ( 11.08848345035334404, -11.08848345035339733, 195.0000000000000284 ) ) ;
#49=FACE_OUTER_BOUND ( 'NONE', #48947, .T. ) ;
#51=DIRECTION ( 'NONE',  ( 1.000000000000000000, 0.000000000000000000, 0.000000000000000000 ) ) ;
#52=VECTOR ( 'NONE', #54469, 1000.000000000000000 ) ;
#57=CIRCLE ( 'NONE', #62089, 0.3999999999999993006 ) ;
#59=DIRECTION ( 'NONE',  ( -0.000000000000000000, -0.000000000000000000, -1.000000000000000000 ) ) ;
#65=VECTOR ( 'NONE', #47625, 1000.000000000000114 ) ;
#78=CARTESIAN_POINT ( 'NONE',  ( 11.48848345035341900, 10.19191654964656202, 455.0000000000000568 ) ) ;
#89=CARTESIAN_POINT ( 'NONE',  ( 6.006483450353353959, 5.993516549646629166, 195.0000000000000284 ) ) ;
#99=LINE ( 'NONE', #17046, #62617 ) ;
#102=EDGE_CURVE ( 'NONE', #33046, #57965, #58906, .T. ) ;
#118=DIRECTION ( 'NONE',  ( -1.836970198721029934E-16, 1.836970198721036344E-16, -1.000000000000000000 ) ) ;
#119=ADVANCED_FACE ( 'NONE', ( #37125 ), #15567, .T. ) ;
#120=EDGE_CURVE ( 'NONE', #5167, #67654, #58950, .T. ) ;
#129=AXIS2_PLACEMENT_3D ( 'NONE', #11576, #55092, #50108 ) ;
#130=CARTESIAN_POINT ( 'NONE',  ( -7.793516549646827940, -11.12648345035340647, 455.0000000000000568 ) ) ;
#136=DIRECTION ( 'NONE',  ( -1.836970198721029934E-16, 1.836970198721036344E-16, -1.000000000000000000 ) ) ;
#140=VECTOR ( 'NONE', #32792, 1000.000000000000000 ) ;
#143=DIRECTION ( 'NONE',  ( 1.047444401652939849E-14, 1.000000000000000000, 1.836970198721029934E-16 ) ) ;
#144=VERTEX_POINT ( 'NONE', #43447 ) ;
#153=ADVANCED_FACE ( 'NONE', ( #5637 ), #10243, .T. ) ;
#154=AXIS2_PLACEMENT_3D ( 'NONE', #15103, #20746, #47621 ) ;
#160=CARTESIAN_POINT ( 'NONE',  ( 12.00648345035338060, -7.826483450353491023, 455.0000000000000568 ) ) ;
#161=DIRECTION ( 'NONE',  ( -1.000000000000000000, 4.121462285523434458E-16, 1.514200678731842937E-31 ) ) ;
#162=EDGE_CURVE ( 'NONE', #51028, #19307, #65708, .T. ) ;
#164=VECTOR ( 'NONE', #31402, 1000.000000000000000 ) ;
#172=DIRECTION ( 'NONE',  ( 1.356437060717831815E-15, 1.000000000000000000, 0.000000000000000000 ) ) ;
#176=AXIS2_PLACEMENT_3D ( 'NONE', #44626, #60208, #34021 ) ;
#182=DIRECTION ( 'NONE',  ( -0.000000000000000000, 3.673940397442059868E-16, -1.000000000000000000 ) ) ;
#189=DIRECTION ( 'NONE',  ( -1.813998472013049506E-14, -1.000000000000000000, -1.836970198721043986E-16 ) ) ;
#191=VERTEX_POINT ( 'NONE', #61342 ) ;
#194=DIRECTION ( 'NONE',  ( 1.000000000000000000, 0.000000000000000000, 0.000000000000000000 ) ) ;
#197=CIRCLE ( 'NONE', #57770, 2.204799999999999205 ) ;
#199=ORIENTED_EDGE ( 'NONE', *, *, #12386, .F. ) ;
#201=AXIS2_PLACEMENT_3D ( 'NONE', #59073, #10628, #38219 ) ;
#217=DIRECTION ( 'NONE',  ( -1.047444401652940164E-14, -1.000000000000000000, -1.836970198721030181E-16 ) ) ;
#232=ORIENTED_EDGE ( 'NONE', *, *, #38318, .F. ) ;
#234=DIRECTION ( 'NONE',  ( -1.000000000000000000, 0.000000000000000000, 0.000000000000000000 ) ) ;
#235=AXIS2_PLACEMENT_3D ( 'NONE', #32460, #32097, #54031 ) ;
#237=ADVANCED_FACE ( 'NONE', ( #40838 ), #18219, .F. ) ;
#239=LINE ( 'NONE', #1275, #59908 ) ;
#241=ORIENTED_EDGE ( 'NONE', *, *, #54639, .T. ) ;
#242=ORIENTED_EDGE ( 'NONE', *, *, #68755, .F. ) ;
#261=ORIENTED_EDGE ( 'NONE', *, *, #56801, .T. ) ;
#267=EDGE_LOOP ( 'NONE', ( #46441, #3343, #16944, #35181, #20767, #32717, #56095, #39421 ) ) ;
#274=CARTESIAN_POINT ( 'NONE',  ( -8.593516549646745162, -4.396432944014545541, 455.0000000000000568 ) ) ;
#280=ADVANCED_FACE ( 'NONE', ( #45792 ), #62049, .F. ) ;
#281=ORIENTED_EDGE ( 'NONE', *, *, #951, .F. ) ;
#284=CARTESIAN_POINT ( 'NONE',  ( -11.33351654964671162, 1.077516549646603483, 455.0000000000000568 ) ) ;
#293=ORIENTED_EDGE ( 'NONE', *, *, #42329, .T. ) ;
#295=AXIS2_PLACEMENT_3D ( 'NONE', #54190, #47225, #5411 ) ;
#318=LINE ( 'NONE', #15885, #62736 ) ;
#322=CARTESIAN_POINT ( 'NONE',  ( 4.186483450353422953, 11.77351654964658501, 455.0000000000000568 ) ) ;
#325=VERTEX_POINT ( 'NONE', #15027 ) ;
#326=ORIENTED_EDGE ( 'NONE', *, *, #36665, .T. ) ;
#332=EDGE_CURVE ( 'NONE', #67879, #12341, #4078, .T. ) ;
#333=DIRECTION ( 'NONE',  ( -1.836970198721029934E-16, -1.836970198721010706E-16, 1.000000000000000000 ) ) ;
#339=CARTESIAN_POINT ( 'NONE',  ( -6.331612867284244217, -8.406483450353421816, 455.0000000000000568 ) ) ;
#340=ORIENTED_EDGE ( 'NONE', *, *, #61679, .T. ) ;
#350=DIRECTION ( 'NONE',  ( -1.000000000000000000, 0.000000000000000000, 0.000000000000000000 ) ) ;
#352=ORIENTED_EDGE ( 'NONE', *, *, #34899, .F. ) ;
#353=DIRECTION ( 'NONE',  ( 1.047444401652940007E-14, 1.000000000000000000, 1.836970198721029934E-16 ) ) ;
#354=VERTEX_POINT ( 'NONE', #52877 ) ;
#356=EDGE_CURVE ( 'NONE', #64205, #63555, #57452, .T. ) ;
#358=VECTOR ( 'NONE', #51370, 1000.000000000000000 ) ;
#366=ORIENTED_EDGE ( 'NONE', *, *, #51811, .T. ) ;
#379=ORIENTED_EDGE ( 'NONE', *, *, #51031, .F. ) ;
#387=CARTESIAN_POINT ( 'NONE',  ( 7.811466277050736373, -4.740315990920159095, 195.0000000000000284 ) ) ;
#388=DIRECTION ( 'NONE',  ( 1.836970198721029934E-16, 1.836970198721010706E-16, -1.000000000000000000 ) ) ;
#391=VERTEX_POINT ( 'NONE', #36234 ) ;
#399=ORIENTED_EDGE ( 'NONE', *, *, #14387, .F. ) ;
#410=ORIENTED_EDGE ( 'NONE', *, *, #40798, .T. ) ;
#423=VECTOR ( 'NONE', #48895, 1000.000000000000000 ) ;
#431=DIRECTION ( 'NONE',  ( 1.901462112903059913E-14, 1.000000000000000000, 1.836970198721045958E-16 ) ) ;
#432=DIRECTION ( 'NONE',  ( 8.673617379884068604E-15, 1.000000000000000000, 0.000000000000000000 ) ) ;
#433=CARTESIAN_POINT ( 'NONE',  ( -2.993516549646791258, -7.428221114745081621, 455.0000000000000568 ) ) ;
#441=ORIENTED_EDGE ( 'NONE', *, *, #10741, .T. ) ;
#443=EDGE_LOOP ( 'NONE', ( #42999, #49146, #19104, #67733 ) ) ;
#445=EDGE_CURVE ( 'NONE', #15497, #55902, #11786, .T. ) ;
#449=FACE_OUTER_BOUND ( 'NONE', #18243, .T. ) ;
#452=ORIENTED_EDGE ( 'NONE', *, *, #12447, .F. ) ;
#461=DIRECTION ( 'NONE',  ( 1.836970198721029934E-16, -1.836970198721036344E-16, 1.000000000000000000 ) ) ;
#462=ORIENTED_EDGE ( 'NONE', *, *, #49079, .T. ) ;
#463=EDGE_CURVE ( 'NONE', #56608, #65774, #59207, .T. ) ;
#469=ORIENTED_EDGE ( 'NONE', *, *, #18723, .T. ) ;
#470=CARTESIAN_POINT ( 'NONE',  ( -9.093516549646711411, 11.11351654964659730, 195.0000000000000284 ) ) ;
#472=VECTOR ( 'NONE', #25072, 1000.000000000000000 ) ;
#474=DIRECTION ( 'NONE',  ( -0.6414496315691494699, -0.7671651518153064231, -0.000000000000000000 ) ) ;
#477=VECTOR ( 'NONE', #26958, 1000.000000000000000 ) ;
#481=CARTESIAN_POINT ( 'NONE',  ( -9.093516549646711411, 10.08346604330776941, 195.0000000000000284 ) ) ;
#483=CARTESIAN_POINT ( 'NONE',  ( -8.198316549646712303, 5.993516549646603409, 455.0000000000000568 ) ) ;
#485=DIRECTION ( 'NONE',  ( 0.8660254037844435926, 0.4999999999999913958, 2.509347957447859069E-16 ) ) ;
#486=FACE_OUTER_BOUND ( 'NONE', #18940, .T. ) ;
#488=CARTESIAN_POINT ( 'NONE',  ( 5.668387132715918320, -8.406483450353393394, 195.0000000000000284 ) ) ;
#492=DIRECTION ( 'NONE',  ( -0.000000000000000000, 3.673940397442059868E-16, -1.000000000000000000 ) ) ;
#493=DIRECTION ( 'NONE',  ( -1.000000000000000000, 0.000000000000000000, 0.000000000000000000 ) ) ;
#499=ORIENTED_EDGE ( 'NONE', *, *, #54883, .F. ) ;
#504=CARTESIAN_POINT ( 'NONE',  ( -4.173516549646792306, -12.00648345035339837, 195.0000000000000284 ) ) ;
#506=DIRECTION ( 'NONE',  ( 0.000000000000000000, 1.000000000000000000, 0.000000000000000000 ) ) ;
#510=ORIENTED_EDGE ( 'NONE', *, *, #6735, .F. ) ;
#514=CARTESIAN_POINT ( 'NONE',  ( 10.92648345035336277, 2.893516549646527825, 455.0000000000000568 ) ) ;
#518=CARTESIAN_POINT ( 'NONE',  ( -11.11351654964671098, 4.193516549646605363, 455.0000000000000568 ) ) ;
#554=PLANE ( 'NONE',  #7433 ) ;
#566=DIRECTION ( 'NONE',  ( 0.000000000000000000, -1.000000000000000000, 0.000000000000000000 ) ) ;
#567=PLANE ( 'NONE',  #57123 ) ;
#587=VERTEX_POINT ( 'NONE', #66922 ) ;
#588=AXIS2_PLACEMENT_3D ( 'NONE', #30987, #41594, #37012 ) ;
#590=ADVANCED_FACE ( 'NONE', ( #7529 ), #61257, .F. ) ;
#593=ORIENTED_EDGE ( 'NONE', *, *, #855, .F. ) ;
#600=ORIENTED_EDGE ( 'NONE', *, *, #16363, .T. ) ;
#606=AXIS2_PLACEMENT_3D ( 'NONE', #28514, #56090, #7641 ) ;
#631=EDGE_CURVE ( 'NONE', #59475, #32917, #18840, .T. ) ;
#635=DIRECTION ( 'NONE',  ( 1.836970198721029934E-16, 1.836970198721010706E-16, -1.000000000000000000 ) ) ;
#642=CARTESIAN_POINT ( 'NONE',  ( -7.593516549646838421, -11.78648345035340839, 455.0000000000000568 ) ) ;
#650=DIRECTION ( 'NONE',  ( -1.185108578570163244E-14, -1.000000000000000000, -1.836970198721014650E-16 ) ) ;
#651=DIRECTION ( 'NONE',  ( -1.836970198721029934E-16, 1.836970198721036344E-16, -1.000000000000000000 ) ) ;
#663=DIRECTION ( 'NONE',  ( -0.000000000000000000, 3.673940397442059868E-16, -1.000000000000000000 ) ) ;
#672=CARTESIAN_POINT ( 'NONE',  ( -7.259684009079930611, 7.798499376343971612, 195.0000000000000284 ) ) ;
#674=EDGE_CURVE ( 'NONE', #5423, #64032, #46062, .T. ) ;
#675=ADVANCED_FACE ( 'NONE', ( #1525 ), #23797, .F. ) ;
#685=DIRECTION ( 'NONE',  ( -1.000000000000000000, 7.304098846218132892E-15, -0.000000000000000000 ) ) ;
#693=DIRECTION ( 'NONE',  ( -0.4999999999999913958, 0.8660254037844437036, 6.723777587268537869E-17 ) ) ;
#695=ORIENTED_EDGE ( 'NONE', *, *, #12685, .F. ) ;
#704=DIRECTION ( 'NONE',  ( 8.359604446858500663E-15, 1.000000000000000000, 3.673940397442059868E-16 ) ) ;
#705=VERTEX_POINT ( 'NONE', #39361 ) ;
#722=CARTESIAN_POINT ( 'NONE',  ( -9.093516549646711411, 10.91351654964659978, 455.0000000000000568 ) ) ;
#733=LINE ( 'NONE', #60793, #54302 ) ;
#757=DIRECTION ( 'NONE',  ( -1.836970198721029934E-16, 1.836970198721036344E-16, -1.000000000000000000 ) ) ;
#761=CARTESIAN_POINT ( 'NONE',  ( -8.593516549646793123, -7.616533956692233431, 455.0000000000000568 ) ) ;
#765=LINE ( 'NONE', #44212, #31442 ) ;
#785=ORIENTED_EDGE ( 'NONE', *, *, #39572, .T. ) ;
#788=DIRECTION ( 'NONE',  ( 1.000000000000000000, 0.000000000000000000, 0.000000000000000000 ) ) ;
#798=CARTESIAN_POINT ( 'NONE',  ( -4.242044687070611886, -8.465062094116088787, 195.0000000000000284 ) ) ;
#799=ORIENTED_EDGE ( 'NONE', *, *, #48308, .T. ) ;
#803=VERTEX_POINT ( 'NONE', #53143 ) ;
#805=PLANE ( 'NONE',  #55812 ) ;
#812=CARTESIAN_POINT ( 'NONE',  ( 7.806483450353418618, 11.11351654964657421, 455.0000000000000568 ) ) ;
#816=ORIENTED_EDGE ( 'NONE', *, *, #61457, .T. ) ;
#819=CARTESIAN_POINT ( 'NONE',  ( 8.406483450353404052, 6.331612867284015955, 455.0000000000000568 ) ) ;
#823=CIRCLE ( 'NONE', #22260, 0.1999999999999987899 ) ;
#842=LINE ( 'NONE', #42642, #9618 ) ;
#848=LINE ( 'NONE', #483, #11059 ) ;
#850=LINE ( 'NONE', #43258, #19324 ) ;
#855=EDGE_CURVE ( 'NONE', #46179, #68965, #3278, .T. ) ;
#865=EDGE_LOOP ( 'NONE', ( #51644, #64448, #69573, #67536 ) ) ;
#872=CIRCLE ( 'NONE', #32458, 0.5999999999999989786 ) ;
#879=EDGE_CURVE ( 'NONE', #24754, #25574, #42511, .T. ) ;
#882=CARTESIAN_POINT ( 'NONE',  ( -4.734785091273957747, 6.606374702650051667, 455.0000000000000568 ) ) ;
#886=ORIENTED_EDGE ( 'NONE', *, *, #67563, .F. ) ;
#889=DIRECTION ( 'NONE',  ( 3.491481338843132961E-15, 1.000000000000000000, 0.000000000000000000 ) ) ;
#891=ORIENTED_EDGE ( 'NONE', *, *, #39004, .T. ) ;
#895=CARTESIAN_POINT ( 'NONE',  ( 5.393625297349890602, 7.252248008019372527, 195.0000000000000284 ) ) ;
#905=EDGE_LOOP ( 'NONE', ( #8696, #17992, #23017, #20153 ) ) ;
#909=EDGE_CURVE ( 'NONE', #50899, #60848, #15648, .T. ) ;
#921=LINE ( 'NONE', #10807, #30327 ) ;
#934=CARTESIAN_POINT ( 'NONE',  ( -9.404046420174067222, -1.866219381641389674, 195.0000000000000284 ) ) ;
#938=VERTEX_POINT ( 'NONE', #16694 ) ;
#951=EDGE_CURVE ( 'NONE', #35648, #2273, #6897, .T. ) ;
#953=CARTESIAN_POINT ( 'NONE',  ( 3.006483450353407250, 7.415254214038215608, 455.0000000000000568 ) ) ;
#954=LINE ( 'NONE', #38420, #18746 ) ;
#966=FACE_OUTER_BOUND ( 'NONE', #3399, .T. ) ;
#967=PLANE ( 'NONE',  #5428 ) ;
#968=ORIENTED_EDGE ( 'NONE', *, *, #62086, .T. ) ;
#975=ORIENTED_EDGE ( 'NONE', *, *, #64139, .T. ) ;
#983=ORIENTED_EDGE ( 'NONE', *, *, #34081, .F. ) ;
#984=ORIENTED_EDGE ( 'NONE', *, *, #42876, .T. ) ;
#985=EDGE_CURVE ( 'NONE', #67402, #14886, #60148, .T. ) ;
#987=EDGE_CURVE ( 'NONE', #52737, #4257, #6425, .T. ) ;
#994=DIRECTION ( 'NONE',  ( -1.053224967557348291E-14, -1.000000000000000000, 0.000000000000000000 ) ) ;
#999=LINE ( 'NONE', #23231, #47913 ) ;
#1004=CARTESIAN_POINT ( 'NONE',  ( -9.293516549646827940, -10.92648345035338764, 455.0000000000000568 ) ) ;
#1006=DIRECTION ( 'NONE',  ( 1.000000000000000000, -2.135044278125299371E-15, -7.844025423732059533E-31 ) ) ;
#1007=PLANE ( 'NONE',  #27095 ) ;
#1009=VECTOR ( 'NONE', #69897, 1000.000000000000114 ) ;
#1016=ORIENTED_EDGE ( 'NONE', *, *, #15929, .T. ) ;
#1034=ADVANCED_FACE ( 'NONE', ( #33964 ), #61177, .T. ) ;
#1041=CARTESIAN_POINT ( 'NONE',  ( -7.813516549646711162, 11.77351654964660277, 455.0000000000000568 ) ) ;
#1050=LINE ( 'NONE', #38193, #15255 ) ;
#1058=DIRECTION ( 'NONE',  ( 0.000000000000000000, 3.673940397442059868E-16, -1.000000000000000000 ) ) ;
#1066=DIRECTION ( 'NONE',  ( -1.836970198721029934E-16, 1.836970198721036344E-16, -1.000000000000000000 ) ) ;
#1070=ORIENTED_EDGE ( 'NONE', *, *, #5352, .T. ) ;
#1094=ORIENTED_EDGE ( 'NONE', *, *, #27274, .F. ) ;
#1099=DIRECTION ( 'NONE',  ( 0.000000000000000000, 0.000000000000000000, 1.000000000000000000 ) ) ;
#1101=LINE ( 'NONE', #28304, #13515 ) ;
#1104=DIRECTION ( 'NONE',  ( 1.836970198721029934E-16, 1.836970198721010706E-16, -1.000000000000000000 ) ) ;
#1106=DIRECTION ( 'NONE',  ( 0.000000000000000000, 0.000000000000000000, -1.000000000000000000 ) ) ;
#1119=CARTESIAN_POINT ( 'NONE',  ( -10.91351654964670637, 9.293516549646604119, 455.0000000000000568 ) ) ;
#1122=VECTOR ( 'NONE', #20226, 1000.000000000000000 ) ;
#1125=DIRECTION ( 'NONE',  ( -1.836970198721029934E-16, 1.836970198721036344E-16, -1.000000000000000000 ) ) ;
#1128=CARTESIAN_POINT ( 'NONE',  ( 10.92648345035337343, -9.306483450353493225, 455.0000000000000568 ) ) ;
#1132=ORIENTED_EDGE ( 'NONE', *, *, #68198, .T. ) ;
#1133=ORIENTED_EDGE ( 'NONE', *, *, #46290, .F. ) ;
#1156=EDGE_CURVE ( 'NONE', #55902, #66560, #52704, .T. ) ;
#1164=CARTESIAN_POINT ( 'NONE',  ( 5.393625297349950110, 4.734785091273829849, 455.0000000000000568 ) ) ;
#1176=LINE ( 'NONE', #22729, #65952 ) ;
#1177=CARTESIAN_POINT ( 'NONE',  ( -11.77351654964669336, -4.186483450353275515, 195.0000000000000284 ) ) ;
#1190=EDGE_CURVE ( 'NONE', #3757, #43775, #51019, .T. ) ;
#1203=ORIENTED_EDGE ( 'NONE', *, *, #20044, .F. ) ;
#1217=LINE ( 'NONE', #22771, #19721 ) ;
#1222=EDGE_CURVE ( 'NONE', #22220, #53770, #14862, .T. ) ;
#1223=ORIENTED_EDGE ( 'NONE', *, *, #46884, .T. ) ;
#1246=PLANE ( 'NONE',  #58564 ) ;
#1249=VECTOR ( 'NONE', #13838, 1000.000000000000114 ) ;
#1266=CIRCLE ( 'NONE', #20449, 0.5999999999999998668 ) ;
#1275=CARTESIAN_POINT ( 'NONE',  ( 2.706483450353419862, 10.91351654964658735, 455.0000000000000568 ) ) ;
#1281=ORIENTED_EDGE ( 'NONE', *, *, #66042, .F. ) ;
#1285=ORIENTED_EDGE ( 'NONE', *, *, #38363, .T. ) ;
#1290=DIRECTION ( 'NONE',  ( -1.000000000000000000, 0.000000000000000000, 0.000000000000000000 ) ) ;
#1297=ADVANCED_FACE ( 'NONE', ( #32859 ), #64347, .F. ) ;
#1298=VERTEX_POINT ( 'NONE', #54091 ) ;
#1300=EDGE_CURVE ( 'NONE', #9609, #39844, #5648, .T. ) ;
#1301=CARTESIAN_POINT ( 'NONE',  ( 4.206483450353343478, -11.12648345035337982, 195.0000000000000284 ) ) ;
#1305=ADVANCED_FACE ( 'NONE', ( #59733 ), #11279, .F. ) ;
#1311=VERTEX_POINT ( 'NONE', #21555 ) ;
#1318=ORIENTED_EDGE ( 'NONE', *, *, #5140, .F. ) ;
#1323=CARTESIAN_POINT ( 'NONE',  ( 7.606483450353376696, 11.77351654964662053, 195.0000000000000284 ) ) ;
#1326=CARTESIAN_POINT ( 'NONE',  ( 6.344579767990823349, -8.406483450353396947, 195.0000000000000284 ) ) ;
#1332=CARTESIAN_POINT ( 'NONE',  ( 6.344579767990823349, -8.406483450353491094, 455.0000000000000568 ) ) ;
#1334=DIRECTION ( 'NONE',  ( -1.084202172485501594E-14, -1.000000000000000000, 0.000000000000000000 ) ) ;
#1336=VERTEX_POINT ( 'NONE', #22257 ) ;
#1339=AXIS2_PLACEMENT_3D ( 'NONE', #35757, #36831, #19845 ) ;
#1349=DIRECTION ( 'NONE',  ( 0.000000000000000000, -1.000000000000000000, -3.673940397442059868E-16 ) ) ;
#1354=DIRECTION ( 'NONE',  ( 0.000000000000000000, 0.000000000000000000, 1.000000000000000000 ) ) ;
#1355=CARTESIAN_POINT ( 'NONE',  ( -7.793516549646712477, 11.11351654964660085, 455.0000000000000568 ) ) ;
#1362=VERTEX_POINT ( 'NONE', #43461 ) ;
#1363=EDGE_CURVE ( 'NONE', #17706, #30714, #5313, .T. ) ;
#1365=AXIS2_PLACEMENT_3D ( 'NONE', #30474, #52049, #14558 ) ;
#1374=ORIENTED_EDGE ( 'NONE', *, *, #51278, .F. ) ;
#1377=LINE ( 'NONE', #60762, #24532 ) ;
#1384=LINE ( 'NONE', #45543, #33091 ) ;
#1393=DIRECTION ( 'NONE',  ( -1.000000000000000000, 0.000000000000000000, 0.000000000000000000 ) ) ;
#1401=EDGE_CURVE ( 'NONE', #2837, #64033, #17624, .T. ) ;
#1406=VERTEX_POINT ( 'NONE', #39528 ) ;
#1410=CARTESIAN_POINT ( 'NONE',  ( -11.18071654964681372, -11.19368345035335821, 455.0000000000000568 ) ) ;
#1412=DIRECTION ( 'NONE',  ( 1.836970198721029934E-16, -1.836970198721036344E-16, 1.000000000000000000 ) ) ;
#1419=DIRECTION ( 'NONE',  ( 1.000000000000000000, -3.491481338843133355E-15, -1.836970198721036344E-16 ) ) ;
#1422=CARTESIAN_POINT ( 'NONE',  ( -7.798499376344109280, -4.740315990920159095, 455.0000000000000568 ) ) ;
#1439=FACE_OUTER_BOUND ( 'NONE', #15747, .T. ) ;
#1441=EDGE_CURVE ( 'NONE', #56939, #1406, #61091, .T. ) ;
#1449=ORIENTED_EDGE ( 'NONE', *, *, #1893, .F. ) ;
#1452=DIRECTION ( 'NONE',  ( -0.000000000000000000, 3.673940397442059868E-16, -1.000000000000000000 ) ) ;
#1455=VECTOR ( 'NONE', #11168, 1000.000000000000000 ) ;
#1463=ORIENTED_EDGE ( 'NONE', *, *, #22319, .T. ) ;
#1469=ORIENTED_EDGE ( 'NONE', *, *, #10867, .T. ) ;
#1470=ORIENTED_EDGE ( 'NONE', *, *, #29362, .T. ) ;
#1490=LINE ( 'NONE', #29402, #14826 ) ;
#1492=CARTESIAN_POINT ( 'NONE',  ( -6.331612867284154511, 8.393516549646601987, 195.0000000000000284 ) ) ;
#1496=CARTESIAN_POINT ( 'NONE',  ( -8.393516549646712122, 6.331612867284047041, 455.0000000000000568 ) ) ;
#1498=ORIENTED_EDGE ( 'NONE', *, *, #56858, .T. ) ;
#1499=FACE_OUTER_BOUND ( 'NONE', #3883, .T. ) ;
#1504=CARTESIAN_POINT ( 'NONE',  ( 9.306483450353418618, 10.91351654964656426, 455.0000000000000568 ) ) ;
#1508=ORIENTED_EDGE ( 'NONE', *, *, #11975, .T. ) ;
#1509=ORIENTED_EDGE ( 'NONE', *, *, #62192, .F. ) ;
#1511=LINE ( 'NONE', #22738, #3157 ) ;
#1516=ORIENTED_EDGE ( 'NONE', *, *, #68122, .F. ) ;
#1524=ORIENTED_EDGE ( 'NONE', *, *, #59667, .T. ) ;
#1525=FACE_OUTER_BOUND ( 'NONE', #31691, .T. ) ;
#1534=EDGE_CURVE ( 'NONE', #42678, #52964, #27904, .T. ) ;
#1543=EDGE_CURVE ( 'NONE', #33912, #33774, #60405, .T. ) ;
#1547=AXIS2_PLACEMENT_3D ( 'NONE', #61946, #34725, #13513 ) ;
#1548=CIRCLE ( 'NONE', #10597, 1.399999999999998579 ) ;
#1552=ORIENTED_EDGE ( 'NONE', *, *, #17669, .F. ) ;
#1556=AXIS2_PLACEMENT_3D ( 'NONE', #57071, #35142, #8635 ) ;
#1561=AXIS2_PLACEMENT_3D ( 'NONE', #7094, #24422, #50240 ) ;
#1562=VECTOR ( 'NONE', #37245, 1000.000000000000000 ) ;
#1564=ORIENTED_EDGE ( 'NONE', *, *, #25883, .T. ) ;
#1565=DIRECTION ( 'NONE',  ( 3.491481338843132961E-15, 1.000000000000000000, 0.000000000000000000 ) ) ;
#1568=LINE ( 'NONE', #18175, #59424 ) ;
#1570=FACE_OUTER_BOUND ( 'NONE', #29203, .T. ) ;
#1572=EDGE_CURVE ( 'NONE', #5389, #36022, #29616, .T. ) ;
#1577=FACE_OUTER_BOUND ( 'NONE', #60002, .T. ) ;
#1581=DIRECTION ( 'NONE',  ( -1.836970198721029934E-16, 1.836970198721036344E-16, -1.000000000000000000 ) ) ;
#1588=DIRECTION ( 'NONE',  ( 0.000000000000000000, 1.000000000000000000, 0.000000000000000000 ) ) ;
#1592=VERTEX_POINT ( 'NONE', #14426 ) ;
#1601=DIRECTION ( 'NONE',  ( -0.6414496315691617934, -0.7671651518152962090, -2.818519042763987834E-16 ) ) ;
#1603=CARTESIAN_POINT ( 'NONE',  ( 11.12648345035337982, -4.206483450353492692, 455.0000000000000568 ) ) ;
#1609=DIRECTION ( 'NONE',  ( 3.614007241618349165E-15, 1.000000000000000000, 0.000000000000000000 ) ) ;
#1613=AXIS2_PLACEMENT_3D ( 'NONE', #62679, #69039, #20597 ) ;
#1618=ORIENTED_EDGE ( 'NONE', *, *, #42670, .T. ) ;
#1619=CARTESIAN_POINT ( 'NONE',  ( -1.077516549646670541, 11.33351654964656596, 455.0000000000000568 ) ) ;
#1622=ADVANCED_FACE ( 'NONE', ( #8046 ), #52613, .F. ) ;
#1639=AXIS2_PLACEMENT_3D ( 'NONE', #45428, #66654, #67362 ) ;
#1644=VECTOR ( 'NONE', #60064, 1000.000000000000000 ) ;
#1649=CARTESIAN_POINT ( 'NONE',  ( -4.727349090213463612, 7.798499376343949407, 455.0000000000000568 ) ) ;
#1655=ORIENTED_EDGE ( 'NONE', *, *, #59855, .T. ) ;
#1664=EDGE_CURVE ( 'NONE', #31939, #11916, #24681, .T. ) ;
#1667=CARTESIAN_POINT ( 'NONE',  ( -4.188533722949374649, -7.272650909786617213, 195.0000000000000284 ) ) ;
#1672=EDGE_CURVE ( 'NONE', #26901, #3811, #20074, .T. ) ;
#1689=DIRECTION ( 'NONE',  ( -1.000000000000000000, 0.000000000000000000, 0.000000000000000000 ) ) ;
#1691=ADVANCED_FACE ( 'NONE', ( #48690 ), #32440, .F. ) ;
#1695=ORIENTED_EDGE ( 'NONE', *, *, #58865, .T. ) ;
#1702=CIRCLE ( 'NONE', #54821, 0.3999999999999993006 ) ;
#1703=CARTESIAN_POINT ( 'NONE',  ( 11.78648345035335865, 7.813516549646607245, 195.0000000000000284 ) ) ;
#1712=EDGE_CURVE ( 'NONE', #65266, #65838, #58954, .T. ) ;
#1714=CARTESIAN_POINT ( 'NONE',  ( -11.77351654964669514, -4.406483450353273490, 195.0000000000000284 ) ) ;
#1727=DIRECTION ( 'NONE',  ( -1.000000000000000000, 0.000000000000000000, 0.000000000000000000 ) ) ;
#1730=ORIENTED_EDGE ( 'NONE', *, *, #55564, .T. ) ;
#1732=DIRECTION ( 'NONE',  ( -1.000000000000000000, 1.214636490590110115E-14, -1.836970198721007501E-16 ) ) ;
#1734=ORIENTED_EDGE ( 'NONE', *, *, #15533, .T. ) ;
#1740=EDGE_CURVE ( 'NONE', #48692, #36045, #21815, .T. ) ;
#1742=CIRCLE ( 'NONE', #37914, 0.1999999999999987899 ) ;
#1743=VECTOR ( 'NONE', #55400, 1000.000000000000114 ) ;
#1773=ORIENTED_EDGE ( 'NONE', *, *, #26359, .F. ) ;
#1795=EDGE_CURVE ( 'NONE', #57965, #33976, #20768, .T. ) ;
#1796=AXIS2_PLACEMENT_3D ( 'NONE', #20618, #52462, #63772 ) ;
#1802=EDGE_CURVE ( 'NONE', #23208, #33832, #4865, .T. ) ;
#1804=VECTOR ( 'NONE', #62363, 1000.000000000000000 ) ;
#1809=ORIENTED_EDGE ( 'NONE', *, *, #53810, .T. ) ;
#1813=ORIENTED_EDGE ( 'NONE', *, *, #23355, .F. ) ;
#1814=CIRCLE ( 'NONE', #10853, 0.2000000000000005107 ) ;
#1815=CARTESIAN_POINT ( 'NONE',  ( 9.247904806590725002, 9.942044687070426434, 455.0000000000000568 ) ) ;
#1817=LINE ( 'NONE', #28008, #25247 ) ;
#1821=AXIS2_PLACEMENT_3D ( 'NONE', #4575, #30737, #41337 ) ;
#1831=CIRCLE ( 'NONE', #69596, 0.2000000000000005107 ) ;
#1835=EDGE_CURVE ( 'NONE', #47486, #64753, #4652, .T. ) ;
#1837=CARTESIAN_POINT ( 'NONE',  ( 11.12648345035337627, -2.906483450353491094, 455.0000000000000568 ) ) ;
#1853=ORIENTED_EDGE ( 'NONE', *, *, #28054, .F. ) ;
#1858=FACE_OUTER_BOUND ( 'NONE', #31054, .T. ) ;
#1860=DIRECTION ( 'NONE',  ( -1.047444401652940007E-14, -1.000000000000000000, -1.836970198721029934E-16 ) ) ;
#1879=CARTESIAN_POINT ( 'NONE',  ( -2.752095193409509033, -9.955011587777317317, 455.0000000000000568 ) ) ;
#1880=CARTESIAN_POINT ( 'NONE',  ( 1.866219381641426533, -9.417013320880872840, 455.0000000000000568 ) ) ;
#1881=DIRECTION ( 'NONE',  ( -1.836970198721029934E-16, 1.836970198721036344E-16, -1.000000000000000000 ) ) ;
#1884=ORIENTED_EDGE ( 'NONE', *, *, #34073, .T. ) ;
#1893=EDGE_CURVE ( 'NONE', #37032, #63752, #50757, .T. ) ;
#1894=CARTESIAN_POINT ( 'NONE',  ( 4.201500623656003519, -4.740315990920286104, 455.0000000000000568 ) ) ;
#1895=CYLINDRICAL_SURFACE ( 'NONE', #21751, 0.5999999999999989786 ) ;
#1900=VECTOR ( 'NONE', #62542, 1000.000000000000000 ) ;
#1902=ORIENTED_EDGE ( 'NONE', *, *, #52669, .F. ) ;
#1913=VECTOR ( 'NONE', #20902, 1000.000000000000000 ) ;
#1918=ORIENTED_EDGE ( 'NONE', *, *, #23000, .F. ) ;
#1931=CARTESIAN_POINT ( 'NONE',  ( -11.77351654964670935, 4.173516549646604901, 455.0000000000000568 ) ) ;
#1933=CARTESIAN_POINT ( 'NONE',  ( -11.77351654964679284, -7.826483450353365789, 455.0000000000000568 ) ) ;
#1935=ORIENTED_EDGE ( 'NONE', *, *, #52374, .T. ) ;
#1949=EDGE_CURVE ( 'NONE', #587, #58549, #27821, .T. ) ;
#1952=AXIS2_PLACEMENT_3D ( 'NONE', #45923, #56869, #26031 ) ;
#1955=CYLINDRICAL_SURFACE ( 'NONE', #9476, 0.1999999999999987899 ) ;
#1965=CARTESIAN_POINT ( 'NONE',  ( -11.11351654964674118, -4.206483450353336373, 455.0000000000000568 ) ) ;
#1974=CARTESIAN_POINT ( 'NONE',  ( -10.73351654964669599, -1.690483450353341910, 455.0000000000000568 ) ) ;
#1976=ADVANCED_FACE ( 'NONE', ( #38768 ), #60322, .F. ) ;
#1977=CARTESIAN_POINT ( 'NONE',  ( -4.727349090213461835, 4.188533722949259186, 455.0000000000000568 ) ) ;
#1978=VERTEX_POINT ( 'NONE', #60680 ) ;
#1982=CYLINDRICAL_SURFACE ( 'NONE', #24707, 0.1999999999999987899 ) ;
#1983=DIRECTION ( 'NONE',  ( -1.836970198721029934E-16, 1.836970198721036344E-16, -1.000000000000000000 ) ) ;
#1987=DIRECTION ( 'NONE',  ( -0.000000000000000000, 3.673940397442059868E-16, -1.000000000000000000 ) ) ;
#1996=EDGE_CURVE ( 'NONE', #37495, #25592, #19996, .T. ) ;
#2001=AXIS2_PLACEMENT_3D ( 'NONE', #69068, #14987, #42194 ) ;
#2002=CARTESIAN_POINT ( 'NONE',  ( -4.609516549646713202, 3.593516549646603941, 455.0000000000000568 ) ) ;
#2004=CIRCLE ( 'NONE', #41532, 0.8128000000000145109 ) ;
#2006=ORIENTED_EDGE ( 'NONE', *, *, #4750, .T. ) ;
#2023=EDGE_CURVE ( 'NONE', #26897, #48692, #25302, .T. ) ;
#2026=CARTESIAN_POINT ( 'NONE',  ( -7.793516549646712477, 11.11351654964660085, 455.0000000000000568 ) ) ;
#2033=CARTESIAN_POINT ( 'NONE',  ( -11.77351654964674132, -4.186483450353323477, 455.0000000000000568 ) ) ;
#2040=CARTESIAN_POINT ( 'NONE',  ( 12.00648345035338060, -7.826483450353491023, 455.0000000000000568 ) ) ;
#2043=LINE ( 'NONE', #11941, #38994 ) ;
#2046=CARTESIAN_POINT ( 'NONE',  ( 9.106483450353371367, 10.91351654964661222, 195.0000000000000284 ) ) ;
#2064=VECTOR ( 'NONE', #49003, 1000.000000000000000 ) ;
#2074=CARTESIAN_POINT ( 'NONE',  ( -7.793516549646781755, -11.12648345035335851, 195.0000000000000284 ) ) ;
#2080=VERTEX_POINT ( 'NONE', #40142 ) ;
#2087=DIRECTION ( 'NONE',  ( 0.000000000000000000, -0.000000000000000000, -1.000000000000000000 ) ) ;
#2113=ORIENTED_EDGE ( 'NONE', *, *, #32730, .T. ) ;
#2117=EDGE_CURVE ( 'NONE', #12465, #8340, #16094, .T. ) ;
#2120=ORIENTED_EDGE ( 'NONE', *, *, #67768, .T. ) ;
#2124=DIRECTION ( 'NONE',  ( -0.7071067811865422437, 0.7071067811865529018, 2.597868168706500319E-16 ) ) ;
#2133=DIRECTION ( 'NONE',  ( -0.7071067811865503483, 0.7071067811865446862, 0.000000000000000000 ) ) ;
#2136=LINE ( 'NONE', #46317, #42637 ) ;
#2158=CYLINDRICAL_SURFACE ( 'NONE', #17188, 0.1999999999999987899 ) ;
#2166=AXIS2_PLACEMENT_3D ( 'NONE', #23921, #45474, #57146 ) ;
#2167=DIRECTION ( 'NONE',  ( 0.000000000000000000, -1.000000000000000000, 0.000000000000000000 ) ) ;
#2169=ORIENTED_EDGE ( 'NONE', *, *, #43684, .T. ) ;
#2172=DIRECTION ( 'NONE',  ( 0.5000000000000018874, 0.8660254037844374864, 0.000000000000000000 ) ) ;
#2174=ORIENTED_EDGE ( 'NONE', *, *, #51095, .F. ) ;
#2177=VERTEX_POINT ( 'NONE', #48527 ) ;
#2178=PLANE ( 'NONE',  #57907 ) ;
#2182=CARTESIAN_POINT ( 'NONE',  ( 10.20488345035338185, -9.804883450353433005, 195.0000000000000284 ) ) ;
#2191=CARTESIAN_POINT ( 'NONE',  ( 8.406483450353379183, -7.616533956692230767, 195.0000000000000284 ) ) ;
#2195=EDGE_CURVE ( 'NONE', #66560, #16506, #36375, .T. ) ;
#2198=VECTOR ( 'NONE', #62489, 1000.000000000000000 ) ;
#2204=CARTESIAN_POINT ( 'NONE',  ( 10.20488345035338007, -11.48848345035349361, 455.0000000000000568 ) ) ;
#2205=DIRECTION ( 'NONE',  ( -5.163402228214836012E-15, -1.000000000000000000, -1.836970198721026976E-16 ) ) ;
#2208=ORIENTED_EDGE ( 'NONE', *, *, #34444, .F. ) ;
#2212=VECTOR ( 'NONE', #34453, 1000.000000000000000 ) ;
#2220=LINE ( 'NONE', #9989, #10523 ) ;
#2221=ORIENTED_EDGE ( 'NONE', *, *, #37349, .F. ) ;
#2223=LINE ( 'NONE', #1880, #6116 ) ;
#2227=CARTESIAN_POINT ( 'NONE',  ( 2.906483450353342324, -11.12648345035346331, 455.0000000000000568 ) ) ;
#2230=EDGE_CURVE ( 'NONE', #2766, #7775, #69754, .T. ) ;
#2237=LINE ( 'NONE', #34390, #32211 ) ;
#2248=DIRECTION ( 'NONE',  ( 3.540573132209560831E-15, 1.000000000000000000, 0.000000000000000000 ) ) ;
#2249=AXIS2_PLACEMENT_3D ( 'NONE', #19984, #47557, #41895 ) ;
#2253=AXIS2_PLACEMENT_3D ( 'NONE', #30312, #18636, #24657 ) ;
#2258=AXIS2_PLACEMENT_3D ( 'NONE', #60030, #16573, #11580 ) ;
#2273=VERTEX_POINT ( 'NONE', #34675 ) ;
#2275=AXIS2_PLACEMENT_3D ( 'NONE', #4400, #54225, #27350 ) ;
#2277=LINE ( 'NONE', #66968, #53206 ) ;
#2281=DIRECTION ( 'NONE',  ( 1.000000000000000000, -1.261617073437657577E-14, 0.000000000000000000 ) ) ;
#2305=CARTESIAN_POINT ( 'NONE',  ( -10.91351654964670637, 2.693516549646604030, 195.0000000000000284 ) ) ;
#2306=ORIENTED_EDGE ( 'NONE', *, *, #38956, .T. ) ;
#2307=CARTESIAN_POINT ( 'NONE',  ( -12.00854180281611328, 7.798491296477224388, 195.0000000000000284 ) ) ;
#2310=VECTOR ( 'NONE', #48676, 1000.000000000000000 ) ;
#2312=AXIS2_PLACEMENT_3D ( 'NONE', #15326, #32283, #31597 ) ;
#2315=ORIENTED_EDGE ( 'NONE', *, *, #9003, .T. ) ;
#2317=DIRECTION ( 'NONE',  ( -0.000000000000000000, -0.000000000000000000, -1.000000000000000000 ) ) ;
#2318=DIRECTION ( 'NONE',  ( 0.000000000000000000, 1.000000000000000000, 0.000000000000000000 ) ) ;
#2320=VECTOR ( 'NONE', #388, 1000.000000000000000 ) ;
#2329=ADVANCED_FACE ( 'NONE', ( #50601 ), #2158, .T. ) ;
#2330=LINE ( 'NONE', #18232, #35409 ) ;
#2335=ORIENTED_EDGE ( 'NONE', *, *, #39615, .F. ) ;
#2338=DIRECTION ( 'NONE',  ( 8.673617379884087537E-15, 1.000000000000000000, 0.000000000000000000 ) ) ;
#2341=ORIENTED_EDGE ( 'NONE', *, *, #2759, .T. ) ;
#2349=LINE ( 'NONE', #29206, #63370 ) ;
#2352=ORIENTED_EDGE ( 'NONE', *, *, #66934, .T. ) ;
#2354=AXIS2_PLACEMENT_3D ( 'NONE', #339, #693, #53051 ) ;
#2355=FACE_OUTER_BOUND ( 'NONE', #33408, .T. ) ;
#2357=DIRECTION ( 'NONE',  ( -1.000000000000000000, 9.799566706031580591E-15, 1.836970198721047683E-16 ) ) ;
#2358=VECTOR ( 'NONE', #30939, 1000.000000000000000 ) ;
#2364=EDGE_CURVE ( 'NONE', #53484, #9595, #62357, .T. ) ;
#2365=CARTESIAN_POINT ( 'NONE',  ( -8.393516549646712122, 5.655420232009161552, 455.0000000000000568 ) ) ;
#2376=LINE ( 'NONE', #23939, #14254 ) ;
#2386=DIRECTION ( 'NONE',  ( 8.673617379884087537E-15, 1.000000000000000000, 0.000000000000000000 ) ) ;
#2412=CARTESIAN_POINT ( 'NONE',  ( -4.193516549646831848, -11.12648345035344377, 455.0000000000000568 ) ) ;
#2422=ADVANCED_FACE ( 'NONE', ( #9572 ), #8499, .F. ) ;
#2424=VERTEX_POINT ( 'NONE', #68262 ) ;
#2431=DIRECTION ( 'NONE',  ( -3.540573132209561620E-15, -1.000000000000000000, 0.000000000000000000 ) ) ;
#2441=AXIS2_PLACEMENT_3D ( 'NONE', #6036, #10297, #26560 ) ;
#2442=ORIENTED_EDGE ( 'NONE', *, *, #45546, .T. ) ;
#2443=LINE ( 'NONE', #17668, #50449 ) ;
#2462=LINE ( 'NONE', #24027, #12594 ) ;
#2463=CIRCLE ( 'NONE', #30697, 0.3999999999999993006 ) ;
#2474=CARTESIAN_POINT ( 'NONE',  ( -11.07551654964667520, 11.07551654964660237, 455.0000000000000568 ) ) ;
#2476=DIRECTION ( 'NONE',  ( 0.7071067811865500152, 0.7071067811865451302, -4.361490581750784942E-31 ) ) ;
#2480=DIRECTION ( 'NONE',  ( 0.000000000000000000, -1.000000000000000000, 0.000000000000000000 ) ) ;
#2484=DIRECTION ( 'NONE',  ( 1.836970198721029934E-16, 1.836970198721010706E-16, -1.000000000000000000 ) ) ;
#2488=CIRCLE ( 'NONE', #52211, 0.5999999999999989786 ) ;
#2491=DIRECTION ( 'NONE',  ( -1.836970198721029934E-16, 1.836970198721036344E-16, -1.000000000000000000 ) ) ;
#2496=ORIENTED_EDGE ( 'NONE', *, *, #63798, .T. ) ;
#2498=CARTESIAN_POINT ( 'NONE',  ( 4.740315990920131561, -4.201500623656145628, 455.0000000000000568 ) ) ;
#2500=CARTESIAN_POINT ( 'NONE',  ( 8.406483450353379183, -5.668387132715952959, 195.0000000000000284 ) ) ;
#2501=ORIENTED_EDGE ( 'NONE', *, *, #12826, .T. ) ;
#2511=AXIS2_PLACEMENT_3D ( 'NONE', #14849, #13782, #36403 ) ;
#2512=ORIENTED_EDGE ( 'NONE', *, *, #17816, .F. ) ;
#2531=CARTESIAN_POINT ( 'NONE',  ( -5.655420232009359616, -8.406483450353428921, 455.0000000000000568 ) ) ;
#2535=CARTESIAN_POINT ( 'NONE',  ( 10.74648345035338082, -1.090483450353491035, 455.0000000000000568 ) ) ;
#2537=EDGE_LOOP ( 'NONE', ( #68844, #37953, #46584, #8427 ) ) ;
#2540=DIRECTION ( 'NONE',  ( -0.7071067811865552333, -0.7071067811865398012, 2.389338318698257180E-30 ) ) ;
#2559=ORIENTED_EDGE ( 'NONE', *, *, #20044, .T. ) ;
#2560=EDGE_CURVE ( 'NONE', #16514, #20589, #58711, .T. ) ;
#2561=ORIENTED_EDGE ( 'NONE', *, *, #24346, .F. ) ;
#2562=EDGE_CURVE ( 'NONE', #25048, #26901, #17231, .T. ) ;
#2571=EDGE_CURVE ( 'NONE', #8498, #4905, #5331, .T. ) ;
#2590=ORIENTED_EDGE ( 'NONE', *, *, #59099, .F. ) ;
#2598=EDGE_LOOP ( 'NONE', ( #37550, #60580, #10876, #67982 ) ) ;
#2610=CARTESIAN_POINT ( 'NONE',  ( 7.826483450353380000, -12.00648345035349251, 455.0000000000000568 ) ) ;
#2617=AXIS2_PLACEMENT_3D ( 'NONE', #2474, #24038, #67175 ) ;
#2630=CARTESIAN_POINT ( 'NONE',  ( 7.826483450353380000, -12.00648345035339659, 195.0000000000000284 ) ) ;
#2638=EDGE_CURVE ( 'NONE', #58346, #66347, #1384, .T. ) ;
#2639=DIRECTION ( 'NONE',  ( 0.4999999999999695799, -0.8660254037844563602, -6.723777587269172655E-17 ) ) ;
#2640=ORIENTED_EDGE ( 'NONE', *, *, #46648, .T. ) ;
#2642=DIRECTION ( 'NONE',  ( 0.000000000000000000, -1.000000000000000000, 0.000000000000000000 ) ) ;
#2643=DIRECTION ( 'NONE',  ( -0.7071067811865486830, -0.7071067811865464625, -2.597868168706476160E-16 ) ) ;
#2647=PLANE ( 'NONE',  #1639 ) ;
#2649=DIRECTION ( 'NONE',  ( -1.836970198721029934E-16, 1.836970198721036344E-16, -1.000000000000000000 ) ) ;
#2651=CARTESIAN_POINT ( 'NONE',  ( -5.993516549646776603, -6.006483450353426790, 455.0000000000000568 ) ) ;
#2660=ORIENTED_EDGE ( 'NONE', *, *, #24158, .F. ) ;
#2661=AXIS2_PLACEMENT_3D ( 'NONE', #26499, #21210, #27203 ) ;
#2662=VECTOR ( 'NONE', #46837, 1000.000000000000000 ) ;
#2678=ORIENTED_EDGE ( 'NONE', *, *, #28225, .T. ) ;
#2691=VECTOR ( 'NONE', #48240, 1000.000000000000000 ) ;
#2694=CARTESIAN_POINT ( 'NONE',  ( 1.690483450353371442, 10.73351654964664270, 195.0000000000000284 ) ) ;
#2696=EDGE_CURVE ( 'NONE', #5555, #39293, #38859, .T. ) ;
#2697=AXIS2_PLACEMENT_3D ( 'NONE', #28551, #66728, #61412 ) ;
#2707=VECTOR ( 'NONE', #68907, 1000.000000000000000 ) ;
#2715=CARTESIAN_POINT ( 'NONE',  ( -5.993516549646728642, -6.006483450353378828, 195.0000000000000284 ) ) ;
#2723=VECTOR ( 'NONE', #11038, 1000.000000000000000 ) ;
#2735=DIRECTION ( 'NONE',  ( 1.836970198721029934E-16, 1.836970198721010706E-16, -1.000000000000000000 ) ) ;
#2744=DIRECTION ( 'NONE',  ( 0.000000000000000000, 1.000000000000000000, 0.000000000000000000 ) ) ;
#2751=CARTESIAN_POINT ( 'NONE',  ( -11.47551654964667733, 11.07551654964660237, 455.0000000000000568 ) ) ;
#2754=AXIS2_PLACEMENT_3D ( 'NONE', #13905, #46769, #35456 ) ;
#2755=CARTESIAN_POINT ( 'NONE',  ( -10.91351654964680584, -9.306483450353375986, 455.0000000000000568 ) ) ;
#2758=CARTESIAN_POINT ( 'NONE',  ( -9.791916549646712653, 11.07551654964660415, 455.0000000000000568 ) ) ;
#2759=EDGE_CURVE ( 'NONE', #24541, #35101, #55139, .T. ) ;
#2766=VERTEX_POINT ( 'NONE', #44500 ) ;
#2770=VECTOR ( 'NONE', #60601, 1000.000000000000000 ) ;
#2771=CARTESIAN_POINT ( 'NONE',  ( 4.747751991980625696, -6.619341603356940773, 455.0000000000000568 ) ) ;
#2778=AXIS2_PLACEMENT_3D ( 'NONE', #65398, #60078, #11625 ) ;
#2782=LINE ( 'NONE', #45561, #33592 ) ;
#2799=ORIENTED_EDGE ( 'NONE', *, *, #32986, .F. ) ;
#2804=CARTESIAN_POINT ( 'NONE',  ( 4.396432944014527777, -8.406483450353478659, 455.0000000000000568 ) ) ;
#2807=AXIS2_PLACEMENT_3D ( 'NONE', #9613, #36474, #40383 ) ;
#2811=EDGE_CURVE ( 'NONE', #35986, #61486, #68533, .T. ) ;
#2812=CARTESIAN_POINT ( 'NONE',  ( 10.09643294401453417, 2.893516549646536262, 455.0000000000000568 ) ) ;
#2814=AXIS2_PLACEMENT_3D ( 'NONE', #25463, #64680, #44144 ) ;
#2837=VERTEX_POINT ( 'NONE', #20090 ) ;
#2839=CARTESIAN_POINT ( 'NONE',  ( 9.955011587777235604, -9.247904806590705462, 195.0000000000000284 ) ) ;
#2846=CARTESIAN_POINT ( 'NONE',  ( -10.73351654964671020, 1.677516549646604016, 455.0000000000000568 ) ) ;
#2857=VECTOR ( 'NONE', #68920, 1000.000000000000000 ) ;
#2875=DIRECTION ( 'NONE',  ( 6.308085367188446447E-15, 1.000000000000000000, 3.673940397442059868E-16 ) ) ;
#2879=VECTOR ( 'NONE', #22312, 1000.000000000000000 ) ;
#2883=DIRECTION ( 'NONE',  ( 1.000000000000000000, -3.491481338843132961E-15, 0.000000000000000000 ) ) ;
#2888=ORIENTED_EDGE ( 'NONE', *, *, #28482, .F. ) ;
#2890=EDGE_CURVE ( 'NONE', #66424, #5664, #62870, .T. ) ;
#2891=FACE_OUTER_BOUND ( 'NONE', #4618, .T. ) ;
#2892=ORIENTED_EDGE ( 'NONE', *, *, #4662, .T. ) ;
#2895=ADVANCED_FACE ( 'NONE', ( #51565 ), #35995, .F. ) ;
#2900=DIRECTION ( 'NONE',  ( 1.836970198721029934E-16, -1.836970198721036344E-16, 1.000000000000000000 ) ) ;
#2904=DIRECTION ( 'NONE',  ( -1.836970198721029934E-16, 1.836970198721036344E-16, -1.000000000000000000 ) ) ;
#2906=CIRCLE ( 'NONE', #51463, 0.6000000000000006439 ) ;
#2913=CARTESIAN_POINT ( 'NONE',  ( -3.593516549646728286, -6.006483450353403697, 195.0000000000000284 ) ) ;
#2918=DIRECTION ( 'NONE',  ( 1.000000000000000000, -7.304098846218132892E-15, 0.000000000000000000 ) ) ;
#2921=VECTOR ( 'NONE', #20071, 1000.000000000000000 ) ;
#2926=CARTESIAN_POINT ( 'NONE',  ( 11.78648345035340661, 7.593516549646560421, 455.0000000000000568 ) ) ;
#2934=DIRECTION ( 'NONE',  ( 1.836970198721029934E-16, 1.836970198721010706E-16, -1.000000000000000000 ) ) ;
#2942=EDGE_CURVE ( 'NONE', #1978, #5458, #18484, .T. ) ;
#2958=VERTEX_POINT ( 'NONE', #23864 ) ;
#2959=ORIENTED_EDGE ( 'NONE', *, *, #66910, .F. ) ;
#2960=VECTOR ( 'NONE', #59887, 1000.000000000000000 ) ;
#2961=DIRECTION ( 'NONE',  ( 0.000000000000000000, 3.673940397442059868E-16, -1.000000000000000000 ) ) ;
#2963=FACE_OUTER_BOUND ( 'NONE', #3451, .T. ) ;
#2968=VECTOR ( 'NONE', #30045, 1000.000000000000000 ) ;
#2970=DIRECTION ( 'NONE',  ( 0.000000000000000000, 1.000000000000000000, 0.000000000000000000 ) ) ;
#2972=EDGE_CURVE ( 'NONE', #62416, #64892, #20723, .T. ) ;
#2973=CARTESIAN_POINT ( 'NONE',  ( 4.740315990920191958, 4.188533722949208560, 455.0000000000000568 ) ) ;
#2977=VECTOR ( 'NONE', #69791, 1000.000000000000000 ) ;
#2983=ADVANCED_FACE ( 'NONE', ( #50387 ), #1955, .F. ) ;
#2990=VECTOR ( 'NONE', #61660, 1000.000000000000000 ) ;
#3002=EDGE_CURVE ( 'NONE', #59936, #58981, #21890, .T. ) ;
#3010=DIRECTION ( 'NONE',  ( 1.836970198721029934E-16, 1.836970198721010706E-16, -1.000000000000000000 ) ) ;
#3013=DIRECTION ( 'NONE',  ( -0.000000000000000000, 3.673940397442059868E-16, -1.000000000000000000 ) ) ;
#3017=VECTOR ( 'NONE', #61130, 1000.000000000000000 ) ;
#3025=VECTOR ( 'NONE', #58679, 1000.000000000000000 ) ;
#3026=AXIS2_PLACEMENT_3D ( 'NONE', #42452, #64715, #32884 ) ;
#3027=CARTESIAN_POINT ( 'NONE',  ( 6.006483450353379716, -6.006483450353394815, 195.0000000000000284 ) ) ;
#3029=CARTESIAN_POINT ( 'NONE',  ( 11.78648345035337819, -7.606483450353493936, 455.0000000000000568 ) ) ;
#3035=ADVANCED_FACE ( 'NONE', ( #68053 ), #42222, .F. ) ;
#3038=ORIENTED_EDGE ( 'NONE', *, *, #38237, .T. ) ;
#3040=LINE ( 'NONE', #40852, #69302 ) ;
#3043=DIRECTION ( 'NONE',  ( 0.000000000000000000, 1.000000000000000000, 0.000000000000000000 ) ) ;
#3045=ORIENTED_EDGE ( 'NONE', *, *, #7343, .T. ) ;
#3049=CARTESIAN_POINT ( 'NONE',  ( 6.006483450353353959, 5.993516549646629166, 195.0000000000000284 ) ) ;
#3073=CARTESIAN_POINT ( 'NONE',  ( 11.48848345035341900, 10.19191654964656202, 455.0000000000000568 ) ) ;
#3075=EDGE_LOOP ( 'NONE', ( #56979, #48373, #24959, #46643 ) ) ;
#3080=VECTOR ( 'NONE', #15220, 1000.000000000000000 ) ;
#3087=ADVANCED_FACE ( 'NONE', ( #62380 ), #25269, .T. ) ;
#3091=FACE_OUTER_BOUND ( 'NONE', #46101, .T. ) ;
#3097=CARTESIAN_POINT ( 'NONE',  ( -7.593516549646838421, -11.78648345035340839, 455.0000000000000568 ) ) ;
#3099=DIRECTION ( 'NONE',  ( 0.7071067811865475727, 0.7071067811865475727, -0.000000000000000000 ) ) ;
#3102=ORIENTED_EDGE ( 'NONE', *, *, #58936, .F. ) ;
#3106=DIRECTION ( 'NONE',  ( 1.000000000000000000, -1.047444401652940007E-14, 1.836970198721010706E-16 ) ) ;
#3108=ORIENTED_EDGE ( 'NONE', *, *, #3126, .F. ) ;
#3111=VECTOR ( 'NONE', #58580, 1000.000000000000000 ) ;
#3112=CARTESIAN_POINT ( 'NONE',  ( -8.393516549646779623, -6.344579767990844665, 455.0000000000000568 ) ) ;
#3126=EDGE_CURVE ( 'NONE', #24433, #9595, #36569, .T. ) ;
#3141=CARTESIAN_POINT ( 'NONE',  ( 6.006483450353361953, 8.198316549646628815, 195.0000000000000284 ) ) ;
#3142=EDGE_LOOP ( 'NONE', ( #23809, #13514, #32415, #24549 ) ) ;
#3144=CARTESIAN_POINT ( 'NONE',  ( 6.006483450353353959, 5.993516549646629166, 195.0000000000000284 ) ) ;
#3145=EDGE_CURVE ( 'NONE', #44522, #21711, #50139, .T. ) ;
#3146=CARTESIAN_POINT ( 'NONE',  ( -5.380658396643321240, -7.265214908726175480, 455.0000000000000568 ) ) ;
#3157=VECTOR ( 'NONE', #6137, 1000.000000000000000 ) ;
#3161=ORIENTED_EDGE ( 'NONE', *, *, #21418, .T. ) ;
#3169=CARTESIAN_POINT ( 'NONE',  ( 1.690483450353415629, 9.828310488885938057, 455.0000000000000568 ) ) ;
#3175=DIRECTION ( 'NONE',  ( -1.000000000000000000, 0.000000000000000000, 0.000000000000000000 ) ) ;
#3180=AXIS2_PLACEMENT_3D ( 'NONE', #30604, #20685, #15398 ) ;
#3184=CARTESIAN_POINT ( 'NONE',  ( 1.690483450353351458, -9.841277389592800517, 455.0000000000000568 ) ) ;
#3207=CARTESIAN_POINT ( 'NONE',  ( 8.211283450353379365, -6.006483450353394815, 195.0000000000000284 ) ) ;
#3209=VERTEX_POINT ( 'NONE', #15715 ) ;
#3211=CARTESIAN_POINT ( 'NONE',  ( 11.78648345035337819, -7.606483450353493936, 455.0000000000000568 ) ) ;
#3223=ORIENTED_EDGE ( 'NONE', *, *, #41811, .T. ) ;
#3232=EDGE_LOOP ( 'NONE', ( #29472, #40885, #34702, #23697 ) ) ;
#3235=CARTESIAN_POINT ( 'NONE',  ( 8.406483450353379183, -5.668387132716048882, 455.0000000000000568 ) ) ;
#3241=FACE_OUTER_BOUND ( 'NONE', #11427, .T. ) ;
#3246=VERTEX_POINT ( 'NONE', #37285 ) ;
#3251=LINE ( 'NONE', #20210, #35750 ) ;
#3253=EDGE_CURVE ( 'NONE', #49587, #26502, #48936, .T. ) ;
#3256=ORIENTED_EDGE ( 'NONE', *, *, #22041, .F. ) ;
#3257=CARTESIAN_POINT ( 'NONE',  ( 1.090483450353420425, 11.33351654964659971, 455.0000000000000568 ) ) ;
#3266=ORIENTED_EDGE ( 'NONE', *, *, #38956, .F. ) ;
#3271=CARTESIAN_POINT ( 'NONE',  ( -11.33351654964668676, -1.090483450353329165, 455.0000000000000568 ) ) ;
#3275=DIRECTION ( 'NONE',  ( -0.000000000000000000, -0.000000000000000000, -1.000000000000000000 ) ) ;
#3276=ORIENTED_EDGE ( 'NONE', *, *, #32419, .F. ) ;
#3278=LINE ( 'NONE', #24848, #10360 ) ;
#3285=LINE ( 'NONE', #62322, #4134 ) ;
#3292=ORIENTED_EDGE ( 'NONE', *, *, #47515, .F. ) ;
#3294=CARTESIAN_POINT ( 'NONE',  ( -7.252248008019455128, 5.380658396643134722, 455.0000000000000568 ) ) ;
#3312=LINE ( 'NONE', #47159, #48567 ) ;
#3317=AXIS2_PLACEMENT_3D ( 'NONE', #23011, #24669, #56830 ) ;
#3318=ADVANCED_FACE ( 'NONE', ( #16408 ), #37985, .F. ) ;
#3321=PLANE ( 'NONE',  #17664 ) ;
#3328=CYLINDRICAL_SURFACE ( 'NONE', #13095, 0.4000000000000010214 ) ;
#3332=DIRECTION ( 'NONE',  ( 1.115702204244422993E-14, 1.000000000000000000, 1.836970198721015882E-16 ) ) ;
#3341=VECTOR ( 'NONE', #5233, 1000.000000000000000 ) ;
#3343=ORIENTED_EDGE ( 'NONE', *, *, #39047, .F. ) ;
#3350=CARTESIAN_POINT ( 'NONE',  ( -11.07551654964683330, -11.48848345035333907, 455.0000000000000568 ) ) ;
#3356=DIRECTION ( 'NONE',  ( 1.836970198721029934E-16, 1.836970198721010706E-16, -1.000000000000000000 ) ) ;
#3363=VECTOR ( 'NONE', #67292, 1000.000000000000000 ) ;
#3371=EDGE_CURVE ( 'NONE', #56924, #37001, #24051, .T. ) ;
#3376=EDGE_CURVE ( 'NONE', #587, #30271, #29014, .T. ) ;
#3395=DIRECTION ( 'NONE',  ( 0.000000000000000000, 0.000000000000000000, 1.000000000000000000 ) ) ;
#3398=PLANE ( 'NONE',  #17543 ) ;
#3399=EDGE_LOOP ( 'NONE', ( #57939, #47283, #25392, #29218 ) ) ;
#3410=VECTOR ( 'NONE', #21932, 1000.000000000000000 ) ;
#3413=DIRECTION ( 'NONE',  ( 1.920885163218982051E-15, 1.000000000000000000, 1.836970198721033139E-16 ) ) ;
#3417=DIRECTION ( 'NONE',  ( -0.000000000000000000, -0.000000000000000000, -1.000000000000000000 ) ) ;
#3425=ORIENTED_EDGE ( 'NONE', *, *, #10973, .F. ) ;
#3430=EDGE_CURVE ( 'NONE', #58177, #49212, #18750, .T. ) ;
#3432=LINE ( 'NONE', #46902, #51843 ) ;
#3433=FACE_OUTER_BOUND ( 'NONE', #8361, .T. ) ;
#3447=ADVANCED_FACE ( 'NONE', ( #40667 ), #14143, .F. ) ;
#3450=DIRECTION ( 'NONE',  ( -1.836970198721029934E-16, 1.836970198721036344E-16, -1.000000000000000000 ) ) ;
#3451=EDGE_LOOP ( 'NONE', ( #69149, #41449, #59312, #58498 ) ) ;
#3459=ORIENTED_EDGE ( 'NONE', *, *, #52326, .F. ) ;
#3467=ORIENTED_EDGE ( 'NONE', *, *, #28860, .T. ) ;
#3471=CARTESIAN_POINT ( 'NONE',  ( 9.417013320880768035, 1.853252480934615809, 455.0000000000000568 ) ) ;
#3474=VERTEX_POINT ( 'NONE', #21220 ) ;
#3475=AXIS2_PLACEMENT_3D ( 'NONE', #51966, #18732, #3529 ) ;
#3476=DIRECTION ( 'NONE',  ( -1.000000000000000000, 0.000000000000000000, 0.000000000000000000 ) ) ;
#3482=ORIENTED_EDGE ( 'NONE', *, *, #23570, .T. ) ;
#3487=CARTESIAN_POINT ( 'NONE',  ( -1.077516549646670541, 11.33351654964656596, 195.0000000000000284 ) ) ;
#3488=ORIENTED_EDGE ( 'NONE', *, *, #47137, .T. ) ;
#3489=AXIS2_PLACEMENT_3D ( 'NONE', #35172, #13618, #24589 ) ;
#3490=EDGE_CURVE ( 'NONE', #7275, #44289, #26170, .T. ) ;
#3494=ORIENTED_EDGE ( 'NONE', *, *, #61274, .T. ) ;
#3502=PLANE ( 'NONE',  #8712 ) ;
#3503=DIRECTION ( 'NONE',  ( -0.7071067811865446862, -0.7071067811865503483, -0.000000000000000000 ) ) ;
#3505=EDGE_LOOP ( 'NONE', ( #52893, #35686, #40265, #27042, #44988, #7102, #57814, #55494, #69032, #68711, #23358, #61982, #3569, #22742, #29398, #40872, #51710 ) ) ;
#3506=LINE ( 'NONE', #39913, #472 ) ;
#3512=CARTESIAN_POINT ( 'NONE',  ( 4.186483450353335023, -12.00648345035347830, 455.0000000000000568 ) ) ;
#3513=CARTESIAN_POINT ( 'NONE',  ( 11.12648345035337982, 4.193516549646526315, 455.0000000000000568 ) ) ;
#3515=CARTESIAN_POINT ( 'NONE',  ( 4.396432944014530442, 8.593516549646635028, 195.0000000000000284 ) ) ;
#3526=EDGE_LOOP ( 'NONE', ( #10495, #65986, #69084, #16453 ) ) ;
#3529=DIRECTION ( 'NONE',  ( -1.000000000000000000, 0.000000000000000000, 0.000000000000000000 ) ) ;
#3535=DIRECTION ( 'NONE',  ( -0.000000000000000000, 0.000000000000000000, -1.000000000000000000 ) ) ;
#3542=ORIENTED_EDGE ( 'NONE', *, *, #24613, .F. ) ;
#3545=VERTEX_POINT ( 'NONE', #36782 ) ;
#3548=CIRCLE ( 'NONE', #48718, 0.2000000000000005107 ) ;
#3550=CARTESIAN_POINT ( 'NONE',  ( -1.077516549646670541, 11.33351654964656596, 455.0000000000000568 ) ) ;
#3552=EDGE_LOOP ( 'NONE', ( #16167, #31327, #33798, #441 ) ) ;
#3555=EDGE_LOOP ( 'NONE', ( #29131, #48787, #32367, #5146 ) ) ;
#3557=DIRECTION ( 'NONE',  ( -0.000000000000000000, 3.673940397442059868E-16, -1.000000000000000000 ) ) ;
#3562=CARTESIAN_POINT ( 'NONE',  ( 7.606483450353420217, 11.31351654964657349, 455.0000000000000568 ) ) ;
#3567=ORIENTED_EDGE ( 'NONE', *, *, #20849, .T. ) ;
#3569=ORIENTED_EDGE ( 'NONE', *, *, #37008, .T. ) ;
#3573=CARTESIAN_POINT ( 'NONE',  ( 10.92648345035336277, 2.893516549646527825, 455.0000000000000568 ) ) ;
#3576=ORIENTED_EDGE ( 'NONE', *, *, #62843, .F. ) ;
#3580=ORIENTED_EDGE ( 'NONE', *, *, #28905, .T. ) ;
#3584=LINE ( 'NONE', #13477, #42106 ) ;
#3588=LINE ( 'NONE', #4983, #38010 ) ;
#3591=VERTEX_POINT ( 'NONE', #48080 ) ;
#3596=DIRECTION ( 'NONE',  ( -1.836970198721029934E-16, 1.836970198721036344E-16, -1.000000000000000000 ) ) ;
#3607=AXIS2_PLACEMENT_3D ( 'NONE', #56709, #29833, #2970 ) ;
#3609=EDGE_CURVE ( 'NONE', #11215, #21581, #16340, .T. ) ;
#3618=ADVANCED_FACE ( 'NONE', ( #4263 ), #63652, .T. ) ;
#3625=EDGE_LOOP ( 'NONE', ( #26612, #20607, #510, #68968 ) ) ;
#3632=CARTESIAN_POINT ( 'NONE',  ( -7.603567055985586798, -8.406483450353363196, 195.0000000000000284 ) ) ;
#3634=ORIENTED_EDGE ( 'NONE', *, *, #44778, .F. ) ;
#3641=CARTESIAN_POINT ( 'NONE',  ( -5.993516549646776603, -6.006483450353426790, 455.0000000000000568 ) ) ;
#3642=FACE_BOUND ( 'NONE', #3505, .T. ) ;
#3654=ORIENTED_EDGE ( 'NONE', *, *, #3793, .T. ) ;
#3656=VERTEX_POINT ( 'NONE', #10943 ) ;
#3660=DIRECTION ( 'NONE',  ( 1.011922027653139155E-14, 1.000000000000000000, 0.000000000000000000 ) ) ;
#3661=EDGE_LOOP ( 'NONE', ( #22537, #17400, #69287, #31174 ) ) ;
#3670=ORIENTED_EDGE ( 'NONE', *, *, #42572, .T. ) ;
#3671=VERTEX_POINT ( 'NONE', #22589 ) ;
#3675=CARTESIAN_POINT ( 'NONE',  ( -7.259684009079930611, 7.798499376343971612, 455.0000000000000568 ) ) ;
#3676=VERTEX_POINT ( 'NONE', #54432 ) ;
#3710=EDGE_CURVE ( 'NONE', #8669, #66944, #38839, .T. ) ;
#3713=CARTESIAN_POINT ( 'NONE',  ( -9.093516549646711411, 10.08346604330776941, 455.0000000000000568 ) ) ;
#3732=VERTEX_POINT ( 'NONE', #54772 ) ;
#3735=AXIS2_PLACEMENT_3D ( 'NONE', #17345, #28646, #34288 ) ;
#3742=ORIENTED_EDGE ( 'NONE', *, *, #25915, .F. ) ;
#3750=ORIENTED_EDGE ( 'NONE', *, *, #9607, .F. ) ;
#3757=VERTEX_POINT ( 'NONE', #35616 ) ;
#3764=DIRECTION ( 'NONE',  ( -0.7671651518153028704, -0.6414496315691537998, -2.587583378555113506E-16 ) ) ;
#3768=DIRECTION ( 'NONE',  ( -1.000000000000000000, -1.671920889371702854E-15, -0.000000000000000000 ) ) ;
#3781=DIRECTION ( 'NONE',  ( -1.203165845134433242E-14, -1.000000000000000000, -1.836970198721014403E-16 ) ) ;
#3782=ORIENTED_EDGE ( 'NONE', *, *, #46884, .F. ) ;
#3784=PLANE ( 'NONE',  #8400 ) ;
#3786=VERTEX_POINT ( 'NONE', #57198 ) ;
#3791=CARTESIAN_POINT ( 'NONE',  ( -3.593516549646701197, 7.415254214038210279, 195.0000000000000284 ) ) ;
#3793=EDGE_CURVE ( 'NONE', #44814, #28277, #8761, .T. ) ;
#3796=ADVANCED_FACE ( 'NONE', ( #67470 ), #45884, .F. ) ;
#3802=FACE_OUTER_BOUND ( 'NONE', #3552, .T. ) ;
#3805=ORIENTED_EDGE ( 'NONE', *, *, #30524, .F. ) ;
#3806=LINE ( 'NONE', #21123, #37921 ) ;
#3811=VERTEX_POINT ( 'NONE', #17960 ) ;
#3813=DIRECTION ( 'NONE',  ( 1.836970198721029934E-16, 1.836970198721010706E-16, -1.000000000000000000 ) ) ;
#3826=LINE ( 'NONE', #14795, #33312 ) ;
#3828=VERTEX_POINT ( 'NONE', #45172 ) ;
#3830=DIRECTION ( 'NONE',  ( -0.000000000000000000, -0.000000000000000000, -1.000000000000000000 ) ) ;
#3832=VECTOR ( 'NONE', #182, 1000.000000000000000 ) ;
#3840=CARTESIAN_POINT ( 'NONE',  ( -7.813516549646791098, -12.00648345035336284, 195.0000000000000284 ) ) ;
#3841=EDGE_LOOP ( 'NONE', ( #46707, #12659, #16235, #39354 ) ) ;
#3846=EDGE_CURVE ( 'NONE', #50458, #44289, #8392, .T. ) ;
#3851=ADVANCED_FACE ( 'NONE', ( #61429 ), #51188, .T. ) ;
#3852=CARTESIAN_POINT ( 'NONE',  ( 1.090483450353370687, 10.73351654964664625, 195.0000000000000284 ) ) ;
#3853=EDGE_LOOP ( 'NONE', ( #26943, #60184, #16348, #45531 ) ) ;
#3857=EDGE_CURVE ( 'NONE', #16139, #43734, #18658, .T. ) ;
#3860=ADVANCED_FACE ( 'NONE', ( #67102 ), #40227, .F. ) ;
#3862=EDGE_CURVE ( 'NONE', #54387, #3671, #9464, .T. ) ;
#3865=CARTESIAN_POINT ( 'NONE',  ( -4.383466043307920224, -8.406483450353396947, 195.0000000000000284 ) ) ;
#3866=ORIENTED_EDGE ( 'NONE', *, *, #120, .F. ) ;
#3867=CARTESIAN_POINT ( 'NONE',  ( -8.198316549646712303, 5.993516549646603409, 195.0000000000000284 ) ) ;
#3869=EDGE_CURVE ( 'NONE', #59906, #3912, #25737, .T. ) ;
#3872=VERTEX_POINT ( 'NONE', #10504 ) ;
#3876=CARTESIAN_POINT ( 'NONE',  ( -9.293516549646710700, 10.91351654964659801, 195.0000000000000284 ) ) ;
#3879=ORIENTED_EDGE ( 'NONE', *, *, #45949, .F. ) ;
#3883=EDGE_LOOP ( 'NONE', ( #51739, #53835, #65818, #22194 ) ) ;
#3887=EDGE_CURVE ( 'NONE', #4257, #52360, #69569, .T. ) ;
#3891=VECTOR ( 'NONE', #57736, 1000.000000000000000 ) ;
#3900=AXIS2_PLACEMENT_3D ( 'NONE', #62723, #13938, #41514 ) ;
#3907=ORIENTED_EDGE ( 'NONE', *, *, #4372, .F. ) ;
#3912=VERTEX_POINT ( 'NONE', #37386 ) ;
#3924=VERTEX_POINT ( 'NONE', #15814 ) ;
#3932=ORIENTED_EDGE ( 'NONE', *, *, #45631, .F. ) ;
#3933=ORIENTED_EDGE ( 'NONE', *, *, #29321, .T. ) ;
#3938=VECTOR ( 'NONE', #25880, 1000.000000000000000 ) ;
#3947=CARTESIAN_POINT ( 'NONE',  ( -9.942044687070620057, -9.247904806590648619, 195.0000000000000284 ) ) ;
#3952=VECTOR ( 'NONE', #65236, 1000.000000000000000 ) ;
#3961=AXIS2_PLACEMENT_3D ( 'NONE', #7837, #2540, #17770 ) ;
#3970=EDGE_CURVE ( 'NONE', #803, #56608, #5161, .T. ) ;
#3973=CARTESIAN_POINT ( 'NONE',  ( 2.765062094116041980, -9.955011587777324422, 455.0000000000000568 ) ) ;
#3974=ORIENTED_EDGE ( 'NONE', *, *, #24102, .F. ) ;
#3984=ORIENTED_EDGE ( 'NONE', *, *, #52579, .T. ) ;
#3986=ORIENTED_EDGE ( 'NONE', *, *, #18257, .T. ) ;
#3989=CIRCLE ( 'NONE', #50302, 0.5999999999999989786 ) ;
#3990=CIRCLE ( 'NONE', #28791, 0.1999999999999996503 ) ;
#3995=CARTESIAN_POINT ( 'NONE',  ( -8.393516549646779623, -6.344579767990844665, 455.0000000000000568 ) ) ;
#4003=ORIENTED_EDGE ( 'NONE', *, *, #3253, .T. ) ;
#4014=EDGE_CURVE ( 'NONE', #21676, #20566, #3806, .T. ) ;
#4018=ADVANCED_FACE ( 'NONE', ( #42682 ), #68515, .F. ) ;
#4028=ORIENTED_EDGE ( 'NONE', *, *, #12725, .F. ) ;
#4033=FACE_OUTER_BOUND ( 'NONE', #19286, .T. ) ;
#4035=VERTEX_POINT ( 'NONE', #43024 ) ;
#4046=PLANE ( 'NONE',  #68239 ) ;
#4056=DIRECTION ( 'NONE',  ( -0.000000000000000000, 3.673940397442059868E-16, -1.000000000000000000 ) ) ;
#4059=CIRCLE ( 'NONE', #45830, 0.6000000000000006439 ) ;
#4070=VERTEX_POINT ( 'NONE', #64952 ) ;
#4071=DIRECTION ( 'NONE',  ( -8.540177112501197482E-15, -1.000000000000000000, -3.673940397442060361E-16 ) ) ;
#4078=LINE ( 'NONE', #14333, #2358 ) ;
#4082=CARTESIAN_POINT ( 'NONE',  ( 1.866219381641484931, 9.404046420174006826, 455.0000000000000568 ) ) ;
#4092=CARTESIAN_POINT ( 'NONE',  ( 9.841277389592722358, -1.690483450353490680, 455.0000000000000568 ) ) ;
#4100=ORIENTED_EDGE ( 'NONE', *, *, #35693, .F. ) ;
#4102=LINE ( 'NONE', #52903, #59873 ) ;
#4106=VERTEX_POINT ( 'NONE', #60319 ) ;
#4111=CARTESIAN_POINT ( 'NONE',  ( -5.380658396643274166, -7.265214908726128407, 195.0000000000000284 ) ) ;
#4115=EDGE_LOOP ( 'NONE', ( #47796, #49763, #45969, #63380 ) ) ;
#4117=AXIS2_PLACEMENT_3D ( 'NONE', #13343, #12975, #2386 ) ;
#4118=DIRECTION ( 'NONE',  ( 0.7071067811865474617, -0.7071067811865474617, 0.000000000000000000 ) ) ;
#4121=ORIENTED_EDGE ( 'NONE', *, *, #67855, .T. ) ;
#4132=CARTESIAN_POINT ( 'NONE',  ( -4.727349090213552429, -4.201500623656063915, 455.0000000000000568 ) ) ;
#4134=VECTOR ( 'NONE', #19539, 1000.000000000000000 ) ;
#4135=CARTESIAN_POINT ( 'NONE',  ( -4.393516549646667713, 11.77351654964658856, 455.0000000000000568 ) ) ;
#4140=FACE_OUTER_BOUND ( 'NONE', #49209, .T. ) ;
#4143=DIRECTION ( 'NONE',  ( 0.000000000000000000, 0.000000000000000000, 1.000000000000000000 ) ) ;
#4157=CIRCLE ( 'NONE', #16569, 0.1999999999999987899 ) ;
#4160=CARTESIAN_POINT ( 'NONE',  ( -4.727349090213463612, 4.188533722949258298, 195.0000000000000284 ) ) ;
#4167=DIRECTION ( 'NONE',  ( -0.000000000000000000, -0.000000000000000000, -1.000000000000000000 ) ) ;
#4170=ORIENTED_EDGE ( 'NONE', *, *, #52157, .T. ) ;
#4174=ORIENTED_EDGE ( 'NONE', *, *, #14016, .F. ) ;
#4180=DIRECTION ( 'NONE',  ( 1.836970198721029934E-16, -1.836970198721036344E-16, 1.000000000000000000 ) ) ;
#4181=AXIS2_PLACEMENT_3D ( 'NONE', #37881, #15965, #10648 ) ;
#4182=ORIENTED_EDGE ( 'NONE', *, *, #33978, .F. ) ;
#4183=DIRECTION ( 'NONE',  ( 1.000000000000000000, -1.115702204244422993E-14, -1.836970198721050395E-16 ) ) ;
#4185=CARTESIAN_POINT ( 'NONE',  ( -5.380658396643321240, -7.265214908726175480, 455.0000000000000568 ) ) ;
#4195=ORIENTED_EDGE ( 'NONE', *, *, #53465, .F. ) ;
#4203=VERTEX_POINT ( 'NONE', #13279 ) ;
#4212=CARTESIAN_POINT ( 'NONE',  ( 11.19368345035336532, -11.19368345035347723, 455.0000000000000568 ) ) ;
#4213=CIRCLE ( 'NONE', #49383, 0.8128000000000145109 ) ;
#4217=EDGE_CURVE ( 'NONE', #25895, #55193, #17886, .T. ) ;
#4219=CARTESIAN_POINT ( 'NONE',  ( 4.406483450353373854, 11.77351654964663119, 195.0000000000000284 ) ) ;
#4222=ORIENTED_EDGE ( 'NONE', *, *, #59508, .F. ) ;
#4223=CYLINDRICAL_SURFACE ( 'NONE', #42205, 0.3999999999999993006 ) ;
#4227=PLANE ( 'NONE',  #24017 ) ;
#4229=DIRECTION ( 'NONE',  ( 1.836970198721029934E-16, 1.836970198721010706E-16, -1.000000000000000000 ) ) ;
#4238=CARTESIAN_POINT ( 'NONE',  ( 10.92648345035337343, -2.706483450353490916, 455.0000000000000568 ) ) ;
#4240=DIRECTION ( 'NONE',  ( 1.836970198721029934E-16, 1.836970198721010706E-16, -1.000000000000000000 ) ) ;
#4251=CARTESIAN_POINT ( 'NONE',  ( 11.12648345035337982, -4.206483450353492692, 455.0000000000000568 ) ) ;
#4257=VERTEX_POINT ( 'NONE', #24242 ) ;
#4263=FACE_OUTER_BOUND ( 'NONE', #51756, .T. ) ;
#4276=CARTESIAN_POINT ( 'NONE',  ( -9.942044687070568543, 9.234937905883914055, 195.0000000000000284 ) ) ;
#4277=LINE ( 'NONE', #47390, #19676 ) ;
#4280=CARTESIAN_POINT ( 'NONE',  ( 9.955011587777271131, 9.234937905883876752, 455.0000000000000568 ) ) ;
#4281=VERTEX_POINT ( 'NONE', #1977 ) ;
#4287=EDGE_CURVE ( 'NONE', #55626, #54387, #20251, .T. ) ;
#4291=VECTOR ( 'NONE', #22053, 1000.000000000000000 ) ;
#4297=ORIENTED_EDGE ( 'NONE', *, *, #55372, .T. ) ;
#4300=ADVANCED_FACE ( 'NONE', ( #5040 ), #26263, .F. ) ;
#4302=ORIENTED_EDGE ( 'NONE', *, *, #33168, .F. ) ;
#4315=EDGE_CURVE ( 'NONE', #49314, #52260, #43612, .T. ) ;
#4317=CARTESIAN_POINT ( 'NONE',  ( 7.616533956692244089, 8.393516549646575342, 455.0000000000000568 ) ) ;
#4319=DIRECTION ( 'NONE',  ( -0.000000000000000000, -0.000000000000000000, -1.000000000000000000 ) ) ;
#4323=VERTEX_POINT ( 'NONE', #47817 ) ;
#4326=DIRECTION ( 'NONE',  ( 0.000000000000000000, -3.673940397442059868E-16, 1.000000000000000000 ) ) ;
#4327=PLANE ( 'NONE',  #22883 ) ;
#4330=CARTESIAN_POINT ( 'NONE',  ( -5.993516549646711766, 5.993516549646603409, 455.0000000000000568 ) ) ;
#4359=EDGE_CURVE ( 'NONE', #29457, #43425, #42520, .T. ) ;
#4369=ADVANCED_FACE ( 'NONE', ( #5409 ), #48525, .T. ) ;
#4371=LINE ( 'NONE', #36891, #53611 ) ;
#4372=EDGE_CURVE ( 'NONE', #14815, #30184, #43211, .T. ) ;
#4375=CARTESIAN_POINT ( 'NONE',  ( -11.77351654964679106, -7.606483450353366038, 455.0000000000000568 ) ) ;
#4376=VERTEX_POINT ( 'NONE', #53155 ) ;
#4377=ORIENTED_EDGE ( 'NONE', *, *, #32603, .F. ) ;
#4384=VERTEX_POINT ( 'NONE', #59483 ) ;
#4388=ORIENTED_EDGE ( 'NONE', *, *, #15461, .F. ) ;
#4393=DIRECTION ( 'NONE',  ( 1.000000000000000000, -3.491481338843132961E-15, 0.000000000000000000 ) ) ;
#4400=CARTESIAN_POINT ( 'NONE',  ( -5.993516549646728642, -6.006483450353378828, 195.0000000000000284 ) ) ;
#4401=ORIENTED_EDGE ( 'NONE', *, *, #47876, .F. ) ;
#4406=CARTESIAN_POINT ( 'NONE',  ( 2.765062094116059743, 9.942044687070495712, 195.0000000000000284 ) ) ;
#4411=VECTOR ( 'NONE', #28649, 1000.000000000000000 ) ;
#4415=EDGE_CURVE ( 'NONE', #27000, #50982, #18062, .T. ) ;
#4418=DIRECTION ( 'NONE',  ( 1.000000000000000000, -1.047444401652940007E-14, 1.836970198721010706E-16 ) ) ;
#4424=DIRECTION ( 'NONE',  ( -0.000000000000000000, -0.000000000000000000, -1.000000000000000000 ) ) ;
#4432=EDGE_CURVE ( 'NONE', #11140, #3786, #12065, .T. ) ;
#4433=CARTESIAN_POINT ( 'NONE',  ( -11.11351654964668612, 8.693516549646636449, 455.0000000000000568 ) ) ;
#4435=VERTEX_POINT ( 'NONE', #798 ) ;
#4442=LINE ( 'NONE', #32346, #51427 ) ;
#4452=VERTEX_POINT ( 'NONE', #28327 ) ;
#4453=DIRECTION ( 'NONE',  ( 1.952517519553884087E-14, 1.000000000000000000, 1.836970198721046697E-16 ) ) ;
#4460=DIRECTION ( 'NONE',  ( -1.053224967557347660E-14, -1.000000000000000000, 0.000000000000000000 ) ) ;
#4461=FACE_OUTER_BOUND ( 'NONE', #3142, .T. ) ;
#4470=VERTEX_POINT ( 'NONE', #6086 ) ;
#4471=AXIS2_PLACEMENT_3D ( 'NONE', #16296, #38229, #37527 ) ;
#4473=DIRECTION ( 'NONE',  ( 0.000000000000000000, 0.000000000000000000, 1.000000000000000000 ) ) ;
#4477=CARTESIAN_POINT ( 'NONE',  ( 3.606483450353397568, 4.609516549646590633, 455.0000000000000568 ) ) ;
#4481=FACE_OUTER_BOUND ( 'NONE', #44101, .T. ) ;
#4490=DIRECTION ( 'NONE',  ( 1.000000000000000000, 0.000000000000000000, 0.000000000000000000 ) ) ;
#4492=ORIENTED_EDGE ( 'NONE', *, *, #1672, .T. ) ;
#4493=DIRECTION ( 'NONE',  ( 0.000000000000000000, 0.000000000000000000, 1.000000000000000000 ) ) ;
#4498=EDGE_LOOP ( 'NONE', ( #61576, #27278, #69900, #68635 ) ) ;
#4499=DIRECTION ( 'NONE',  ( 8.903847840905249551E-15, 1.000000000000000000, 0.000000000000000000 ) ) ;
#4502=VECTOR ( 'NONE', #41875, 1000.000000000000000 ) ;
#4503=DIRECTION ( 'NONE',  ( -0.7071067811865474617, 0.7071067811865474617, 0.000000000000000000 ) ) ;
#4506=DIRECTION ( 'NONE',  ( -0.000000000000000000, -0.000000000000000000, -1.000000000000000000 ) ) ;
#4510=EDGE_LOOP ( 'NONE', ( #10401, #32620, #25605, #28328 ) ) ;
#4518=ORIENTED_EDGE ( 'NONE', *, *, #13575, .F. ) ;
#4525=DIRECTION ( 'NONE',  ( -0.000000000000000000, 3.673940397442059868E-16, -1.000000000000000000 ) ) ;
#4542=AXIS2_PLACEMENT_3D ( 'NONE', #57181, #7679, #35593 ) ;
#4543=CARTESIAN_POINT ( 'NONE',  ( -4.609516549646752281, -3.606483450353441533, 455.0000000000000568 ) ) ;
#4544=VERTEX_POINT ( 'NONE', #7455 ) ;
#4546=EDGE_CURVE ( 'NONE', #20667, #40341, #33300, .T. ) ;
#4553=VECTOR ( 'NONE', #6655, 1000.000000000000000 ) ;
#4562=LINE ( 'NONE', #26128, #63618 ) ;
#4563=ORIENTED_EDGE ( 'NONE', *, *, #35453, .T. ) ;
#4572=ORIENTED_EDGE ( 'NONE', *, *, #38966, .F. ) ;
#4573=LINE ( 'NONE', #25793, #56101 ) ;
#4575=CARTESIAN_POINT ( 'NONE',  ( 9.306483450353418618, 10.91351654964656426, 455.0000000000000568 ) ) ;
#4578=FACE_OUTER_BOUND ( 'NONE', #56776, .T. ) ;
#4598=DIRECTION ( 'NONE',  ( -0.000000000000000000, -0.000000000000000000, -1.000000000000000000 ) ) ;
#4601=ORIENTED_EDGE ( 'NONE', *, *, #69559, .T. ) ;
#4604=EDGE_CURVE ( 'NONE', #13479, #14411, #39965, .T. ) ;
#4606=DIRECTION ( 'NONE',  ( 7.808916176531286882E-15, 1.000000000000000000, -0.000000000000000000 ) ) ;
#4608=ORIENTED_EDGE ( 'NONE', *, *, #52674, .F. ) ;
#4614=ORIENTED_EDGE ( 'NONE', *, *, #42496, .F. ) ;
#4618=EDGE_LOOP ( 'NONE', ( #31498, #14160, #45071, #3467 ) ) ;
#4627=CARTESIAN_POINT ( 'NONE',  ( 6.006483450353379716, -6.006483450353394815, 195.0000000000000284 ) ) ;
#4639=VECTOR ( 'NONE', #35749, 1000.000000000000000 ) ;
#4646=CARTESIAN_POINT ( 'NONE',  ( 3.430747519065335815, 7.839518282750141509, 455.0000000000000568 ) ) ;
#4651=AXIS2_PLACEMENT_3D ( 'NONE', #38676, #27379, #506 ) ;
#4652=CIRCLE ( 'NONE', #24973, 0.5999999999999998668 ) ;
#4654=EDGE_CURVE ( 'NONE', #53071, #58452, #58195, .T. ) ;
#4658=SURFACE_STYLE_USAGE ( .BOTH. , #53108 ) ;
#4660=CARTESIAN_POINT ( 'NONE',  ( -5.993516549646776603, -6.006483450353426790, 455.0000000000000568 ) ) ;
#4662=EDGE_CURVE ( 'NONE', #26479, #17661, #18399, .T. ) ;
#4674=EDGE_CURVE ( 'NONE', #4323, #44422, #46876, .T. ) ;
#4683=EDGE_CURVE ( 'NONE', #33316, #35467, #50938, .T. ) ;
#4691=LINE ( 'NONE', #64783, #21349 ) ;
#4715=ORIENTED_EDGE ( 'NONE', *, *, #41936, .T. ) ;
#4720=ORIENTED_EDGE ( 'NONE', *, *, #44326, .F. ) ;
#4730=CARTESIAN_POINT ( 'NONE',  ( 7.757955312929523117, -8.465062094116182934, 455.0000000000000568 ) ) ;
#4734=CARTESIAN_POINT ( 'NONE',  ( -4.727349090213463612, 4.188533722949258298, 455.0000000000000568 ) ) ;
#4735=CARTESIAN_POINT ( 'NONE',  ( -1.853252480934758584, 9.404046420173985510, 455.0000000000000568 ) ) ;
#4738=DIRECTION ( 'NONE',  ( -0.000000000000000000, 0.000000000000000000, -1.000000000000000000 ) ) ;
#4740=CARTESIAN_POINT ( 'NONE',  ( 7.757955312929523117, -8.465062094116087010, 195.0000000000000284 ) ) ;
#4741=AXIS2_PLACEMENT_3D ( 'NONE', #4986, #26553, #15945 ) ;
#4744=DIRECTION ( 'NONE',  ( -0.7071067811865451302, 0.7071067811865500152, 2.597868168706484541E-16 ) ) ;
#4745=ADVANCED_FACE ( 'NONE', ( #14873 ), #32179, .F. ) ;
#4746=FACE_OUTER_BOUND ( 'NONE', #9273, .T. ) ;
#4750=EDGE_CURVE ( 'NONE', #3676, #21914, #21568, .T. ) ;
#4751=ADVANCED_FACE ( 'NONE', ( #59396 ), #10267, .F. ) ;
#4752=AXIS2_PLACEMENT_3D ( 'NONE', #8304, #33186, #18568 ) ;
#4753=ORIENTED_EDGE ( 'NONE', *, *, #33031, .T. ) ;
#4761=CARTESIAN_POINT ( 'NONE',  ( 7.811466277050736373, -4.740315990920255018, 455.0000000000000568 ) ) ;
#4762=AXIS2_PLACEMENT_3D ( 'NONE', #61497, #44544, #60812 ) ;
#4764=CARTESIAN_POINT ( 'NONE',  ( -11.07551654964667520, 9.791916549646639822, 455.0000000000000568 ) ) ;
#4768=CARTESIAN_POINT ( 'NONE',  ( 10.92648345035331303, 2.693516549646575609, 195.0000000000000284 ) ) ;
#4770=CARTESIAN_POINT ( 'NONE',  ( 10.09643294401448443, 2.693516549646584934, 195.0000000000000284 ) ) ;
#4776=CARTESIAN_POINT ( 'NONE',  ( 11.78648345035337819, -7.826483450353491023, 455.0000000000000568 ) ) ;
#4779=ORIENTED_EDGE ( 'NONE', *, *, #2638, .F. ) ;
#4785=ORIENTED_EDGE ( 'NONE', *, *, #63798, .F. ) ;
#4790=ORIENTED_EDGE ( 'NONE', *, *, #31297, .F. ) ;
#4799=DIRECTION ( 'NONE',  ( -1.836970198721029934E-16, -1.836970198721010706E-16, 1.000000000000000000 ) ) ;
#4825=CARTESIAN_POINT ( 'NONE',  ( 2.906483450353417375, 10.08346604330775875, 455.0000000000000568 ) ) ;
#4829=ORIENTED_EDGE ( 'NONE', *, *, #62195, .T. ) ;
#4830=LINE ( 'NONE', #58920, #59553 ) ;
#4834=FACE_OUTER_BOUND ( 'NONE', #14785, .T. ) ;
#4846=CARTESIAN_POINT ( 'NONE',  ( -4.383466043307858939, 8.593516549646588842, 195.0000000000000284 ) ) ;
#4847=EDGE_CURVE ( 'NONE', #52241, #42601, #43472, .T. ) ;
#4849=EDGE_CURVE ( 'NONE', #47832, #66711, #24222, .T. ) ;
#4865=LINE ( 'NONE', #69572, #17057 ) ;
#4867=CARTESIAN_POINT ( 'NONE',  ( 4.201500623656053257, 4.727349090213338378, 455.0000000000000568 ) ) ;
#4870=CARTESIAN_POINT ( 'NONE',  ( 11.32648345035340398, 7.593516549646563085, 455.0000000000000568 ) ) ;
#4871=ORIENTED_EDGE ( 'NONE', *, *, #29362, .F. ) ;
#4875=DIRECTION ( 'NONE',  ( 1.836970198721029934E-16, 1.836970198721010706E-16, -1.000000000000000000 ) ) ;
#4892=EDGE_CURVE ( 'NONE', #8722, #62416, #54787, .T. ) ;
#4897=EDGE_CURVE ( 'NONE', #60569, #67306, #1050, .T. ) ;
#4905=VERTEX_POINT ( 'NONE', #44161 ) ;
#4906=EDGE_LOOP ( 'NONE', ( #12626, #1695, #33315, #22611 ) ) ;
#4907=LINE ( 'NONE', #59340, #52408 ) ;
#4908=AXIS2_PLACEMENT_3D ( 'NONE', #3713, #12899, #30583 ) ;
#4915=CARTESIAN_POINT ( 'NONE',  ( 2.706483450353343478, -10.92648345035336632, 195.0000000000000284 ) ) ;
#4918=CARTESIAN_POINT ( 'NONE',  ( -7.798499376344109280, -4.740315990920159095, 455.0000000000000568 ) ) ;
#4929=AXIS2_PLACEMENT_3D ( 'NONE', #44564, #12044, #35973 ) ;
#4930=ORIENTED_EDGE ( 'NONE', *, *, #64219, .F. ) ;
#4933=CARTESIAN_POINT ( 'NONE',  ( 10.20488345035345290, 9.791916549646566992, 455.0000000000000568 ) ) ;
#4937=ORIENTED_EDGE ( 'NONE', *, *, #54203, .F. ) ;
#4938=ORIENTED_EDGE ( 'NONE', *, *, #16792, .T. ) ;
#4939=DIRECTION ( 'NONE',  ( -1.000000000000000000, 0.000000000000000000, 0.000000000000000000 ) ) ;
#4940=VERTEX_POINT ( 'NONE', #27917 ) ;
#4941=ORIENTED_EDGE ( 'NONE', *, *, #15528, .F. ) ;
#4947=CARTESIAN_POINT ( 'NONE',  ( 7.826483450353374671, 11.99351654964662295, 195.0000000000000284 ) ) ;
#4948=EDGE_LOOP ( 'NONE', ( #20658, #4302, #61906, #5545 ) ) ;
#4952=VERTEX_POINT ( 'NONE', #38528 ) ;
#4957=DIRECTION ( 'NONE',  ( -2.135044278125301343E-15, 1.000000000000000000, 0.000000000000000000 ) ) ;
#4964=ORIENTED_EDGE ( 'NONE', *, *, #28113, .T. ) ;
#4965=CARTESIAN_POINT ( 'NONE',  ( 6.006483450353379716, -6.006483450353490738, 455.0000000000000568 ) ) ;
#4979=DIRECTION ( 'NONE',  ( -1.000000000000000000, 0.000000000000000000, 0.000000000000000000 ) ) ;
#4983=CARTESIAN_POINT ( 'NONE',  ( -1.853252480934758584, 9.404046420173985510, 455.0000000000000568 ) ) ;
#4986=CARTESIAN_POINT ( 'NONE',  ( -8.593516549646711411, 4.383466043307770121, 455.0000000000000568 ) ) ;
#5005=CARTESIAN_POINT ( 'NONE',  ( -9.404046420174124066, 1.853252480934674651, 455.0000000000000568 ) ) ;
#5009=ORIENTED_EDGE ( 'NONE', *, *, #1795, .T. ) ;
#5036=AXIS2_PLACEMENT_3D ( 'NONE', #7439, #45264, #30060 ) ;
#5040=FACE_OUTER_BOUND ( 'NONE', #27941, .T. ) ;
#5043=VECTOR ( 'NONE', #39850, 1000.000000000000000 ) ;
#5044=VERTEX_POINT ( 'NONE', #40242 ) ;
#5046=ADVANCED_FACE ( 'NONE', ( #40596 ), #14443, .F. ) ;
#5052=ORIENTED_EDGE ( 'NONE', *, *, #25202, .F. ) ;
#5053=EDGE_LOOP ( 'NONE', ( #13814, #45545, #67410, #2512, #68724, #53831, #49420, #7440, #20352, #17005, #38027, #49410, #52425, #36063, #25547, #25850, #67607 ) ) ;
#5055=DIRECTION ( 'NONE',  ( -0.4999999999999695244, 0.8660254037844563602, 0.000000000000000000 ) ) ;
#5056=ORIENTED_EDGE ( 'NONE', *, *, #68198, .F. ) ;
#5058=AXIS2_PLACEMENT_3D ( 'NONE', #62334, #46083, #51384 ) ;
#5066=ORIENTED_EDGE ( 'NONE', *, *, #3857, .T. ) ;
#5068=EDGE_CURVE ( 'NONE', #47329, #12465, #66765, .T. ) ;
#5070=EDGE_CURVE ( 'NONE', #325, #8276, #19375, .T. ) ;
#5071=LINE ( 'NONE', #41503, #56213 ) ;
#5077=CARTESIAN_POINT ( 'NONE',  ( -4.383466043307859827, 8.393516549646589553, 195.0000000000000284 ) ) ;
#5078=DIRECTION ( 'NONE',  ( 1.836970198721029934E-16, -1.836970198721036344E-16, 1.000000000000000000 ) ) ;
#5080=DIRECTION ( 'NONE',  ( -0.7071067811865421326, 0.7071067811865530128, 0.000000000000000000 ) ) ;
#5085=ORIENTED_EDGE ( 'NONE', *, *, #14015, .T. ) ;
#5094=CARTESIAN_POINT ( 'NONE',  ( -9.234937905884127218, -9.955011587777249815, 455.0000000000000568 ) ) ;
#5099=AXIS2_PLACEMENT_3D ( 'NONE', #8155, #45998, #62968 ) ;
#5100=EDGE_LOOP ( 'NONE', ( #21115, #17151, #35362, #1655 ) ) ;
#5101=DIRECTION ( 'NONE',  ( -1.836970198721029934E-16, -1.836970198721010706E-16, 1.000000000000000000 ) ) ;
#5104=CYLINDRICAL_SURFACE ( 'NONE', #62456, 1.399999999999998579 ) ;
#5106=LINE ( 'NONE', #47198, #43752 ) ;
#5111=FACE_OUTER_BOUND ( 'NONE', #37457, .T. ) ;
#5117=ORIENTED_EDGE ( 'NONE', *, *, #15164, .T. ) ;
#5119=VERTEX_POINT ( 'NONE', #18674 ) ;
#5121=VECTOR ( 'NONE', #6813, 1000.000000000000114 ) ;
#5135=EDGE_CURVE ( 'NONE', #44422, #26906, #25389, .T. ) ;
#5140=EDGE_CURVE ( 'NONE', #11259, #37252, #57911, .T. ) ;
#5141=VECTOR ( 'NONE', #7340, 1000.000000000000000 ) ;
#5142=ORIENTED_EDGE ( 'NONE', *, *, #65693, .T. ) ;
#5144=EDGE_CURVE ( 'NONE', #57095, #54700, #10521, .T. ) ;
#5146=ORIENTED_EDGE ( 'NONE', *, *, #1222, .T. ) ;
#5161=CIRCLE ( 'NONE', #44644, 1.399999999999999245 ) ;
#5162=AXIS2_PLACEMENT_3D ( 'NONE', #20945, #58080, #53488 ) ;
#5167=VERTEX_POINT ( 'NONE', #63929 ) ;
#5169=EDGE_CURVE ( 'NONE', #6350, #7925, #64278, .T. ) ;
#5170=VECTOR ( 'NONE', #59016, 1000.000000000000000 ) ;
#5173=VECTOR ( 'NONE', #34005, 1000.000000000000000 ) ;
#5176=DIRECTION ( 'NONE',  ( 0.000000000000000000, -3.673940397442059868E-16, 1.000000000000000000 ) ) ;
#5195=CARTESIAN_POINT ( 'NONE',  ( 6.006483450353409914, 8.198316549646580853, 455.0000000000000568 ) ) ;
#5217=ORIENTED_EDGE ( 'NONE', *, *, #28109, .T. ) ;
#5233=DIRECTION ( 'NONE',  ( -1.000000000000000000, 3.016910393003147986E-15, 1.108394896831706469E-30 ) ) ;
#5239=DIRECTION ( 'NONE',  ( 0.6414496315691617934, 0.7671651518152962090, -0.000000000000000000 ) ) ;
#5240=CYLINDRICAL_SURFACE ( 'NONE', #20569, 0.5999999999999989786 ) ;
#5242=LINE ( 'NONE', #26812, #16468 ) ;
#5249=VERTEX_POINT ( 'NONE', #47653 ) ;
#5251=DIRECTION ( 'NONE',  ( -1.000000000000000000, 0.000000000000000000, 0.000000000000000000 ) ) ;
#5253=CYLINDRICAL_SURFACE ( 'NONE', #30565, 0.3999999999999993006 ) ;
#5258=AXIS2_PLACEMENT_3D ( 'NONE', #17341, #38915, #60478 ) ;
#5261=CARTESIAN_POINT ( 'NONE',  ( -4.609516549646713202, 3.593516549646603941, 455.0000000000000568 ) ) ;
#5266=AXIS2_PLACEMENT_3D ( 'NONE', #31409, #52977, #47304 ) ;
#5270=AXIS2_PLACEMENT_3D ( 'NONE', #65420, #12679, #28610 ) ;
#5284=ORIENTED_EDGE ( 'NONE', *, *, #22187, .F. ) ;
#5288=CARTESIAN_POINT ( 'NONE',  ( 4.206483450353373676, 11.11351654964663282, 195.0000000000000284 ) ) ;
#5289=LINE ( 'NONE', #48760, #36741 ) ;
#5290=DIRECTION ( 'NONE',  ( 0.7071067811865361374, -0.7071067811865588970, 0.000000000000000000 ) ) ;
#5294=ORIENTED_EDGE ( 'NONE', *, *, #29619, .F. ) ;
#5296=DIRECTION ( 'NONE',  ( 4.336808689942006692E-15, 1.000000000000000000, 0.000000000000000000 ) ) ;
#5297=VERTEX_POINT ( 'NONE', #11889 ) ;
#5299=EDGE_LOOP ( 'NONE', ( #22492, #54011, #281, #11533 ) ) ;
#5311=VERTEX_POINT ( 'NONE', #65983 ) ;
#5312=EDGE_CURVE ( 'NONE', #15307, #64032, #6608, .T. ) ;
#5313=LINE ( 'NONE', #65389, #55566 ) ;
#5316=AXIS2_PLACEMENT_3D ( 'NONE', #19677, #52584, #62830 ) ;
#5318=CARTESIAN_POINT ( 'NONE',  ( -2.693516549646682190, 10.08346604330774454, 455.0000000000000568 ) ) ;
#5330=ORIENTED_EDGE ( 'NONE', *, *, #32681, .F. ) ;
#5331=LINE ( 'NONE', #11294, #28586 ) ;
#5339=PLANE ( 'NONE',  #3026 ) ;
#5342=ORIENTED_EDGE ( 'NONE', *, *, #48606, .F. ) ;
#5344=CARTESIAN_POINT ( 'NONE',  ( -4.734785091273987057, -6.619341603356850179, 195.0000000000000284 ) ) ;
#5352=EDGE_CURVE ( 'NONE', #19307, #26597, #32781, .T. ) ;
#5356=EDGE_CURVE ( 'NONE', #191, #1311, #64970, .T. ) ;
#5358=CARTESIAN_POINT ( 'NONE',  ( 10.20488345035338007, -11.48848345035349361, 455.0000000000000568 ) ) ;
#5362=CARTESIAN_POINT ( 'NONE',  ( -11.47551654964677326, -10.20488345035332145, 195.0000000000000284 ) ) ;
#5364=CARTESIAN_POINT ( 'NONE',  ( -7.415254214038356828, -3.606483450353401121, 455.0000000000000568 ) ) ;
#5372=ORIENTED_EDGE ( 'NONE', *, *, #4217, .F. ) ;
#5376=VECTOR ( 'NONE', #27776, 1000.000000000000227 ) ;
#5389=VERTEX_POINT ( 'NONE', #65323 ) ;
#5405=LINE ( 'NONE', #42160, #65858 ) ;
#5406=VECTOR ( 'NONE', #4056, 1000.000000000000000 ) ;
#5409=FACE_OUTER_BOUND ( 'NONE', #49902, .T. ) ;
#5410=ORIENTED_EDGE ( 'NONE', *, *, #47764, .F. ) ;
#5411=DIRECTION ( 'NONE',  ( -1.000000000000000000, 0.000000000000000000, 0.000000000000000000 ) ) ;
#5412=ORIENTED_EDGE ( 'NONE', *, *, #35527, .F. ) ;
#5423=VERTEX_POINT ( 'NONE', #32451 ) ;
#5428=AXIS2_PLACEMENT_3D ( 'NONE', #6602, #48695, #22523 ) ;
#5433=CARTESIAN_POINT ( 'NONE',  ( 6.006483450353401921, 5.993516549646582092, 455.0000000000000568 ) ) ;
#5434=CARTESIAN_POINT ( 'NONE',  ( 6.006483450353353959, 5.993516549646629166, 195.0000000000000284 ) ) ;
#5436=AXIS2_PLACEMENT_3D ( 'NONE', #42293, #31706, #53277 ) ;
#5444=CARTESIAN_POINT ( 'NONE',  ( -4.193516549646673752, 11.31351654964658771, 455.0000000000000568 ) ) ;
#5445=CYLINDRICAL_SURFACE ( 'NONE', #11979, 0.2000000000000005107 ) ;
#5446=DIRECTION ( 'NONE',  ( -8.612436249475772606E-15, -1.000000000000000000, -1.836970198721020566E-16 ) ) ;
#5455=DIRECTION ( 'NONE',  ( 0.7071067811865475727, -0.7071067811865475727, 0.000000000000000000 ) ) ;
#5458=VERTEX_POINT ( 'NONE', #39462 ) ;
#5463=ORIENTED_EDGE ( 'NONE', *, *, #10741, .F. ) ;
#5468=CARTESIAN_POINT ( 'NONE',  ( 4.406483450353335662, -11.78648345035337996, 195.0000000000000284 ) ) ;
#5474=VERTEX_POINT ( 'NONE', #40511 ) ;
#5476=VERTEX_POINT ( 'NONE', #68087 ) ;
#5478=AXIS2_PLACEMENT_3D ( 'NONE', #51074, #61678, #66299 ) ;
#5479=LINE ( 'NONE', #49306, #49691 ) ;
#5486=EDGE_CURVE ( 'NONE', #12677, #13563, #13292, .T. ) ;
#5489=EDGE_CURVE ( 'NONE', #10374, #33734, #44060, .T. ) ;
#5492=EDGE_CURVE ( 'NONE', #33426, #9547, #12398, .T. ) ;
#5494=EDGE_CURVE ( 'NONE', #26597, #41272, #23552, .T. ) ;
#5499=ORIENTED_EDGE ( 'NONE', *, *, #10003, .T. ) ;
#5505=CARTESIAN_POINT ( 'NONE',  ( 9.841277389592722358, -2.290483450353395067, 195.0000000000000284 ) ) ;
#5506=ORIENTED_EDGE ( 'NONE', *, *, #3430, .T. ) ;
#5508=CARTESIAN_POINT ( 'NONE',  ( -7.813516549646711162, 11.77351654964660277, 455.0000000000000568 ) ) ;
#5539=EDGE_CURVE ( 'NONE', #38308, #43722, #4102, .T. ) ;
#5545=ORIENTED_EDGE ( 'NONE', *, *, #63518, .T. ) ;
#5546=VECTOR ( 'NONE', #38937, 1000.000000000000000 ) ;
#5552=FACE_OUTER_BOUND ( 'NONE', #16121, .T. ) ;
#5555=VERTEX_POINT ( 'NONE', #36983 ) ;
#5570=CARTESIAN_POINT ( 'NONE',  ( 8.406483450353404052, 6.331612867284015955, 455.0000000000000568 ) ) ;
#5572=DIRECTION ( 'NONE',  ( 1.836970198721029934E-16, 1.836970198721010706E-16, -1.000000000000000000 ) ) ;
#5585=ORIENTED_EDGE ( 'NONE', *, *, #8302, .T. ) ;
#5586=DIRECTION ( 'NONE',  ( -2.135044278125299371E-15, -1.000000000000000000, -3.673940397442060361E-16 ) ) ;
#5589=LINE ( 'NONE', #48722, #30388 ) ;
#5597=PLANE ( 'NONE',  #8270 ) ;
#5603=FACE_OUTER_BOUND ( 'NONE', #45191, .T. ) ;
#5604=EDGE_CURVE ( 'NONE', #44650, #10374, #52534, .T. ) ;
#5606=CARTESIAN_POINT ( 'NONE',  ( 7.428221114745003462, -3.006483450353490294, 455.0000000000000568 ) ) ;
#5610=VERTEX_POINT ( 'NONE', #10440 ) ;
#5611=PLANE ( 'NONE',  #33538 ) ;
#5612=CARTESIAN_POINT ( 'NONE',  ( -7.593516549646711411, 11.31351654964660014, 195.0000000000000284 ) ) ;
#5615=DIRECTION ( 'NONE',  ( 1.000000000000000000, 0.000000000000000000, 0.000000000000000000 ) ) ;
#5620=EDGE_CURVE ( 'NONE', #5167, #31147, #47919, .T. ) ;
#5630=CARTESIAN_POINT ( 'NONE',  ( -10.91351654964670814, 9.093516549646603053, 455.0000000000000568 ) ) ;
#5631=PLANE ( 'NONE',  #42231 ) ;
#5637=FACE_OUTER_BOUND ( 'NONE', #61995, .T. ) ;
#5638=VECTOR ( 'NONE', #32023, 1000.000000000000000 ) ;
#5648=LINE ( 'NONE', #37822, #23955 ) ;
#5650=AXIS2_PLACEMENT_3D ( 'NONE', #48951, #48600, #172 ) ;
#5651=EDGE_LOOP ( 'NONE', ( #59588, #14682, #30911, #68451 ) ) ;
#5654=EDGE_CURVE ( 'NONE', #67578, #10486, #31336, .T. ) ;
#5661=CARTESIAN_POINT ( 'NONE',  ( -11.47551654964667733, 10.19191654964664018, 455.0000000000000568 ) ) ;
#5664=VERTEX_POINT ( 'NONE', #42960 ) ;
#5672=CARTESIAN_POINT ( 'NONE',  ( 4.740315990920131561, -7.811466277050742590, 195.0000000000000284 ) ) ;
#5674=ORIENTED_EDGE ( 'NONE', *, *, #15461, .T. ) ;
#5690=ORIENTED_EDGE ( 'NONE', *, *, #2890, .F. ) ;
#5693=EDGE_CURVE ( 'NONE', #21000, #28585, #47455, .T. ) ;
#5701=ADVANCED_FACE ( 'NONE', ( #11469 ), #33733, .F. ) ;
#5707=FACE_OUTER_BOUND ( 'NONE', #33094, .T. ) ;
#5723=ORIENTED_EDGE ( 'NONE', *, *, #40940, .T. ) ;
#5732=DIRECTION ( 'NONE',  ( 1.130039751537441866E-14, 1.000000000000000000, 1.836970198721015636E-16 ) ) ;
#5736=EDGE_LOOP ( 'NONE', ( #18532, #64339, #15202, #56601 ) ) ;
#5737=VERTEX_POINT ( 'NONE', #60612 ) ;
#5738=ADVANCED_FACE ( 'NONE', ( #48621 ), #49652, .F. ) ;
#5742=DIRECTION ( 'NONE',  ( 0.000000000000000000, 0.000000000000000000, 1.000000000000000000 ) ) ;
#5745=CARTESIAN_POINT ( 'NONE',  ( -10.91351654964670637, 9.293516549646604119, 455.0000000000000568 ) ) ;
#5755=CARTESIAN_POINT ( 'NONE',  ( -4.188533722949335569, 7.259684009079808931, 455.0000000000000568 ) ) ;
#5761=DIRECTION ( 'NONE',  ( -2.135044278125299371E-15, -1.000000000000000000, 0.000000000000000000 ) ) ;
#5777=CIRCLE ( 'NONE', #14804, 0.2000000000000005107 ) ;
#5779=DIRECTION ( 'NONE',  ( 3.717264591378874374E-15, 1.000000000000000000, 0.000000000000000000 ) ) ;
#5784=DIRECTION ( 'NONE',  ( -0.7071067811865435759, 0.7071067811865515695, 0.000000000000000000 ) ) ;
#5786=ADVANCED_FACE ( 'NONE', ( #10778 ), #32362, .F. ) ;
#5790=LINE ( 'NONE', #27355, #27611 ) ;
#5791=CARTESIAN_POINT ( 'NONE',  ( -9.093516549646780689, -10.92648345035334145, 195.0000000000000284 ) ) ;
#5817=VERTEX_POINT ( 'NONE', #34408 ) ;
#5819=CARTESIAN_POINT ( 'NONE',  ( -7.415254214038309755, -3.606483450353353160, 195.0000000000000284 ) ) ;
#5826=CARTESIAN_POINT ( 'NONE',  ( 9.804883450353456098, 11.07551654964653132, 455.0000000000000568 ) ) ;
#5834=AXIS2_PLACEMENT_3D ( 'NONE', #50776, #23914, #45470 ) ;
#5839=ORIENTED_EDGE ( 'NONE', *, *, #34039, .T. ) ;
#5854=CARTESIAN_POINT ( 'NONE',  ( 6.006483450353379716, -3.606483450353490827, 455.0000000000000568 ) ) ;
#5861=DIRECTION ( 'NONE',  ( 1.000000000000000000, 0.000000000000000000, 0.000000000000000000 ) ) ;
#5874=PLANE ( 'NONE',  #51980 ) ;
#5881=CARTESIAN_POINT ( 'NONE',  ( -2.993516549646742853, -7.428221114745035436, 195.0000000000000284 ) ) ;
#5882=DIRECTION ( 'NONE',  ( 1.836970198721029934E-16, -1.836970198721036344E-16, 1.000000000000000000 ) ) ;
#5897=VECTOR ( 'NONE', #25666, 1000.000000000000000 ) ;
#5905=DIRECTION ( 'NONE',  ( -1.836970198721029934E-16, 1.836970198721036344E-16, -1.000000000000000000 ) ) ;
#5913=ORIENTED_EDGE ( 'NONE', *, *, #24591, .F. ) ;
#5915=VECTOR ( 'NONE', #6304, 1000.000000000000000 ) ;
#5924=ORIENTED_EDGE ( 'NONE', *, *, #28054, .T. ) ;
#5933=DIRECTION ( 'NONE',  ( -1.000000000000000000, 0.000000000000000000, 0.000000000000000000 ) ) ;
#5943=CYLINDRICAL_SURFACE ( 'NONE', #35227, 0.1999999999999987899 ) ;
#5956=CARTESIAN_POINT ( 'NONE',  ( -3.593516549646790903, -7.428221114745077180, 455.0000000000000568 ) ) ;
#5967=CARTESIAN_POINT ( 'NONE',  ( 8.606483450353382025, 4.383466043307719495, 455.0000000000000568 ) ) ;
#5975=ORIENTED_EDGE ( 'NONE', *, *, #24545, .T. ) ;
#5976=DIRECTION ( 'NONE',  ( -0.6414496315691565753, 0.7671651518153006499, 0.000000000000000000 ) ) ;
#5977=DIRECTION ( 'NONE',  ( -1.836970198721029934E-16, 1.836970198721036344E-16, -1.000000000000000000 ) ) ;
#5991=ORIENTED_EDGE ( 'NONE', *, *, #14167, .F. ) ;
#6008=CARTESIAN_POINT ( 'NONE',  ( 12.00648345035333620, 4.173516549646563156, 195.0000000000000284 ) ) ;
#6009=VECTOR ( 'NONE', #55896, 1000.000000000000000 ) ;
#6011=EDGE_CURVE ( 'NONE', #67875, #37049, #57746, .T. ) ;
#6021=ORIENTED_EDGE ( 'NONE', *, *, #26181, .F. ) ;
#6026=ORIENTED_EDGE ( 'NONE', *, *, #2560, .T. ) ;
#6029=EDGE_CURVE ( 'NONE', #7366, #25592, #48633, .T. ) ;
#6036=CARTESIAN_POINT ( 'NONE',  ( -10.73351654964671198, 1.077516549646603483, 455.0000000000000568 ) ) ;
#6041=LINE ( 'NONE', #65094, #27023 ) ;
#6048=ORIENTED_EDGE ( 'NONE', *, *, #46875, .F. ) ;
#6057=ADVANCED_FACE ( 'NONE', ( #35827 ), #57395, .F. ) ;
#6062=CARTESIAN_POINT ( 'NONE',  ( -4.193516549646782998, -11.12648345035339581, 195.0000000000000284 ) ) ;
#6063=VECTOR ( 'NONE', #43521, 1000.000000000000000 ) ;
#6069=LINE ( 'NONE', #11025, #24571 ) ;
#6075=ORIENTED_EDGE ( 'NONE', *, *, #51501, .F. ) ;
#6077=CARTESIAN_POINT ( 'NONE',  ( -8.593516549646711411, 7.603567055985436696, 455.0000000000000568 ) ) ;
#6080=ADVANCED_FACE ( 'NONE', ( #36173 ), #45205, .F. ) ;
#6086=CARTESIAN_POINT ( 'NONE',  ( 10.20488345035345645, 11.47551654964653167, 455.0000000000000568 ) ) ;
#6095=FACE_OUTER_BOUND ( 'NONE', #46324, .T. ) ;
#6102=ORIENTED_EDGE ( 'NONE', *, *, #49679, .F. ) ;
#6116=VECTOR ( 'NONE', #28740, 1000.000000000000000 ) ;
#6121=AXIS2_PLACEMENT_3D ( 'NONE', #53748, #4957, #49478 ) ;
#6127=ORIENTED_EDGE ( 'NONE', *, *, #26781, .T. ) ;
#6131=DIRECTION ( 'NONE',  ( -0.000000000000000000, -0.000000000000000000, -1.000000000000000000 ) ) ;
#6133=DIRECTION ( 'NONE',  ( -1.000000000000000000, 1.356437060717834182E-15, 0.000000000000000000 ) ) ;
#6137=DIRECTION ( 'NONE',  ( 1.836970198721029934E-16, 1.836970198721010706E-16, -1.000000000000000000 ) ) ;
#6147=AXIS2_PLACEMENT_3D ( 'NONE', #17947, #40565, #22916 ) ;
#6149=CYLINDRICAL_SURFACE ( 'NONE', #58046, 0.1999999999999987899 ) ;
#6154=EDGE_CURVE ( 'NONE', #8669, #44324, #35028, .T. ) ;
#6156=DIRECTION ( 'NONE',  ( 0.8660254037844363761, -0.5000000000000038858, -1.836970198721044232E-16 ) ) ;
#6159=ORIENTED_EDGE ( 'NONE', *, *, #9694, .T. ) ;
#6168=ADVANCED_FACE ( 'NONE', ( #66437 ), #16719, .F. ) ;
#6170=CARTESIAN_POINT ( 'NONE',  ( 10.09643294401454661, -2.706483450353491804, 455.0000000000000568 ) ) ;
#6178=EDGE_LOOP ( 'NONE', ( #25089, #9906, #42540, #36778 ) ) ;
#6184=ORIENTED_EDGE ( 'NONE', *, *, #45345, .T. ) ;
#6198=DIRECTION ( 'NONE',  ( -0.000000000000000000, 3.673940397442059868E-16, -1.000000000000000000 ) ) ;
#6205=ORIENTED_EDGE ( 'NONE', *, *, #25417, .T. ) ;
#6207=CARTESIAN_POINT ( 'NONE',  ( -7.839518282750280065, -3.430747519065322049, 455.0000000000000568 ) ) ;
#6213=VECTOR ( 'NONE', #69635, 1000.000000000000000 ) ;
#6217=PLANE ( 'NONE',  #6219 ) ;
#6219=AXIS2_PLACEMENT_3D ( 'NONE', #50031, #66641, #60982 ) ;
#6222=CARTESIAN_POINT ( 'NONE',  ( -5.380658396643233310, 7.252248008019342329, 455.0000000000000568 ) ) ;
#6231=CARTESIAN_POINT ( 'NONE',  ( 10.20488345035345468, 10.19191654964656735, 455.0000000000000568 ) ) ;
#6233=EDGE_CURVE ( 'NONE', #29795, #49979, #56865, .T. ) ;
#6249=CARTESIAN_POINT ( 'NONE',  ( -7.259684009079930611, 7.798499376343971612, 455.0000000000000568 ) ) ;
#6254=EDGE_CURVE ( 'NONE', #44953, #26897, #67130, .T. ) ;
#6256=VERTEX_POINT ( 'NONE', #35280 ) ;
#6260=AXIS2_PLACEMENT_3D ( 'NONE', #58535, #10082, #26340 ) ;
#6262=VERTEX_POINT ( 'NONE', #34599 ) ;
#6268=ADVANCED_FACE ( 'NONE', ( #51212 ), #14454, .F. ) ;
#6281=AXIS2_PLACEMENT_3D ( 'NONE', #37688, #16119, #52197 ) ;
#6298=DIRECTION ( 'NONE',  ( 1.000000000000000000, 0.000000000000000000, 0.000000000000000000 ) ) ;
#6299=AXIS2_PLACEMENT_3D ( 'NONE', #11069, #32635, #16726 ) ;
#6303=CARTESIAN_POINT ( 'NONE',  ( -7.415254214038345282, -3.006483450353401032, 455.0000000000000568 ) ) ;
#6304=DIRECTION ( 'NONE',  ( -0.6414496315691420314, 0.7671651518153128624, 2.587583378555127804E-16 ) ) ;
#6312=ORIENTED_EDGE ( 'NONE', *, *, #25907, .T. ) ;
#6320=CARTESIAN_POINT ( 'NONE',  ( 11.08848345035341687, 9.791916549646563439, 455.0000000000000568 ) ) ;
#6327=LINE ( 'NONE', #43106, #67528 ) ;
#6331=VERTEX_POINT ( 'NONE', #52274 ) ;
#6342=ORIENTED_EDGE ( 'NONE', *, *, #37220, .T. ) ;
#6350=VERTEX_POINT ( 'NONE', #3146 ) ;
#6359=CARTESIAN_POINT ( 'NONE',  ( -2.752095193409509033, -9.955011587777317317, 455.0000000000000568 ) ) ;
#6360=ORIENTED_EDGE ( 'NONE', *, *, #62996, .F. ) ;
#6361=ORIENTED_EDGE ( 'NONE', *, *, #65721, .T. ) ;
#6374=DIRECTION ( 'NONE',  ( -0.7671651518153065341, 0.6414496315691495809, 2.356647714346224881E-16 ) ) ;
#6376=CARTESIAN_POINT ( 'NONE',  ( 6.006483450353379716, -6.006483450353490738, 455.0000000000000568 ) ) ;
#6383=CARTESIAN_POINT ( 'NONE',  ( 12.00648345035338238, 4.173516549646515195, 455.0000000000000568 ) ) ;
#6389=VERTEX_POINT ( 'NONE', #41660 ) ;
#6392=LINE ( 'NONE', #5005, #60589 ) ;
#6405=EDGE_CURVE ( 'NONE', #41004, #59963, #21491, .T. ) ;
#6406=DIRECTION ( 'NONE',  ( -1.000000000000000000, 0.000000000000000000, 0.000000000000000000 ) ) ;
#6407=AXIS2_PLACEMENT_3D ( 'NONE', #50865, #39897, #1393 ) ;
#6410=AXIS2_PLACEMENT_3D ( 'NONE', #29190, #13287, #34843 ) ;
#6412=ORIENTED_EDGE ( 'NONE', *, *, #34510, .F. ) ;
#6418=ADVANCED_FACE ( 'NONE', ( #15507 ), #53338, .F. ) ;
#6419=ADVANCED_FACE ( 'NONE', ( #64626 ), #14801, .T. ) ;
#6425=LINE ( 'NONE', #1119, #47596 ) ;
#6426=EDGE_LOOP ( 'NONE', ( #55242, #65312, #42684, #54565 ) ) ;
#6427=ORIENTED_EDGE ( 'NONE', *, *, #38103, .T. ) ;
#6433=LINE ( 'NONE', #59480, #36812 ) ;
#6438=EDGE_LOOP ( 'NONE', ( #51740, #42016, #26144, #4938 ) ) ;
#6449=ORIENTED_EDGE ( 'NONE', *, *, #56689, .F. ) ;
#6451=CARTESIAN_POINT ( 'NONE',  ( 6.006483450353401921, 5.993516549646582092, 455.0000000000000568 ) ) ;
#6471=FACE_OUTER_BOUND ( 'NONE', #27537, .T. ) ;
#6478=LINE ( 'NONE', #22727, #44606 ) ;
#6487=EDGE_CURVE ( 'NONE', #22188, #63555, #58973, .T. ) ;
#6510=CYLINDRICAL_SURFACE ( 'NONE', #40775, 0.3999999999999993006 ) ;
#6513=VERTEX_POINT ( 'NONE', #11900 ) ;
#6516=AXIS2_PLACEMENT_3D ( 'NONE', #32289, #22382, #17063 ) ;
#6530=CARTESIAN_POINT ( 'NONE',  ( 6.344579767990853547, 8.393516549646580671, 455.0000000000000568 ) ) ;
#6544=ORIENTED_EDGE ( 'NONE', *, *, #19900, .T. ) ;
#6564=CARTESIAN_POINT ( 'NONE',  ( 7.428221114744993692, 2.993516549646566105, 455.0000000000000568 ) ) ;
#6572=EDGE_CURVE ( 'NONE', #3924, #64205, #65995, .T. ) ;
#6581=CARTESIAN_POINT ( 'NONE',  ( -5.993516549646728642, -6.006483450353378828, 195.0000000000000284 ) ) ;
#6582=VERTEX_POINT ( 'NONE', #17563 ) ;
#6583=FACE_OUTER_BOUND ( 'NONE', #15741, .T. ) ;
#6586=DIRECTION ( 'NONE',  ( -1.000000000000000000, 0.000000000000000000, 0.000000000000000000 ) ) ;
#6587=DIRECTION ( 'NONE',  ( -0.8660254037844358210, 0.5000000000000049960, 2.509347957447882735E-16 ) ) ;
#6592=PLANE ( 'NONE',  #51010 ) ;
#6602=CARTESIAN_POINT ( 'NONE',  ( -4.393516549646835578, -11.78648345035344214, 455.0000000000000568 ) ) ;
#6607=DIRECTION ( 'NONE',  ( -0.000000000000000000, 3.673940397442059868E-16, -1.000000000000000000 ) ) ;
#6608=LINE ( 'NONE', #1301, #68343 ) ;
#6610=EDGE_LOOP ( 'NONE', ( #65830, #30027, #58651, #15113 ) ) ;
#6614=ORIENTED_EDGE ( 'NONE', *, *, #54108, .T. ) ;
#6617=CARTESIAN_POINT ( 'NONE',  ( -7.813516549646711162, 11.99351654964660341, 195.0000000000000284 ) ) ;
#6627=EDGE_LOOP ( 'NONE', ( #67079, #14290, #12799, #17636 ) ) ;
#6629=DIRECTION ( 'NONE',  ( -0.8660254037844363761, 0.5000000000000038858, 0.000000000000000000 ) ) ;
#6635=ORIENTED_EDGE ( 'NONE', *, *, #29698, .T. ) ;
#6637=EDGE_CURVE ( 'NONE', #67306, #5737, #11223, .T. ) ;
#6638=DIRECTION ( 'NONE',  ( 0.7071067811865401342, -0.7071067811865550112, -1.365336182113289717E-30 ) ) ;
#6639=CIRCLE ( 'NONE', #43943, 0.1999999999999996503 ) ;
#6641=EDGE_CURVE ( 'NONE', #60888, #5423, #17910, .T. ) ;
#6644=AXIS2_PLACEMENT_3D ( 'NONE', #47517, #4738, #43251 ) ;
#6649=VERTEX_POINT ( 'NONE', #54373 ) ;
#6652=AXIS2_PLACEMENT_3D ( 'NONE', #55877, #55536, #7080 ) ;
#6655=DIRECTION ( 'NONE',  ( 1.000000000000000000, 0.000000000000000000, 0.000000000000000000 ) ) ;
#6656=VECTOR ( 'NONE', #67075, 1000.000000000000000 ) ;
#6659=DIRECTION ( 'NONE',  ( -0.000000000000000000, -0.000000000000000000, -1.000000000000000000 ) ) ;
#6662=CIRCLE ( 'NONE', #46181, 0.4000000000000010214 ) ;
#6689=LINE ( 'NONE', #50171, #51733 ) ;
#6691=EDGE_LOOP ( 'NONE', ( #63135, #45173, #49523, #4829 ) ) ;
#6692=VECTOR ( 'NONE', #38231, 1000.000000000000114 ) ;
#6701=FACE_OUTER_BOUND ( 'NONE', #443, .T. ) ;
#6702=DIRECTION ( 'NONE',  ( 1.000000000000000000, 0.000000000000000000, 0.000000000000000000 ) ) ;
#6703=DIRECTION ( 'NONE',  ( -1.000000000000000000, 0.000000000000000000, 0.000000000000000000 ) ) ;
#6713=LINE ( 'NONE', #5364, #7811 ) ;
#6719=ORIENTED_EDGE ( 'NONE', *, *, #9055, .F. ) ;
#6728=ORIENTED_EDGE ( 'NONE', *, *, #38752, .T. ) ;
#6731=DIRECTION ( 'NONE',  ( -1.000000000000000000, 5.120954910632640039E-15, 1.881408311965255020E-30 ) ) ;
#6735=EDGE_CURVE ( 'NONE', #55886, #29102, #2349, .T. ) ;
#6736=VECTOR ( 'NONE', #12230, 1000.000000000000000 ) ;
#6737=DIRECTION ( 'NONE',  ( -1.836970198721029934E-16, 1.836970198721036344E-16, -1.000000000000000000 ) ) ;
#6738=ORIENTED_EDGE ( 'NONE', *, *, #56242, .T. ) ;
#6742=CIRCLE ( 'NONE', #33793, 2.204799999999996540 ) ;
#6755=CARTESIAN_POINT ( 'NONE',  ( -7.259684009079930611, 4.188533722949235205, 455.0000000000000568 ) ) ;
#6759=FACE_OUTER_BOUND ( 'NONE', #60773, .T. ) ;
#6761=ORIENTED_EDGE ( 'NONE', *, *, #17626, .F. ) ;
#6766=DIRECTION ( 'NONE',  ( 0.7071067811865451302, -0.7071067811865500152, -2.597868168706485527E-16 ) ) ;
#6769=LINE ( 'NONE', #44253, #65841 ) ;
#6771=ORIENTED_EDGE ( 'NONE', *, *, #26779, .F. ) ;
#6772=EDGE_CURVE ( 'NONE', #43371, #8459, #10323, .T. ) ;
#6780=AXIS2_PLACEMENT_3D ( 'NONE', #41550, #31655, #25651 ) ;
#6784=DIRECTION ( 'NONE',  ( 1.000000000000000000, 0.000000000000000000, 0.000000000000000000 ) ) ;
#6786=ORIENTED_EDGE ( 'NONE', *, *, #67366, .T. ) ;
#6789=CYLINDRICAL_SURFACE ( 'NONE', #68488, 0.1999999999999987899 ) ;
#6793=DIRECTION ( 'NONE',  ( 1.836970198721029934E-16, 1.836970198721010706E-16, -1.000000000000000000 ) ) ;
#6812=ADVANCED_FACE ( 'NONE', ( #41220 ), #46524, .F. ) ;
#6813=DIRECTION ( 'NONE',  ( -0.7071067811865451302, 0.7071067811865500152, 2.597868168706484541E-16 ) ) ;
#6814=EDGE_CURVE ( 'NONE', #60569, #64371, #8337, .T. ) ;
#6815=ORIENTED_EDGE ( 'NONE', *, *, #64387, .T. ) ;
#6816=CARTESIAN_POINT ( 'NONE',  ( 10.92648345035337520, -2.906483450353395614, 195.0000000000000284 ) ) ;
#6817=ORIENTED_EDGE ( 'NONE', *, *, #41922, .T. ) ;
#6818=ORIENTED_EDGE ( 'NONE', *, *, #59179, .F. ) ;
#6824=DIRECTION ( 'NONE',  ( -0.000000000000000000, 3.673940397442059868E-16, -1.000000000000000000 ) ) ;
#6826=VERTEX_POINT ( 'NONE', #68100 ) ;
#6830=LINE ( 'NONE', #37729, #23544 ) ;
#6839=VERTEX_POINT ( 'NONE', #63147 ) ;
#6845=VECTOR ( 'NONE', #36581, 1000.000000000000000 ) ;
#6849=ORIENTED_EDGE ( 'NONE', *, *, #36414, .T. ) ;
#6864=CARTESIAN_POINT ( 'NONE',  ( 1.690483450353418737, 10.73351654964659652, 455.0000000000000568 ) ) ;
#6873=DIRECTION ( 'NONE',  ( 2.135044278125299371E-15, 1.000000000000000000, 0.000000000000000000 ) ) ;
#6874=ADVANCED_FACE ( 'NONE', ( #36275 ), #57840, .F. ) ;
#6892=VECTOR ( 'NONE', #29540, 1000.000000000000000 ) ;
#6897=CIRCLE ( 'NONE', #53266, 0.2000000000000005107 ) ;
#6910=DIRECTION ( 'NONE',  ( 1.836970198721029934E-16, 1.836970198721010706E-16, -1.000000000000000000 ) ) ;
#6919=CARTESIAN_POINT ( 'NONE',  ( -11.11351654964668612, 8.693516549646636449, 455.0000000000000568 ) ) ;
#6928=DIRECTION ( 'NONE',  ( -1.000000000000000000, 0.000000000000000000, 0.000000000000000000 ) ) ;
#6936=EDGE_CURVE ( 'NONE', #18478, #35648, #20708, .T. ) ;
#6945=LINE ( 'NONE', #29202, #43937 ) ;
#6947=VECTOR ( 'NONE', #42073, 1000.000000000000000 ) ;
#6953=EDGE_CURVE ( 'NONE', #9826, #51301, #34018, .T. ) ;
#6958=CARTESIAN_POINT ( 'NONE',  ( 2.290483450353415495, 9.828310488885934504, 455.0000000000000568 ) ) ;
#6970=DIRECTION ( 'NONE',  ( 0.000000000000000000, -3.673940397442059868E-16, 1.000000000000000000 ) ) ;
#6980=CARTESIAN_POINT ( 'NONE',  ( -9.791916549646867196, -11.08848345035335115, 455.0000000000000568 ) ) ;
#6982=DIRECTION ( 'NONE',  ( -1.836970198721029934E-16, -1.836970198721010706E-16, 1.000000000000000000 ) ) ;
#6986=VECTOR ( 'NONE', #12910, 1000.000000000000000 ) ;
#6989=FACE_OUTER_BOUND ( 'NONE', #17742, .T. ) ;
#6992=AXIS2_PLACEMENT_3D ( 'NONE', #59386, #64013, #38182 ) ;
#6998=CARTESIAN_POINT ( 'NONE',  ( 10.92648345035335922, 9.293516549646611224, 195.0000000000000284 ) ) ;
#7005=ORIENTED_EDGE ( 'NONE', *, *, #9461, .T. ) ;
#7009=DIRECTION ( 'NONE',  ( 1.836970198721029934E-16, 1.836970198721010706E-16, -1.000000000000000000 ) ) ;
#7011=DIRECTION ( 'NONE',  ( 0.000000000000000000, -3.673940397442059868E-16, 1.000000000000000000 ) ) ;
#7012=VERTEX_POINT ( 'NONE', #32715 ) ;
#7017=VERTEX_POINT ( 'NONE', #38709 ) ;
#7024=EDGE_CURVE ( 'NONE', #52964, #3924, #22797, .T. ) ;
#7027=CIRCLE ( 'NONE', #46548, 0.1999999999999987899 ) ;
#7030=EDGE_CURVE ( 'NONE', #13690, #66560, #39055, .T. ) ;
#7038=CARTESIAN_POINT ( 'NONE',  ( -4.173516549646669738, 11.77351654964658678, 455.0000000000000568 ) ) ;
#7041=ORIENTED_EDGE ( 'NONE', *, *, #58586, .F. ) ;
#7046=CARTESIAN_POINT ( 'NONE',  ( 10.92648345035335922, 2.693516549646528091, 455.0000000000000568 ) ) ;
#7054=CIRCLE ( 'NONE', #13878, 0.5999999999999989786 ) ;
#7065=DIRECTION ( 'NONE',  ( 0.000000000000000000, -0.000000000000000000, 1.000000000000000000 ) ) ;
#7068=DIRECTION ( 'NONE',  ( -0.7071067811865529018, -0.7071067811865422437, 0.000000000000000000 ) ) ;
#7074=FACE_OUTER_BOUND ( 'NONE', #4115, .T. ) ;
#7078=CARTESIAN_POINT ( 'NONE',  ( -8.513516549646713116, 11.29351654964659701, 455.0000000000000568 ) ) ;
#7080=DIRECTION ( 'NONE',  ( -1.048062100069321163E-14, -1.000000000000000000, 0.000000000000000000 ) ) ;
#7084=CARTESIAN_POINT ( 'NONE',  ( 4.186483450353335023, -12.00648345035347830, 455.0000000000000568 ) ) ;
#7094=CARTESIAN_POINT ( 'NONE',  ( 1.866219381641485375, 9.404046420174006826, 455.0000000000000568 ) ) ;
#7099=VECTOR ( 'NONE', #7331, 1000.000000000000000 ) ;
#7102=ORIENTED_EDGE ( 'NONE', *, *, #14352, .T. ) ;
#7122=PLANE ( 'NONE',  #37964 ) ;
#7133=CARTESIAN_POINT ( 'NONE',  ( 7.616533956692197016, 8.393516549646621527, 195.0000000000000284 ) ) ;
#7137=CARTESIAN_POINT ( 'NONE',  ( -7.593516549646711411, 11.77351654964660277, 455.0000000000000568 ) ) ;
#7145=VECTOR ( 'NONE', #18035, 1000.000000000000000 ) ;
#7160=ORIENTED_EDGE ( 'NONE', *, *, #25476, .T. ) ;
#7169=DIRECTION ( 'NONE',  ( 0.000000000000000000, 0.000000000000000000, 1.000000000000000000 ) ) ;
#7174=LINE ( 'NONE', #19193, #64348 ) ;
#7178=DIRECTION ( 'NONE',  ( -0.000000000000000000, -0.000000000000000000, -1.000000000000000000 ) ) ;
#7183=DIRECTION ( 'NONE',  ( -0.000000000000000000, -0.000000000000000000, -1.000000000000000000 ) ) ;
#7184=LINE ( 'NONE', #55310, #31545 ) ;
#7188=EDGE_CURVE ( 'NONE', #29997, #6582, #18518, .T. ) ;
#7189=ORIENTED_EDGE ( 'NONE', *, *, #2117, .T. ) ;
#7220=FACE_OUTER_BOUND ( 'NONE', #68173, .T. ) ;
#7224=ADVANCED_FACE ( 'NONE', ( #45739 ), #67328, .T. ) ;
#7229=AXIS2_PLACEMENT_3D ( 'NONE', #55785, #1354, #7330 ) ;
#7235=CARTESIAN_POINT ( 'NONE',  ( 4.406483450353373854, 11.31351654964663211, 195.0000000000000284 ) ) ;
#7236=AXIS2_PLACEMENT_3D ( 'NONE', #20659, #3356, #52146 ) ;
#7238=ORIENTED_EDGE ( 'NONE', *, *, #46194, .T. ) ;
#7244=VECTOR ( 'NONE', #46319, 1000.000000000000114 ) ;
#7245=ORIENTED_EDGE ( 'NONE', *, *, #48956, .T. ) ;
#7255=DIRECTION ( 'NONE',  ( -1.000000000000000000, 0.000000000000000000, 0.000000000000000000 ) ) ;
#7257=AXIS2_PLACEMENT_3D ( 'NONE', #19145, #24096, #57678 ) ;
#7258=EDGE_CURVE ( 'NONE', #15497, #13690, #14287, .T. ) ;
#7261=DIRECTION ( 'NONE',  ( 1.836970198721029934E-16, 1.836970198721010706E-16, -1.000000000000000000 ) ) ;
#7275=VERTEX_POINT ( 'NONE', #25952 ) ;
#7279=DIRECTION ( 'NONE',  ( 1.836970198721029934E-16, -1.836970198721036344E-16, 1.000000000000000000 ) ) ;
#7280=ORIENTED_EDGE ( 'NONE', *, *, #25528, .F. ) ;
#7284=LINE ( 'NONE', #34153, #9054 ) ;
#7294=VECTOR ( 'NONE', #50143, 1000.000000000000114 ) ;
#7301=CYLINDRICAL_SURFACE ( 'NONE', #58399, 0.5999999999999998668 ) ;
#7319=LINE ( 'NONE', #38818, #5915 ) ;
#7326=AXIS2_PLACEMENT_3D ( 'NONE', #42931, #26325, #26678 ) ;
#7328=FACE_OUTER_BOUND ( 'NONE', #27836, .T. ) ;
#7330=DIRECTION ( 'NONE',  ( 1.000000000000000000, 0.000000000000000000, 0.000000000000000000 ) ) ;
#7331=DIRECTION ( 'NONE',  ( -0.000000000000000000, -0.000000000000000000, -1.000000000000000000 ) ) ;
#7336=CIRCLE ( 'NONE', #24263, 2.204799999999997873 ) ;
#7340=DIRECTION ( 'NONE',  ( 1.000000000000000000, 0.000000000000000000, 0.000000000000000000 ) ) ;
#7343=EDGE_CURVE ( 'NONE', #42524, #32112, #23732, .T. ) ;
#7351=ORIENTED_EDGE ( 'NONE', *, *, #61263, .F. ) ;
#7366=VERTEX_POINT ( 'NONE', #61194 ) ;
#7375=ORIENTED_EDGE ( 'NONE', *, *, #21697, .T. ) ;
#7376=ORIENTED_EDGE ( 'NONE', *, *, #47587, .T. ) ;
#7388=CIRCLE ( 'NONE', #46921, 1.399999999999999245 ) ;
#7391=DIRECTION ( 'NONE',  ( 0.000000000000000000, 3.673940397442059868E-16, -1.000000000000000000 ) ) ;
#7404=ORIENTED_EDGE ( 'NONE', *, *, #21881, .T. ) ;
#7413=VECTOR ( 'NONE', #53365, 1000.000000000000000 ) ;
#7425=EDGE_CURVE ( 'NONE', #45642, #47767, #16886, .T. ) ;
#7431=CARTESIAN_POINT ( 'NONE',  ( -8.693516549646711056, 11.11351654964659730, 194.9999952000000292 ) ) ;
#7433=AXIS2_PLACEMENT_3D ( 'NONE', #44705, #21772, #54303 ) ;
#7434=EDGE_LOOP ( 'NONE', ( #42087, #69786, #16376, #52830 ) ) ;
#7435=LINE ( 'NONE', #67893, #16712 ) ;
#7436=DIRECTION ( 'NONE',  ( -0.000000000000000000, -0.000000000000000000, -1.000000000000000000 ) ) ;
#7438=DIRECTION ( 'NONE',  ( 8.673617379884087537E-15, 1.000000000000000000, 0.000000000000000000 ) ) ;
#7439=CARTESIAN_POINT ( 'NONE',  ( -5.655420232009359616, -8.406483450353428921, 455.0000000000000568 ) ) ;
#7440=ORIENTED_EDGE ( 'NONE', *, *, #29181, .F. ) ;
#7453=VECTOR ( 'NONE', #38525, 1000.000000000000000 ) ;
#7455=CARTESIAN_POINT ( 'NONE',  ( 11.34648345035334671, 1.077516549646521327, 455.0000000000000568 ) ) ;
#7474=PLANE ( 'NONE',  #53385 ) ;
#7479=LINE ( 'NONE', #29743, #24966 ) ;
#7490=AXIS2_PLACEMENT_3D ( 'NONE', #26908, #6374, #54813 ) ;
#7501=CARTESIAN_POINT ( 'NONE',  ( 3.430747519065288298, 7.839518282750187694, 195.0000000000000284 ) ) ;
#7507=ORIENTED_EDGE ( 'NONE', *, *, #27325, .T. ) ;
#7509=AXIS2_PLACEMENT_3D ( 'NONE', #45562, #62895, #35651 ) ;
#7520=ORIENTED_EDGE ( 'NONE', *, *, #45587, .T. ) ;
#7521=DIRECTION ( 'NONE',  ( -7.304098846218132892E-15, -1.000000000000000000, 0.000000000000000000 ) ) ;
#7527=ORIENTED_EDGE ( 'NONE', *, *, #4897, .T. ) ;
#7529=FACE_OUTER_BOUND ( 'NONE', #8938, .T. ) ;
#7536=VECTOR ( 'NONE', #21278, 1000.000000000000000 ) ;
#7538=CARTESIAN_POINT ( 'NONE',  ( -10.08346604330787777, 9.293516549646602343, 195.0000000000000284 ) ) ;
#7546=LINE ( 'NONE', #23470, #39938 ) ;
#7547=LINE ( 'NONE', #12498, #52997 ) ;
#7563=ORIENTED_EDGE ( 'NONE', *, *, #10333, .T. ) ;
#7572=CARTESIAN_POINT ( 'NONE',  ( 11.48848345035341900, 10.19191654964656202, 455.0000000000000568 ) ) ;
#7577=LINE ( 'NONE', #51771, #1804 ) ;
#7578=DIRECTION ( 'NONE',  ( 1.836970198721029934E-16, 1.836970198721010706E-16, -1.000000000000000000 ) ) ;
#7581=CARTESIAN_POINT ( 'NONE',  ( 7.811466277050774565, 7.259684009079793832, 455.0000000000000568 ) ) ;
#7588=ORIENTED_EDGE ( 'NONE', *, *, #10733, .F. ) ;
#7593=CARTESIAN_POINT ( 'NONE',  ( 8.406483450353405829, 7.603567055985406498, 455.0000000000000568 ) ) ;
#7599=LINE ( 'NONE', #12886, #2212 ) ;
#7604=VECTOR ( 'NONE', #4525, 1000.000000000000000 ) ;
#7615=ORIENTED_EDGE ( 'NONE', *, *, #60050, .F. ) ;
#7622=FACE_OUTER_BOUND ( 'NONE', #13034, .T. ) ;
#7631=VECTOR ( 'NONE', #18457, 1000.000000000000000 ) ;
#7641=DIRECTION ( 'NONE',  ( -1.000000000000000000, 0.000000000000000000, 0.000000000000000000 ) ) ;
#7651=CARTESIAN_POINT ( 'NONE',  ( -7.798499376344067535, 7.259684009079840017, 455.0000000000000568 ) ) ;
#7654=DIRECTION ( 'NONE',  ( 8.673617379884051249E-15, 1.000000000000000000, 0.000000000000000000 ) ) ;
#7675=DIRECTION ( 'NONE',  ( -1.836970198721029934E-16, -1.836970198721010706E-16, 1.000000000000000000 ) ) ;
#7678=DIRECTION ( 'NONE',  ( -1.836970198721029934E-16, 1.836970198721036344E-16, -1.000000000000000000 ) ) ;
#7679=DIRECTION ( 'NONE',  ( -1.836970198721029934E-16, 1.836970198721036344E-16, -1.000000000000000000 ) ) ;
#7680=ORIENTED_EDGE ( 'NONE', *, *, #16742, .F. ) ;
#7686=DIRECTION ( 'NONE',  ( -1.000000000000000000, 1.047444401652940007E-14, -1.836970198721010706E-16 ) ) ;
#7695=VECTOR ( 'NONE', #61475, 1000.000000000000000 ) ;
#7703=ORIENTED_EDGE ( 'NONE', *, *, #52674, .T. ) ;
#7704=VECTOR ( 'NONE', #50119, 1000.000000000000000 ) ;
#7716=ORIENTED_EDGE ( 'NONE', *, *, #17896, .F. ) ;
#7717=EDGE_CURVE ( 'NONE', #29989, #56381, #7284, .T. ) ;
#7721=EDGE_CURVE ( 'NONE', #33806, #11215, #13297, .T. ) ;
#7730=ORIENTED_EDGE ( 'NONE', *, *, #28665, .F. ) ;
#7742=ORIENTED_EDGE ( 'NONE', *, *, #41609, .F. ) ;
#7744=VERTEX_POINT ( 'NONE', #5672 ) ;
#7756=DIRECTION ( 'NONE',  ( -0.000000000000000000, -0.000000000000000000, -1.000000000000000000 ) ) ;
#7770=FACE_OUTER_BOUND ( 'NONE', #66607, .T. ) ;
#7775=VERTEX_POINT ( 'NONE', #13995 ) ;
#7777=ORIENTED_EDGE ( 'NONE', *, *, #39615, .T. ) ;
#7790=DIRECTION ( 'NONE',  ( 3.491481338843133355E-15, 1.000000000000000000, 1.836970198721029934E-16 ) ) ;
#7805=VECTOR ( 'NONE', #18607, 1000.000000000000000 ) ;
#7811=VECTOR ( 'NONE', #39919, 1000.000000000000000 ) ;
#7812=DIRECTION ( 'NONE',  ( 0.8660254037844375974, -0.5000000000000019984, 0.000000000000000000 ) ) ;
#7818=EDGE_CURVE ( 'NONE', #36255, #4470, #51485, .T. ) ;
#7837=CARTESIAN_POINT ( 'NONE',  ( 9.955011587777223170, 2.752095193409229257, 455.0000000000000568 ) ) ;
#7841=CARTESIAN_POINT ( 'NONE',  ( -7.813516549646839948, -12.00648345035340903, 455.0000000000000568 ) ) ;
#7853=EDGE_CURVE ( 'NONE', #58981, #31830, #13644, .T. ) ;
#7858=EDGE_CURVE ( 'NONE', #4281, #65753, #62080, .T. ) ;
#7861=VECTOR ( 'NONE', #58269, 1000.000000000000000 ) ;
#7866=LINE ( 'NONE', #18473, #21609 ) ;
#7869=DIRECTION ( 'NONE',  ( -0.000000000000000000, 3.673940397442059868E-16, -1.000000000000000000 ) ) ;
#7873=LINE ( 'NONE', #29799, #3363 ) ;
#7875=VECTOR ( 'NONE', #50436, 1000.000000000000114 ) ;
#7883=CARTESIAN_POINT ( 'NONE',  ( 9.306483450353372433, 10.91351654964661044, 195.0000000000000284 ) ) ;
#7884=DIRECTION ( 'NONE',  ( 1.678252938371784572E-14, 1.000000000000000000, 0.000000000000000000 ) ) ;
#7885=DIRECTION ( 'NONE',  ( -0.000000000000000000, 3.673940397442059868E-16, -1.000000000000000000 ) ) ;
#7891=ORIENTED_EDGE ( 'NONE', *, *, #45330, .F. ) ;
#7894=ORIENTED_EDGE ( 'NONE', *, *, #59371, .T. ) ;
#7895=ORIENTED_EDGE ( 'NONE', *, *, #61402, .F. ) ;
#7896=ADVANCED_FACE ( 'NONE', ( #24258 ), #35197, .T. ) ;
#7898=VERTEX_POINT ( 'NONE', #46518 ) ;
#7904=DIRECTION ( 'NONE',  ( 0.000000000000000000, -3.673940397442059868E-16, 1.000000000000000000 ) ) ;
#7911=LINE ( 'NONE', #7572, #41528 ) ;
#7919=LINE ( 'NONE', #1933, #14649 ) ;
#7925=VERTEX_POINT ( 'NONE', #4111 ) ;
#7935=EDGE_CURVE ( 'NONE', #21629, #43736, #25682, .T. ) ;
#7936=VECTOR ( 'NONE', #60665, 1000.000000000000000 ) ;
#7939=DIRECTION ( 'NONE',  ( 1.836970198721029934E-16, 1.836970198721010706E-16, -1.000000000000000000 ) ) ;
#7946=ORIENTED_EDGE ( 'NONE', *, *, #56164, .F. ) ;
#7960=CIRCLE ( 'NONE', #28262, 0.4000000000000010214 ) ;
#7985=CARTESIAN_POINT ( 'NONE',  ( -4.727349090213552429, -4.201500623656063915, 455.0000000000000568 ) ) ;
#7986=CARTESIAN_POINT ( 'NONE',  ( -11.77351654964670935, 4.393516549646602876, 455.0000000000000568 ) ) ;
#7991=ORIENTED_EDGE ( 'NONE', *, *, #53670, .F. ) ;
#7992=VECTOR ( 'NONE', #35260, 1000.000000000000114 ) ;
#7997=EDGE_CURVE ( 'NONE', #3545, #68313, #58894, .T. ) ;
#8008=DIRECTION ( 'NONE',  ( -0.000000000000000000, 3.673940397442059868E-16, -1.000000000000000000 ) ) ;
#8011=CARTESIAN_POINT ( 'NONE',  ( 7.811466277050736373, -4.740315990920255018, 455.0000000000000568 ) ) ;
#8019=VERTEX_POINT ( 'NONE', #38031 ) ;
#8031=CARTESIAN_POINT ( 'NONE',  ( -8.393516549646768965, -5.668387132715940524, 455.0000000000000568 ) ) ;
#8039=VECTOR ( 'NONE', #30851, 1000.000000000000000 ) ;
#8040=AXIS2_PLACEMENT_3D ( 'NONE', #63916, #63570, #64955 ) ;
#8042=EDGE_CURVE ( 'NONE', #391, #12677, #54198, .T. ) ;
#8046=FACE_OUTER_BOUND ( 'NONE', #43894, .T. ) ;
#8051=DIRECTION ( 'NONE',  ( -1.000000000000000000, 0.000000000000000000, 0.000000000000000000 ) ) ;
#8052=FACE_OUTER_BOUND ( 'NONE', #17377, .T. ) ;
#8066=DIRECTION ( 'NONE',  ( 1.836970198721029934E-16, -1.836970198721036344E-16, 1.000000000000000000 ) ) ;
#8075=ADVANCED_FACE ( 'NONE', ( #26024 ), #47577, .F. ) ;
#8085=FACE_OUTER_BOUND ( 'NONE', #64906, .T. ) ;
#8110=CARTESIAN_POINT ( 'NONE',  ( -11.47551654964667733, 11.07551654964660237, 195.0000000000000284 ) ) ;
#8133=ORIENTED_EDGE ( 'NONE', *, *, #11805, .F. ) ;
#8151=ORIENTED_EDGE ( 'NONE', *, *, #41956, .T. ) ;
#8155=CARTESIAN_POINT ( 'NONE',  ( -9.093516549646817992, -10.09643294401455904, 455.0000000000000568 ) ) ;
#8163=VECTOR ( 'NONE', #17937, 1000.000000000000000 ) ;
#8167=ORIENTED_EDGE ( 'NONE', *, *, #58052, .T. ) ;
#8168=CARTESIAN_POINT ( 'NONE',  ( 10.09643294401454661, -9.306483450353491449, 455.0000000000000568 ) ) ;
#8172=EDGE_CURVE ( 'NONE', #50332, #17779, #24832, .T. ) ;
#8174=LINE ( 'NONE', #36101, #15892 ) ;
#8176=VERTEX_POINT ( 'NONE', #51046 ) ;
#8183=DIRECTION ( 'NONE',  ( 0.000000000000000000, -3.673940397442059868E-16, 1.000000000000000000 ) ) ;
#8190=EDGE_LOOP ( 'NONE', ( #26494, #4937, #45455, #8913 ) ) ;
#8198=CARTESIAN_POINT ( 'NONE',  ( 9.417013320880792904, -1.866219381641561315, 455.0000000000000568 ) ) ;
#8200=EDGE_CURVE ( 'NONE', #18501, #68804, #3312, .T. ) ;
#8202=EDGE_CURVE ( 'NONE', #43425, #4452, #22617, .T. ) ;
#8208=EDGE_CURVE ( 'NONE', #20324, #20952, #68728, .T. ) ;
#8224=ORIENTED_EDGE ( 'NONE', *, *, #26718, .F. ) ;
#8238=CARTESIAN_POINT ( 'NONE',  ( -12.00854180281612571, 7.798491296477156887, 195.0000000000000284 ) ) ;
#8240=CARTESIAN_POINT ( 'NONE',  ( 6.006483450353353959, 5.993516549646629166, 195.0000000000000284 ) ) ;
#8241=DIRECTION ( 'NONE',  ( 1.000000000000000000, -1.130039751537442024E-14, -1.836970198721050642E-16 ) ) ;
#8250=ORIENTED_EDGE ( 'NONE', *, *, #62843, .T. ) ;
#8251=LINE ( 'NONE', #16028, #32800 ) ;
#8267=DIRECTION ( 'NONE',  ( -0.000000000000000000, -0.000000000000000000, -1.000000000000000000 ) ) ;
#8270=AXIS2_PLACEMENT_3D ( 'NONE', #5261, #15860, #15524 ) ;
#8276=VERTEX_POINT ( 'NONE', #8957 ) ;
#8287=DIRECTION ( 'NONE',  ( -0.000000000000000000, 3.673940397442059868E-16, -1.000000000000000000 ) ) ;
#8289=AXIS2_PLACEMENT_3D ( 'NONE', #52140, #30232, #36945 ) ;
#8293=ORIENTED_EDGE ( 'NONE', *, *, #35773, .F. ) ;
#8302=EDGE_CURVE ( 'NONE', #27839, #28029, #18880, .T. ) ;
#8304=CARTESIAN_POINT ( 'NONE',  ( 1.866219381641426533, -9.417013320880872840, 455.0000000000000568 ) ) ;
#8306=AXIS2_PLACEMENT_3D ( 'NONE', #24029, #2124, #7068 ) ;
#8308=ADVANCED_FACE ( 'NONE', ( #62000 ), #40443, .F. ) ;
#8323=FACE_OUTER_BOUND ( 'NONE', #13520, .T. ) ;
#8336=EDGE_CURVE ( 'NONE', #45642, #19180, #8251, .T. ) ;
#8337=LINE ( 'NONE', #29561, #17081 ) ;
#8340=VERTEX_POINT ( 'NONE', #20616 ) ;
#8345=CARTESIAN_POINT ( 'NONE',  ( 7.826483450353380000, -11.78648345035339418, 195.0000000000000284 ) ) ;
#8361=EDGE_LOOP ( 'NONE', ( #31465, #63071, #326, #63301 ) ) ;
#8367=VECTOR ( 'NONE', #24985, 1000.000000000000000 ) ;
#8381=EDGE_CURVE ( 'NONE', #13045, #68965, #69061, .T. ) ;
#8392=LINE ( 'NONE', #18303, #17550 ) ;
#8396=VERTEX_POINT ( 'NONE', #15680 ) ;
#8398=CARTESIAN_POINT ( 'NONE',  ( -7.839518282750232991, -3.430747519065274531, 195.0000000000000284 ) ) ;
#8400=AXIS2_PLACEMENT_3D ( 'NONE', #41254, #67784, #4499 ) ;
#8401=VECTOR ( 'NONE', #44586, 1000.000000000000000 ) ;
#8407=VECTOR ( 'NONE', #350, 1000.000000000000000 ) ;
#8409=CIRCLE ( 'NONE', #47954, 1.399999999999998579 ) ;
#8415=VECTOR ( 'NONE', #20772, 1000.000000000000000 ) ;
#8416=DIRECTION ( 'NONE',  ( -0.000000000000000000, 3.673940397442059868E-16, -1.000000000000000000 ) ) ;
#8422=ORIENTED_EDGE ( 'NONE', *, *, #33110, .F. ) ;
#8427=ORIENTED_EDGE ( 'NONE', *, *, #20253, .T. ) ;
#8428=EDGE_CURVE ( 'NONE', #43460, #39509, #58108, .T. ) ;
#8429=DIRECTION ( 'NONE',  ( 1.000000000000000000, 0.000000000000000000, 0.000000000000000000 ) ) ;
#8434=PLANE ( 'NONE',  #15615 ) ;
#8447=ORIENTED_EDGE ( 'NONE', *, *, #36102, .F. ) ;
#8457=ORIENTED_EDGE ( 'NONE', *, *, #35319, .F. ) ;
#8459=VERTEX_POINT ( 'NONE', #37250 ) ;
#8460=CARTESIAN_POINT ( 'NONE',  ( -4.173516549646666185, 11.99351654964658920, 455.0000000000000568 ) ) ;
#8462=VERTEX_POINT ( 'NONE', #31940 ) ;
#8472=CARTESIAN_POINT ( 'NONE',  ( -7.793516549646712477, 11.11351654964660085, 195.0000000000000284 ) ) ;
#8475=ADVANCED_FACE ( 'NONE', ( #10710 ), #27334, .T. ) ;
#8478=EDGE_CURVE ( 'NONE', #68313, #1298, #26987, .T. ) ;
#8479=ADVANCED_FACE ( 'NONE', ( #11067 ), #53868, .F. ) ;
#8485=ORIENTED_EDGE ( 'NONE', *, *, #56455, .T. ) ;
#8491=CARTESIAN_POINT ( 'NONE',  ( -7.798499376344157241, -7.272650909786626983, 455.0000000000000568 ) ) ;
#8494=ORIENTED_EDGE ( 'NONE', *, *, #59179, .T. ) ;
#8498=VERTEX_POINT ( 'NONE', #12763 ) ;
#8499=PLANE ( 'NONE',  #52277 ) ;
#8511=VECTOR ( 'NONE', #68155, 1000.000000000000000 ) ;
#8522=DIRECTION ( 'NONE',  ( 1.000000000000000000, 0.000000000000000000, 0.000000000000000000 ) ) ;
#8532=CARTESIAN_POINT ( 'NONE',  ( -8.393516549646792058, -7.616533956692236096, 455.0000000000000568 ) ) ;
#8552=AXIS2_PLACEMENT_3D ( 'NONE', #10145, #53988, #58235 ) ;
#8557=DIRECTION ( 'NONE',  ( -1.000000000000000000, -0.000000000000000000, -0.000000000000000000 ) ) ;
#8559=ADVANCED_FACE ( 'NONE', ( #17749 ), #65502, .F. ) ;
#8560=CARTESIAN_POINT ( 'NONE',  ( -7.259684009079930611, 7.798499376343971612, 455.0000000000000568 ) ) ;
#8567=CARTESIAN_POINT ( 'NONE',  ( -10.91351654964666373, -2.706483450353290632, 195.0000000000000284 ) ) ;
#8575=ORIENTED_EDGE ( 'NONE', *, *, #50576, .F. ) ;
#8584=AXIS2_PLACEMENT_3D ( 'NONE', #57255, #53020, #8818 ) ;
#8603=LINE ( 'NONE', #25590, #57070 ) ;
#8614=VECTOR ( 'NONE', #43593, 1000.000000000000000 ) ;
#8616=CIRCLE ( 'NONE', #57172, 0.1999999999999987899 ) ;
#8621=VERTEX_POINT ( 'NONE', #39646 ) ;
#8624=CARTESIAN_POINT ( 'NONE',  ( 12.00648345035338060, -7.826483450353395988, 195.0000000000000284 ) ) ;
#8626=ADVANCED_FACE ( 'NONE', ( #34330 ), #7474, .F. ) ;
#8629=CARTESIAN_POINT ( 'NONE',  ( -7.259684009080030975, -7.811466277050769236, 455.0000000000000568 ) ) ;
#8631=EDGE_CURVE ( 'NONE', #4384, #62416, #11736, .T. ) ;
#8635=DIRECTION ( 'NONE',  ( 0.000000000000000000, 1.000000000000000000, 0.000000000000000000 ) ) ;
#8638=EDGE_CURVE ( 'NONE', #61820, #63196, #3584, .T. ) ;
#8639=CARTESIAN_POINT ( 'NONE',  ( -11.07551654964667520, 9.791916549646639822, 195.0000000000000284 ) ) ;
#8640=ADVANCED_FACE ( 'NONE', ( #39981 ), #2178, .F. ) ;
#8642=FACE_OUTER_BOUND ( 'NONE', #39029, .T. ) ;
#8646=CARTESIAN_POINT ( 'NONE',  ( 7.272650909786554152, 4.188533722949247640, 195.0000000000000284 ) ) ;
#8658=CARTESIAN_POINT ( 'NONE',  ( -2.893516549646675706, 10.91351654964657669, 455.0000000000000568 ) ) ;
#8669=VERTEX_POINT ( 'NONE', #8168 ) ;
#8672=CIRCLE ( 'NONE', #6407, 0.1999999999999987899 ) ;
#8675=CARTESIAN_POINT ( 'NONE',  ( 4.396432944014527777, -8.406483450353478659, 455.0000000000000568 ) ) ;
#8676=ORIENTED_EDGE ( 'NONE', *, *, #42746, .F. ) ;
#8680=EDGE_LOOP ( 'NONE', ( #33374, #4377, #6761, #10881 ) ) ;
#8682=ORIENTED_EDGE ( 'NONE', *, *, #54108, .F. ) ;
#8693=EDGE_LOOP ( 'NONE', ( #38367, #32430, #7376, #60810 ) ) ;
#8694=ORIENTED_EDGE ( 'NONE', *, *, #57895, .F. ) ;
#8696=ORIENTED_EDGE ( 'NONE', *, *, #48703, .F. ) ;
#8697=DIRECTION ( 'NONE',  ( -1.000000000000000000, 3.491481338843133355E-15, 1.836970198721036344E-16 ) ) ;
#8700=EDGE_CURVE ( 'NONE', #14045, #40926, #51672, .T. ) ;
#8703=AXIS2_PLACEMENT_3D ( 'NONE', #58668, #10222, #31802 ) ;
#8711=VECTOR ( 'NONE', #49771, 1000.000000000000000 ) ;
#8712=AXIS2_PLACEMENT_3D ( 'NONE', #9868, #30722, #41319 ) ;
#8715=CARTESIAN_POINT ( 'NONE',  ( -9.828310488886053520, 2.277516549646603661, 195.0000000000000284 ) ) ;
#8716=AXIS2_PLACEMENT_3D ( 'NONE', #57362, #8915, #45691 ) ;
#8722=VERTEX_POINT ( 'NONE', #45643 ) ;
#8724=CARTESIAN_POINT ( 'NONE',  ( 1.090483450353338268, -11.34648345035345329, 455.0000000000000568 ) ) ;
#8735=VECTOR ( 'NONE', #9876, 1000.000000000000000 ) ;
#8758=ORIENTED_EDGE ( 'NONE', *, *, #16929, .T. ) ;
#8761=LINE ( 'NONE', #3112, #24372 ) ;
#8768=VECTOR ( 'NONE', #32637, 1000.000000000000000 ) ;
#8773=CYLINDRICAL_SURFACE ( 'NONE', #62889, 0.2000000000000000944 ) ;
#8780=ORIENTED_EDGE ( 'NONE', *, *, #13491, .F. ) ;
#8781=ORIENTED_EDGE ( 'NONE', *, *, #20057, .T. ) ;
#8783=DIRECTION ( 'NONE',  ( 1.836970198721029934E-16, 1.836970198721010706E-16, -1.000000000000000000 ) ) ;
#8790=VERTEX_POINT ( 'NONE', #10282 ) ;
#8797=LINE ( 'NONE', #13742, #59070 ) ;
#8809=ORIENTED_EDGE ( 'NONE', *, *, #12390, .F. ) ;
#8810=LINE ( 'NONE', #66793, #64521 ) ;
#8817=CARTESIAN_POINT ( 'NONE',  ( -2.893516549646820035, -10.09643294401462654, 455.0000000000000568 ) ) ;
#8818=DIRECTION ( 'NONE',  ( -1.000000000000000000, 0.000000000000000000, 0.000000000000000000 ) ) ;
#8825=ORIENTED_EDGE ( 'NONE', *, *, #57844, .F. ) ;
#8830=DIRECTION ( 'NONE',  ( 1.000000000000000000, 0.000000000000000000, -0.000000000000000000 ) ) ;
#8831=PLANE ( 'NONE',  #14 ) ;
#8838=ORIENTED_EDGE ( 'NONE', *, *, #69950, .T. ) ;
#8851=FACE_OUTER_BOUND ( 'NONE', #69820, .T. ) ;
#8854=CARTESIAN_POINT ( 'NONE',  ( -11.77351654964674310, -4.406483450353321452, 455.0000000000000568 ) ) ;
#8858=DIRECTION ( 'NONE',  ( -4.336808689942025625E-15, -1.000000000000000000, 0.000000000000000000 ) ) ;
#8869=VECTOR ( 'NONE', #48993, 1000.000000000000000 ) ;
#8876=VERTEX_POINT ( 'NONE', #30800 ) ;
#8877=ADVANCED_FACE ( 'NONE', ( #68977 ), #20884, .F. ) ;
#8887=EDGE_CURVE ( 'NONE', #3656, #48554, #42456, .T. ) ;
#8901=DIRECTION ( 'NONE',  ( 0.000000000000000000, 0.000000000000000000, 1.000000000000000000 ) ) ;
#8903=CARTESIAN_POINT ( 'NONE',  ( -4.193516549646675529, 11.11351654964658664, 455.0000000000000568 ) ) ;
#8906=AXIS2_PLACEMENT_3D ( 'NONE', #15744, #59574, #59225 ) ;
#8913=ORIENTED_EDGE ( 'NONE', *, *, #59914, .T. ) ;
#8915=DIRECTION ( 'NONE',  ( 1.000000000000000000, -3.491481338843132961E-15, -1.836970198721036344E-16 ) ) ;
#8923=ORIENTED_EDGE ( 'NONE', *, *, #31560, .F. ) ;
#8925=ORIENTED_EDGE ( 'NONE', *, *, #3887, .F. ) ;
#8933=CARTESIAN_POINT ( 'NONE',  ( -9.942044687070527687, -2.765062094115999791, 195.0000000000000284 ) ) ;
#8938=EDGE_LOOP ( 'NONE', ( #23030, #26324, #43991, #48099 ) ) ;
#8951=ORIENTED_EDGE ( 'NONE', *, *, #47460, .T. ) ;
#8957=CARTESIAN_POINT ( 'NONE',  ( 11.12648345035336028, 9.093516549646610159, 195.0000000000000284 ) ) ;
#8961=ORIENTED_EDGE ( 'NONE', *, *, #59025, .F. ) ;
#8966=DIRECTION ( 'NONE',  ( -7.665540703601096574E-15, -1.000000000000000000, -3.673940397442059868E-16 ) ) ;
#8969=ORIENTED_EDGE ( 'NONE', *, *, #7425, .F. ) ;
#8971=LINE ( 'NONE', #8624, #17437 ) ;
#8977=ORIENTED_EDGE ( 'NONE', *, *, #18550, .F. ) ;
#8978=DIRECTION ( 'NONE',  ( -1.836970198721029934E-16, 1.836970198721036344E-16, -1.000000000000000000 ) ) ;
#8989=DIRECTION ( 'NONE',  ( 0.7071067811865401342, -0.7071067811865550112, -1.355854680848614216E-30 ) ) ;
#8998=DIRECTION ( 'NONE',  ( 0.000000000000000000, 1.000000000000000000, 0.000000000000000000 ) ) ;
#9001=DIRECTION ( 'NONE',  ( -1.000000000000000000, 0.000000000000000000, 0.000000000000000000 ) ) ;
#9003=EDGE_CURVE ( 'NONE', #56939, #67203, #17997, .T. ) ;
#9025=EDGE_CURVE ( 'NONE', #28622, #7275, #26316, .T. ) ;
#9029=VECTOR ( 'NONE', #17092, 1000.000000000000000 ) ;
#9034=ORIENTED_EDGE ( 'NONE', *, *, #21107, .F. ) ;
#9039=VECTOR ( 'NONE', #53586, 1000.000000000000000 ) ;
#9041=EDGE_CURVE ( 'NONE', #67467, #18151, #12332, .T. ) ;
#9054=VECTOR ( 'NONE', #49740, 1000.000000000000000 ) ;
#9055=EDGE_CURVE ( 'NONE', #40737, #5474, #8797, .T. ) ;
#9060=AXIS2_PLACEMENT_3D ( 'NONE', #24807, #41759, #29746 ) ;
#9073=DIRECTION ( 'NONE',  ( 0.000000000000000000, 0.000000000000000000, 1.000000000000000000 ) ) ;
#9080=CARTESIAN_POINT ( 'NONE',  ( 9.955011587777223170, 9.234937905883922937, 195.0000000000000284 ) ) ;
#9083=DIRECTION ( 'NONE',  ( 0.000000000000000000, 3.673940397442059868E-16, -1.000000000000000000 ) ) ;
#9084=PLANE ( 'NONE',  #28546 ) ;
#9088=LINE ( 'NONE', #69188, #16084 ) ;
#9099=EDGE_CURVE ( 'NONE', #68671, #67553, #52810, .T. ) ;
#9102=LINE ( 'NONE', #22673, #53492 ) ;
#9107=CARTESIAN_POINT ( 'NONE',  ( 4.186483450353422953, 11.77351654964658501, 455.0000000000000568 ) ) ;
#9111=CIRCLE ( 'NONE', #55398, 1.399999999999999245 ) ;
#9124=ORIENTED_EDGE ( 'NONE', *, *, #14564, .T. ) ;
#9126=PLANE ( 'NONE',  #5266 ) ;
#9135=VECTOR ( 'NONE', #40231, 1000.000000000000000 ) ;
#9137=CYLINDRICAL_SURFACE ( 'NONE', #22057, 0.2000000000000005107 ) ;
#9141=CARTESIAN_POINT ( 'NONE',  ( -5.993516549646711766, 5.993516549646603409, 455.0000000000000568 ) ) ;
#9147=ORIENTED_EDGE ( 'NONE', *, *, #69936, .F. ) ;
#9151=EDGE_CURVE ( 'NONE', #938, #51166, #2782, .T. ) ;
#9152=ORIENTED_EDGE ( 'NONE', *, *, #64526, .T. ) ;
#9155=AXIS2_PLACEMENT_3D ( 'NONE', #10533, #69237, #15838 ) ;
#9163=DIRECTION ( 'NONE',  ( 0.000000000000000000, 3.673940397442059868E-16, -1.000000000000000000 ) ) ;
#9164=CARTESIAN_POINT ( 'NONE',  ( 10.92648345035335922, 9.293516549646611224, 195.0000000000000284 ) ) ;
#9166=DIRECTION ( 'NONE',  ( -3.491481338843132961E-15, -1.000000000000000000, 0.000000000000000000 ) ) ;
#9167=EDGE_LOOP ( 'NONE', ( #38706, #55004, #19211, #10524 ) ) ;
#9179=LINE ( 'NONE', #25094, #63710 ) ;
#9189=EDGE_CURVE ( 'NONE', #47124, #67875, #42631, .T. ) ;
#9194=VERTEX_POINT ( 'NONE', #30006 ) ;
#9211=PLANE ( 'NONE',  #59800 ) ;
#9218=CARTESIAN_POINT ( 'NONE',  ( -7.813516549646711162, 11.77351654964660277, 455.0000000000000568 ) ) ;
#9221=DIRECTION ( 'NONE',  ( -0.7071067811865451302, 0.7071067811865500152, 2.597868168706485527E-16 ) ) ;
#9234=AXIS2_PLACEMENT_3D ( 'NONE', #48071, #26504, #5296 ) ;
#9252=DIRECTION ( 'NONE',  ( -1.047444401652939849E-14, -1.000000000000000000, 0.000000000000000000 ) ) ;
#9254=DIRECTION ( 'NONE',  ( -1.047444401652940007E-14, -1.000000000000000000, -1.836970198721029934E-16 ) ) ;
#9265=ORIENTED_EDGE ( 'NONE', *, *, #6011, .F. ) ;
#9269=ORIENTED_EDGE ( 'NONE', *, *, #9681, .T. ) ;
#9272=DIRECTION ( 'NONE',  ( -0.000000000000000000, -0.000000000000000000, -1.000000000000000000 ) ) ;
#9273=EDGE_LOOP ( 'NONE', ( #816, #59814, #8224, #56427 ) ) ;
#9274=DIRECTION ( 'NONE',  ( 1.836970198721029934E-16, 1.836970198721010706E-16, -1.000000000000000000 ) ) ;
#9277=CARTESIAN_POINT ( 'NONE',  ( 11.48848345035334617, -11.08848345035349148, 455.0000000000000568 ) ) ;
#9288=VECTOR ( 'NONE', #54775, 1000.000000000000000 ) ;
#9294=LINE ( 'NONE', #52432, #28989 ) ;
#9295=FACE_BOUND ( 'NONE', #19070, .T. ) ;
#9298=DIRECTION ( 'NONE',  ( 0.000000000000000000, -3.673940397442059868E-16, 1.000000000000000000 ) ) ;
#9303=ORIENTED_EDGE ( 'NONE', *, *, #12776, .T. ) ;
#9314=ORIENTED_EDGE ( 'NONE', *, *, #47587, .F. ) ;
#9315=VERTEX_POINT ( 'NONE', #31778 ) ;
#9320=CARTESIAN_POINT ( 'NONE',  ( 7.428221114745003462, -3.006483450353395259, 195.0000000000000284 ) ) ;
#9342=ORIENTED_EDGE ( 'NONE', *, *, #33177, .T. ) ;
#9365=FACE_OUTER_BOUND ( 'NONE', #26787, .T. ) ;
#9366=AXIS2_PLACEMENT_3D ( 'NONE', #63528, #59614, #68824 ) ;
#9367=VERTEX_POINT ( 'NONE', #11907 ) ;
#9373=DIRECTION ( 'NONE',  ( 0.000000000000000000, 1.000000000000000000, 0.000000000000000000 ) ) ;
#9377=AXIS2_PLACEMENT_3D ( 'NONE', #4965, #59399, #64701 ) ;
#9378=DIRECTION ( 'NONE',  ( -1.000000000000000000, -3.016910393003147986E-15, -0.000000000000000000 ) ) ;
#9379=EDGE_CURVE ( 'NONE', #15862, #20689, #62977, .T. ) ;
#9381=EDGE_LOOP ( 'NONE', ( #44418, #15834, #34747, #21670 ) ) ;
#9383=ORIENTED_EDGE ( 'NONE', *, *, #18158, .F. ) ;
#9388=LINE ( 'NONE', #25670, #13393 ) ;
#9410=ORIENTED_EDGE ( 'NONE', *, *, #7258, .F. ) ;
#9413=DIRECTION ( 'NONE',  ( -4.336808689942025625E-15, -1.000000000000000000, 0.000000000000000000 ) ) ;
#9423=LINE ( 'NONE', #57156, #14981 ) ;
#9436=EDGE_CURVE ( 'NONE', #68196, #46286, #5589, .T. ) ;
#9437=DIRECTION ( 'NONE',  ( 1.047444401652939849E-14, 1.000000000000000000, 1.836970198721029934E-16 ) ) ;
#9443=DIRECTION ( 'NONE',  ( 1.836970198721029934E-16, -1.836970198721036344E-16, 1.000000000000000000 ) ) ;
#9461=EDGE_CURVE ( 'NONE', #25131, #7744, #68806, .T. ) ;
#9464=LINE ( 'NONE', #64263, #2921 ) ;
#9472=CARTESIAN_POINT ( 'NONE',  ( -6.606374702650211539, -4.747751991980665665, 455.0000000000000568 ) ) ;
#9476=AXIS2_PLACEMENT_3D ( 'NONE', #23165, #8287, #61686 ) ;
#9482=VERTEX_POINT ( 'NONE', #14003 ) ;
#9485=ORIENTED_EDGE ( 'NONE', *, *, #32476, .T. ) ;
#9486=CARTESIAN_POINT ( 'NONE',  ( 7.272650909786598561, -4.201500623656122535, 455.0000000000000568 ) ) ;
#9500=CARTESIAN_POINT ( 'NONE',  ( -4.727349090213560423, -7.811466277050794993, 455.0000000000000568 ) ) ;
#9502=EDGE_CURVE ( 'NONE', #39173, #26484, #51139, .T. ) ;
#9507=CARTESIAN_POINT ( 'NONE',  ( -8.393516549646712122, 7.603567055985436696, 455.0000000000000568 ) ) ;
#9516=ADVANCED_FACE ( 'NONE', ( #2355 ), #56438, .F. ) ;
#9520=DIRECTION ( 'NONE',  ( 0.7671651518153043137, -0.6414496315691521344, 0.000000000000000000 ) ) ;
#9531=CARTESIAN_POINT ( 'NONE',  ( 4.406483450353340103, -11.32648345035338089, 195.0000000000000284 ) ) ;
#9534=ORIENTED_EDGE ( 'NONE', *, *, #22320, .F. ) ;
#9535=ADVANCED_FACE ( 'NONE', ( #40527 ), #19311, .F. ) ;
#9541=CYLINDRICAL_SURFACE ( 'NONE', #25244, 2.204799999999997429 ) ;
#9546=ORIENTED_EDGE ( 'NONE', *, *, #53805, .F. ) ;
#9547=VERTEX_POINT ( 'NONE', #130 ) ;
#9550=VECTOR ( 'NONE', #7436, 1000.000000000000000 ) ;
#9552=CARTESIAN_POINT ( 'NONE',  ( 6.006483450353401921, 5.993516549646582092, 455.0000000000000568 ) ) ;
#9557=CARTESIAN_POINT ( 'NONE',  ( 4.396432944014526889, -8.606483450353477949, 455.0000000000000568 ) ) ;
#9563=LINE ( 'NONE', #32535, #59567 ) ;
#9572=FACE_OUTER_BOUND ( 'NONE', #39219, .T. ) ;
#9575=LINE ( 'NONE', #31149, #35557 ) ;
#9593=VERTEX_POINT ( 'NONE', #470 ) ;
#9595=VERTEX_POINT ( 'NONE', #37260 ) ;
#9604=CARTESIAN_POINT ( 'NONE',  ( 10.20488345035338007, -11.48848345035339769, 195.0000000000000284 ) ) ;
#9607=EDGE_CURVE ( 'NONE', #50982, #11259, #48910, .T. ) ;
#9609=VERTEX_POINT ( 'NONE', #31951 ) ;
#9612=EDGE_LOOP ( 'NONE', ( #34316, #68815, #51307, #55290 ) ) ;
#9613=CARTESIAN_POINT ( 'NONE',  ( 11.78648345035340839, 7.813516549646560172, 455.0000000000000568 ) ) ;
#9616=EDGE_CURVE ( 'NONE', #43669, #47649, #63097, .T. ) ;
#9618=VECTOR ( 'NONE', #58209, 1000.000000000000000 ) ;
#9622=DIRECTION ( 'NONE',  ( 1.000000000000000000, 0.000000000000000000, 0.000000000000000000 ) ) ;
#9628=CARTESIAN_POINT ( 'NONE',  ( -4.734785091274035018, -6.619341603356897252, 455.0000000000000568 ) ) ;
#9629=ORIENTED_EDGE ( 'NONE', *, *, #43323, .T. ) ;
#9632=CARTESIAN_POINT ( 'NONE',  ( -9.942044687070573872, -2.765062094116047309, 455.0000000000000568 ) ) ;
#9633=LINE ( 'NONE', #3271, #50293 ) ;
#9637=LINE ( 'NONE', #42508, #8039 ) ;
#9639=ORIENTED_EDGE ( 'NONE', *, *, #69950, .F. ) ;
#9641=ORIENTED_EDGE ( 'NONE', *, *, #45495, .F. ) ;
#9643=EDGE_CURVE ( 'NONE', #62060, #27405, #66467, .T. ) ;
#9644=CIRCLE ( 'NONE', #45757, 0.5999999999999998668 ) ;
#9647=LINE ( 'NONE', #69746, #51821 ) ;
#9648=DIRECTION ( 'NONE',  ( 1.836970198721029934E-16, 1.836970198721010706E-16, -1.000000000000000000 ) ) ;
#9652=VECTOR ( 'NONE', #68531, 1000.000000000000000 ) ;
#9658=EDGE_CURVE ( 'NONE', #20610, #37207, #26644, .T. ) ;
#9662=ORIENTED_EDGE ( 'NONE', *, *, #60407, .T. ) ;
#9671=DIRECTION ( 'NONE',  ( 0.6414496315691494699, 0.7671651518153064231, 2.818519042764025305E-16 ) ) ;
#9676=ORIENTED_EDGE ( 'NONE', *, *, #63743, .T. ) ;
#9678=CARTESIAN_POINT ( 'NONE',  ( -8.393516549646744096, -4.396432944014549093, 455.0000000000000568 ) ) ;
#9681=EDGE_CURVE ( 'NONE', #46263, #11892, #53186, .T. ) ;
#9689=VECTOR ( 'NONE', #49464, 1000.000000000000000 ) ;
#9691=PLANE ( 'NONE',  #42502 ) ;
#9692=DIRECTION ( 'NONE',  ( -0.000000000000000000, 3.673940397442059868E-16, -1.000000000000000000 ) ) ;
#9693=CIRCLE ( 'NONE', #15342, 2.204799999999997429 ) ;
#9694=EDGE_CURVE ( 'NONE', #3757, #46850, #20980, .T. ) ;
#9700=DIRECTION ( 'NONE',  ( 1.883404846338789915E-14, 1.000000000000000000, 1.836970198721045218E-16 ) ) ;
#9713=LINE ( 'NONE', #20309, #4502 ) ;
#9714=ORIENTED_EDGE ( 'NONE', *, *, #25668, .T. ) ;
#9717=DIRECTION ( 'NONE',  ( 0.000000000000000000, 1.000000000000000000, 0.000000000000000000 ) ) ;
#9725=PLANE ( 'NONE',  #28300 ) ;
#9726=ORIENTED_EDGE ( 'NONE', *, *, #46045, .T. ) ;
#9728=ORIENTED_EDGE ( 'NONE', *, *, #44487, .F. ) ;
#9740=VERTEX_POINT ( 'NONE', #60875 ) ;
#9749=AXIS2_PLACEMENT_3D ( 'NONE', #49497, #1732, #66442 ) ;
#9750=ORIENTED_EDGE ( 'NONE', *, *, #14123, .T. ) ;
#9751=ORIENTED_EDGE ( 'NONE', *, *, #55708, .F. ) ;
#9752=DIRECTION ( 'NONE',  ( -1.000000000000000000, 1.952517519553884087E-14, 0.000000000000000000 ) ) ;
#9755=AXIS2_PLACEMENT_3D ( 'NONE', #43559, #21655, #48877 ) ;
#9757=ORIENTED_EDGE ( 'NONE', *, *, #7717, .T. ) ;
#9759=ORIENTED_EDGE ( 'NONE', *, *, #49640, .F. ) ;
#9760=ORIENTED_EDGE ( 'NONE', *, *, #1190, .T. ) ;
#9780=DIRECTION ( 'NONE',  ( -1.000000000000000000, 1.047444401652940007E-14, -1.836970198721010706E-16 ) ) ;
#9784=DIRECTION ( 'NONE',  ( 0.4999999999999785727, -0.8660254037844510311, 0.000000000000000000 ) ) ;
#9789=AXIS2_PLACEMENT_3D ( 'NONE', #44186, #23323, #54817 ) ;
#9790=AXIS2_PLACEMENT_3D ( 'NONE', #42806, #48820, #10288 ) ;
#9799=VECTOR ( 'NONE', #65290, 1000.000000000000114 ) ;
#9801=EDGE_LOOP ( 'NONE', ( #43853, #68201, #12579, #38778 ) ) ;
#9811=CARTESIAN_POINT ( 'NONE',  ( -11.11351654964671098, 4.193516549646605363, 195.0000000000000284 ) ) ;
#9822=CYLINDRICAL_SURFACE ( 'NONE', #67575, 0.1999999999999992339 ) ;
#9826=VERTEX_POINT ( 'NONE', #17759 ) ;
#9830=CARTESIAN_POINT ( 'NONE',  ( -11.07551654964667520, 9.791916549646639822, 455.0000000000000568 ) ) ;
#9838=EDGE_CURVE ( 'NONE', #59053, #21746, #18089, .T. ) ;
#9843=ORIENTED_EDGE ( 'NONE', *, *, #59125, .F. ) ;
#9844=VECTOR ( 'NONE', #17240, 1000.000000000000000 ) ;
#9863=CYLINDRICAL_SURFACE ( 'NONE', #14344, 0.5999999999999989786 ) ;
#9865=ORIENTED_EDGE ( 'NONE', *, *, #25883, .F. ) ;
#9866=VECTOR ( 'NONE', #10212, 1000.000000000000000 ) ;
#9868=CARTESIAN_POINT ( 'NONE',  ( -11.99351654964679526, -7.826483450353362237, 455.0000000000000568 ) ) ;
#9875=LINE ( 'NONE', #47689, #42023 ) ;
#9876=DIRECTION ( 'NONE',  ( -0.000000000000000000, 1.000000000000000000, -0.000000000000000000 ) ) ;
#9878=CYLINDRICAL_SURFACE ( 'NONE', #39805, 1.399999999999998579 ) ;
#9883=ADVANCED_FACE ( 'NONE', ( #67596 ), #14543, .F. ) ;
#9884=DIRECTION ( 'NONE',  ( 0.000000000000000000, 3.673940397442059868E-16, -1.000000000000000000 ) ) ;
#9905=PRODUCT_DEFINITION_FORMATION_WITH_SPECIFIED_SOURCE ( 'ANY', '', #44233, .NOT_KNOWN. ) ;
#9906=ORIENTED_EDGE ( 'NONE', *, *, #20888, .F. ) ;
#9913=CARTESIAN_POINT ( 'NONE',  ( 1.866219381641426533, -9.417013320880872840, 455.0000000000000568 ) ) ;
#9919=EDGE_CURVE ( 'NONE', #12232, #27294, #58115, .T. ) ;
#9923=LINE ( 'NONE', #62958, #54679 ) ;
#9926=DIRECTION ( 'NONE',  ( 0.000000000000000000, 0.000000000000000000, 1.000000000000000000 ) ) ;
#9933=ORIENTED_EDGE ( 'NONE', *, *, #17695, .T. ) ;
#9939=EDGE_CURVE ( 'NONE', #64793, #31474, #67753, .T. ) ;
#9945=EDGE_CURVE ( 'NONE', #20689, #62061, #68291, .T. ) ;
#9951=VECTOR ( 'NONE', #48426, 1000.000000000000000 ) ;
#9970=ORIENTED_EDGE ( 'NONE', *, *, #10236, .T. ) ;
#9972=DIRECTION ( 'NONE',  ( -1.000000000000000000, 1.047444401652940007E-14, -1.836970198721010706E-16 ) ) ;
#9983=ORIENTED_EDGE ( 'NONE', *, *, #62573, .T. ) ;
#9989=CARTESIAN_POINT ( 'NONE',  ( -10.91351654964670992, -2.706483450353338593, 455.0000000000000568 ) ) ;
#9994=ORIENTED_EDGE ( 'NONE', *, *, #10025, .F. ) ;
#10002=CARTESIAN_POINT ( 'NONE',  ( 4.255011587777269177, 8.452095193409277840, 455.0000000000000568 ) ) ;
#10003=EDGE_CURVE ( 'NONE', #47329, #59237, #15888, .T. ) ;
#10011=ORIENTED_EDGE ( 'NONE', *, *, #31938, .F. ) ;
#10012=CARTESIAN_POINT ( 'NONE',  ( 11.78648345035337819, -4.406483450353490205, 455.0000000000000568 ) ) ;
#10013=EDGE_CURVE ( 'NONE', #26698, #52241, #9111, .T. ) ;
#10014=DIRECTION ( 'NONE',  ( -0.8660254037844510311, -0.4999999999999785727, 0.000000000000000000 ) ) ;
#10019=EDGE_LOOP ( 'NONE', ( #984, #51020, #29032, #6159 ) ) ;
#10024=ORIENTED_EDGE ( 'NONE', *, *, #63066, .F. ) ;
#10025=EDGE_CURVE ( 'NONE', #35382, #69020, #64396, .T. ) ;
#10028=DIRECTION ( 'NONE',  ( -1.000000000000000000, 0.000000000000000000, 0.000000000000000000 ) ) ;
#10031=DIRECTION ( 'NONE',  ( -0.000000000000000000, -0.000000000000000000, -1.000000000000000000 ) ) ;
#10052=DIRECTION ( 'NONE',  ( 0.000000000000000000, 1.000000000000000000, 0.000000000000000000 ) ) ;
#10064=EDGE_CURVE ( 'NONE', #31340, #20149, #48473, .T. ) ;
#10073=PLANE ( 'NONE',  #15901 ) ;
#10082=DIRECTION ( 'NONE',  ( -0.7071067811865475727, -0.7071067811865475727, 0.000000000000000000 ) ) ;
#10083=DIRECTION ( 'NONE',  ( -1.836970198721029934E-16, 1.836970198721036344E-16, -1.000000000000000000 ) ) ;
#10097=ORIENTED_EDGE ( 'NONE', *, *, #52881, .T. ) ;
#10107=DIRECTION ( 'NONE',  ( -1.000000000000000000, 0.000000000000000000, 0.000000000000000000 ) ) ;
#10108=VERTEX_POINT ( 'NONE', #69337 ) ;
#10109=DIRECTION ( 'NONE',  ( -1.000000000000000000, 7.304098846218132892E-15, -0.000000000000000000 ) ) ;
#10110=CARTESIAN_POINT ( 'NONE',  ( 9.955011587777235604, -9.247904806590801385, 455.0000000000000568 ) ) ;
#10113=ORIENTED_EDGE ( 'NONE', *, *, #58936, .T. ) ;
#10121=CARTESIAN_POINT ( 'NONE',  ( -10.91351654964680584, -9.306483450353375986, 455.0000000000000568 ) ) ;
#10125=DIRECTION ( 'NONE',  ( -1.000000000000000000, 0.000000000000000000, 0.000000000000000000 ) ) ;
#10131=ORIENTED_EDGE ( 'NONE', *, *, #54335, .T. ) ;
#10142=ORIENTED_EDGE ( 'NONE', *, *, #44083, .F. ) ;
#10145=CARTESIAN_POINT ( 'NONE',  ( 9.841277389592701041, 2.277516549646538824, 455.0000000000000568 ) ) ;
#10153=LINE ( 'NONE', #31735, #24407 ) ;
#10156=AXIS2_PLACEMENT_3D ( 'NONE', #4735, #5784, #63787 ) ;
#10159=DIRECTION ( 'NONE',  ( 1.000000000000000000, 0.000000000000000000, 0.000000000000000000 ) ) ;
#10163=EDGE_CURVE ( 'NONE', #33821, #13319, #2004, .T. ) ;
#10165=ADVANCED_FACE ( 'NONE', ( #65430 ), #61132, .T. ) ;
#10166=CARTESIAN_POINT ( 'NONE',  ( 11.32648345035338089, 4.393516549646522051, 455.0000000000000568 ) ) ;
#10167=FACE_OUTER_BOUND ( 'NONE', #66950, .T. ) ;
#10168=DIRECTION ( 'NONE',  ( 1.836970198721029934E-16, -1.836970198721036344E-16, 1.000000000000000000 ) ) ;
#10176=VERTEX_POINT ( 'NONE', #44526 ) ;
#10188=DIRECTION ( 'NONE',  ( 1.836970198721029934E-16, -1.836970198721036344E-16, 1.000000000000000000 ) ) ;
#10197=CARTESIAN_POINT ( 'NONE',  ( -11.99351654964671354, 4.173516549646604901, 195.0000000000000284 ) ) ;
#10212=DIRECTION ( 'NONE',  ( 1.836970198721029934E-16, 1.836970198721010706E-16, -1.000000000000000000 ) ) ;
#10221=ORIENTED_EDGE ( 'NONE', *, *, #60089, .T. ) ;
#10222=DIRECTION ( 'NONE',  ( -0.000000000000000000, 3.673940397442059868E-16, -1.000000000000000000 ) ) ;
#10230=CARTESIAN_POINT ( 'NONE',  ( 4.206483450353421638, 11.11351654964658486, 455.0000000000000568 ) ) ;
#10236=EDGE_CURVE ( 'NONE', #54829, #26529, #60454, .T. ) ;
#10243=PLANE ( 'NONE',  #35195 ) ;
#10244=ORIENTED_EDGE ( 'NONE', *, *, #16062, .T. ) ;
#10267=PLANE ( 'NONE',  #31101 ) ;
#10281=EDGE_LOOP ( 'NONE', ( #34845, #65716, #17903, #8151 ) ) ;
#10282=CARTESIAN_POINT ( 'NONE',  ( -11.77351654964674665, -7.826483450353317828, 195.0000000000000284 ) ) ;
#10284=CARTESIAN_POINT ( 'NONE',  ( -10.19191654964671301, 11.07551654964660415, 455.0000000000000568 ) ) ;
#10288=DIRECTION ( 'NONE',  ( -1.000000000000000000, 8.540177112501197482E-15, 0.000000000000000000 ) ) ;
#10297=DIRECTION ( 'NONE',  ( -0.000000000000000000, -0.000000000000000000, -1.000000000000000000 ) ) ;
#10303=LINE ( 'NONE', #9604, #66671 ) ;
#10309=ORIENTED_EDGE ( 'NONE', *, *, #69352, .T. ) ;
#10317=ORIENTED_EDGE ( 'NONE', *, *, #68111, .F. ) ;
#10319=CARTESIAN_POINT ( 'NONE',  ( 8.406483450353404052, 6.331612867284015955, 455.0000000000000568 ) ) ;
#10322=VERTEX_POINT ( 'NONE', #41324 ) ;
#10323=CIRCLE ( 'NONE', #5834, 0.1999999999999987899 ) ;
#10333=EDGE_CURVE ( 'NONE', #20182, #24541, #8810, .T. ) ;
#10346=DIRECTION ( 'NONE',  ( 0.000000000000000000, 3.673940397442059868E-16, -1.000000000000000000 ) ) ;
#10355=VECTOR ( 'NONE', #2484, 1000.000000000000000 ) ;
#10358=EDGE_CURVE ( 'NONE', #24992, #68360, #46280, .T. ) ;
#10360=VECTOR ( 'NONE', #52069, 1000.000000000000000 ) ;
#10362=CARTESIAN_POINT ( 'NONE',  ( 2.706483450353419862, 10.91351654964658735, 455.0000000000000568 ) ) ;
#10368=CARTESIAN_POINT ( 'NONE',  ( 2.906483450353372078, 10.91351654964663531, 195.0000000000000284 ) ) ;
#10374=VERTEX_POINT ( 'NONE', #30376 ) ;
#10376=VECTOR ( 'NONE', #64900, 1000.000000000000000 ) ;
#10377=LINE ( 'NONE', #14625, #64121 ) ;
#10382=DIRECTION ( 'NONE',  ( 0.000000000000000000, 1.000000000000000000, 0.000000000000000000 ) ) ;
#10383=PLANE ( 'NONE',  #11431 ) ;
#10388=ORIENTED_EDGE ( 'NONE', *, *, #67041, .T. ) ;
#10389=CARTESIAN_POINT ( 'NONE',  ( 1.690483450353415629, 9.828310488885938057, 455.0000000000000568 ) ) ;
#10401=ORIENTED_EDGE ( 'NONE', *, *, #35369, .T. ) ;
#10406=LINE ( 'NONE', #31981, #31619 ) ;
#10408=FACE_OUTER_BOUND ( 'NONE', #28695, .T. ) ;
#10418=CARTESIAN_POINT ( 'NONE',  ( -2.752095193409509033, -9.955011587777317317, 455.0000000000000568 ) ) ;
#10422=VERTEX_POINT ( 'NONE', #69947 ) ;
#10430=EDGE_LOOP ( 'NONE', ( #42821, #38084, #65221, #43435 ) ) ;
#10433=EDGE_CURVE ( 'NONE', #48685, #19113, #4907, .T. ) ;
#10440=CARTESIAN_POINT ( 'NONE',  ( 9.106483450353380249, -11.12648345035339048, 195.0000000000000284 ) ) ;
#10449=CARTESIAN_POINT ( 'NONE',  ( -10.19191654964680360, -9.804883450353337082, 195.0000000000000284 ) ) ;
#10455=VECTOR ( 'NONE', #23600, 1000.000000000000114 ) ;
#10466=EDGE_CURVE ( 'NONE', #67402, #43025, #42726, .T. ) ;
#10468=CYLINDRICAL_SURFACE ( 'NONE', #13270, 2.204799999999997429 ) ;
#10476=CARTESIAN_POINT ( 'NONE',  ( -8.393516549646712122, 7.603567055985436696, 455.0000000000000568 ) ) ;
#10485=DIRECTION ( 'NONE',  ( 1.836970198721029934E-16, 1.836970198721010706E-16, -1.000000000000000000 ) ) ;
#10486=VERTEX_POINT ( 'NONE', #16205 ) ;
#10487=DIRECTION ( 'NONE',  ( 0.6414496315691494699, 0.7671651518153064231, 2.818519042764025305E-16 ) ) ;
#10495=ORIENTED_EDGE ( 'NONE', *, *, #43961, .T. ) ;
#10504=CARTESIAN_POINT ( 'NONE',  ( -9.828310488886053520, 1.677516549646603794, 455.0000000000000568 ) ) ;
#10515=ORIENTED_EDGE ( 'NONE', *, *, #62383, .F. ) ;
#10517=ADVANCED_FACE ( 'NONE', ( #64641 ), #4223, .F. ) ;
#10519=EDGE_CURVE ( 'NONE', #63196, #13233, #62523, .T. ) ;
#10521=LINE ( 'NONE', #63216, #48007 ) ;
#10523=VECTOR ( 'NONE', #67975, 1000.000000000000000 ) ;
#10524=ORIENTED_EDGE ( 'NONE', *, *, #31643, .T. ) ;
#10525=EDGE_CURVE ( 'NONE', #64753, #20149, #20811, .T. ) ;
#10527=EDGE_LOOP ( 'NONE', ( #60564, #17112, #37313, #29831 ) ) ;
#10528=CARTESIAN_POINT ( 'NONE',  ( -4.188533722949335569, 7.259684009079808931, 195.0000000000000284 ) ) ;
#10533=CARTESIAN_POINT ( 'NONE',  ( -4.188533722949417282, -4.740315990920197287, 455.0000000000000568 ) ) ;
#10541=DIRECTION ( 'NONE',  ( 1.836970198721029934E-16, 1.836970198721010706E-16, -1.000000000000000000 ) ) ;
#10546=LINE ( 'NONE', #37431, #69261 ) ;
#10549=AXIS2_PLACEMENT_3D ( 'NONE', #49194, #69105, #9717 ) ;
#10553=VECTOR ( 'NONE', #35459, 1000.000000000000000 ) ;
#10555=CARTESIAN_POINT ( 'NONE',  ( 3.606483450353358045, 7.415254214038261793, 195.0000000000000284 ) ) ;
#10557=DIRECTION ( 'NONE',  ( 1.836970198721029934E-16, -1.836970198721036344E-16, 1.000000000000000000 ) ) ;
#10559=FACE_OUTER_BOUND ( 'NONE', #43967, .T. ) ;
#10590=ORIENTED_EDGE ( 'NONE', *, *, #25741, .F. ) ;
#10594=CARTESIAN_POINT ( 'NONE',  ( -10.19191654964686578, -11.08848345035334759, 455.0000000000000568 ) ) ;
#10597=AXIS2_PLACEMENT_3D ( 'NONE', #24947, #51820, #36977 ) ;
#10616=CIRCLE ( 'NONE', #55777, 2.204799999999999205 ) ;
#10618=CARTESIAN_POINT ( 'NONE',  ( -4.393516549646671265, 11.31351654964658771, 195.0000000000000284 ) ) ;
#10624=FACE_OUTER_BOUND ( 'NONE', #28505, .T. ) ;
#10625=ORIENTED_EDGE ( 'NONE', *, *, #42876, .F. ) ;
#10628=DIRECTION ( 'NONE',  ( 0.000000000000000000, 3.673940397442059868E-16, -1.000000000000000000 ) ) ;
#10630=DIRECTION ( 'NONE',  ( 1.836970198721029934E-16, 1.836970198721010706E-16, -1.000000000000000000 ) ) ;
#10643=VERTEX_POINT ( 'NONE', #642 ) ;
#10646=VECTOR ( 'NONE', #26151, 1000.000000000000000 ) ;
#10648=DIRECTION ( 'NONE',  ( 1.000000000000000000, -8.728482790395504563E-15, 0.000000000000000000 ) ) ;
#10653=AXIS2_PLACEMENT_3D ( 'NONE', #9552, #41362, #36415 ) ;
#10661=DIRECTION ( 'NONE',  ( 1.836970198721029934E-16, 1.836970198721010706E-16, -1.000000000000000000 ) ) ;
#10666=EDGE_CURVE ( 'NONE', #12808, #31731, #999, .T. ) ;
#10674=CARTESIAN_POINT ( 'NONE',  ( -7.798499376344067535, 7.259684009079840017, 455.0000000000000568 ) ) ;
#10675=CARTESIAN_POINT ( 'NONE',  ( -7.415254214038336400, 3.593516549646602609, 455.0000000000000568 ) ) ;
#10679=EDGE_LOOP ( 'NONE', ( #43393, #12772, #10728, #59459 ) ) ;
#10690=EDGE_LOOP ( 'NONE', ( #26392, #41397, #3266, #60551 ) ) ;
#10691=VECTOR ( 'NONE', #23952, 1000.000000000000000 ) ;
#10701=ORIENTED_EDGE ( 'NONE', *, *, #41865, .T. ) ;
#10703=CARTESIAN_POINT ( 'NONE',  ( 10.09643294401454661, -9.106483450353492159, 455.0000000000000568 ) ) ;
#10706=DIRECTION ( 'NONE',  ( -1.000000000000000000, 0.000000000000000000, 0.000000000000000000 ) ) ;
#10707=CARTESIAN_POINT ( 'NONE',  ( -11.33351654964671162, 1.077516549646603483, 195.0000000000000284 ) ) ;
#10708=ORIENTED_EDGE ( 'NONE', *, *, #24528, .F. ) ;
#10710=FACE_OUTER_BOUND ( 'NONE', #57371, .T. ) ;
#10718=DIRECTION ( 'NONE',  ( 0.000000000000000000, 3.673940397442059868E-16, -1.000000000000000000 ) ) ;
#10722=DIRECTION ( 'NONE',  ( 8.673617379884087537E-15, 1.000000000000000000, 0.000000000000000000 ) ) ;
#10728=ORIENTED_EDGE ( 'NONE', *, *, #49200, .T. ) ;
#10733=EDGE_CURVE ( 'NONE', #1298, #48685, #46538, .T. ) ;
#10739=EDGE_CURVE ( 'NONE', #14886, #58272, #67063, .T. ) ;
#10741=EDGE_CURVE ( 'NONE', #24680, #50893, #13670, .T. ) ;
#10748=CARTESIAN_POINT ( 'NONE',  ( -7.593516549646711411, 11.77351654964660277, 455.0000000000000568 ) ) ;
#10750=VECTOR ( 'NONE', #4875, 1000.000000000000000 ) ;
#10756=DIRECTION ( 'NONE',  ( -0.000000000000000000, 3.673940397442059868E-16, -1.000000000000000000 ) ) ;
#10761=DIRECTION ( 'NONE',  ( -1.836970198721029934E-16, 1.836970198721036344E-16, -1.000000000000000000 ) ) ;
#10762=FACE_OUTER_BOUND ( 'NONE', #31458, .T. ) ;
#10778=FACE_OUTER_BOUND ( 'NONE', #53669, .T. ) ;
#10785=VECTOR ( 'NONE', #52949, 1000.000000000000000 ) ;
#10800=VECTOR ( 'NONE', #40682, 1000.000000000000114 ) ;
#10803=CYLINDRICAL_SURFACE ( 'NONE', #16511, 0.4000000000000010214 ) ;
#10807=CARTESIAN_POINT ( 'NONE',  ( 9.804883450353379715, -10.20488345035352928, 455.0000000000000568 ) ) ;
#10813=AXIS2_PLACEMENT_3D ( 'NONE', #67527, #23672, #61144 ) ;
#10816=LINE ( 'NONE', #16124, #2064 ) ;
#10824=ORIENTED_EDGE ( 'NONE', *, *, #3970, .T. ) ;
#10844=DIRECTION ( 'NONE',  ( -1.836970198721029934E-16, 1.836970198721036344E-16, -1.000000000000000000 ) ) ;
#10849=VECTOR ( 'NONE', #45275, 1000.000000000000000 ) ;
#10853=AXIS2_PLACEMENT_3D ( 'NONE', #30191, #66617, #40075 ) ;
#10856=ORIENTED_EDGE ( 'NONE', *, *, #61496, .F. ) ;
#10863=CIRCLE ( 'NONE', #28914, 0.3999999999999993006 ) ;
#10867=EDGE_CURVE ( 'NONE', #40219, #24424, #31071, .T. ) ;
#10869=CARTESIAN_POINT ( 'NONE',  ( -7.744988412222897800, -8.465062094116051483, 195.0000000000000284 ) ) ;
#10872=EDGE_CURVE ( 'NONE', #354, #39516, #49143, .T. ) ;
#10876=ORIENTED_EDGE ( 'NONE', *, *, #38863, .F. ) ;
#10879=CARTESIAN_POINT ( 'NONE',  ( -7.593516549646711411, 11.77351654964660277, 455.0000000000000568 ) ) ;
#10881=ORIENTED_EDGE ( 'NONE', *, *, #5070, .T. ) ;
#10882=DIRECTION ( 'NONE',  ( 3.540573132209560831E-15, 1.000000000000000000, 0.000000000000000000 ) ) ;
#10886=ORIENTED_EDGE ( 'NONE', *, *, #49405, .T. ) ;
#10888=VECTOR ( 'NONE', #21727, 1000.000000000000000 ) ;
#10891=CARTESIAN_POINT ( 'NONE',  ( -11.11351654964679270, -7.806483450353373321, 455.0000000000000568 ) ) ;
#10892=VECTOR ( 'NONE', #44884, 1000.000000000000000 ) ;
#10894=EDGE_LOOP ( 'NONE', ( #12623, #69695, #36653, #7245 ) ) ;
#10898=DIRECTION ( 'NONE',  ( 2.309061475090597584E-14, 1.000000000000000000, 1.836970198721053107E-16 ) ) ;
#10903=CIRCLE ( 'NONE', #39107, 0.3999999999999993006 ) ;
#10913=CARTESIAN_POINT ( 'NONE',  ( 8.406483450353379183, -5.668387132716048882, 455.0000000000000568 ) ) ;
#10914=CARTESIAN_POINT ( 'NONE',  ( 9.247904806590725002, 9.942044687070426434, 455.0000000000000568 ) ) ;
#10919=CARTESIAN_POINT ( 'NONE',  ( -10.08346604330797547, -9.306483450353381315, 455.0000000000000568 ) ) ;
#10943=CARTESIAN_POINT ( 'NONE',  ( -9.234937905884020637, 9.942044687070460185, 455.0000000000000568 ) ) ;
#10948=ORIENTED_EDGE ( 'NONE', *, *, #51853, .F. ) ;
#10950=ADVANCED_FACE ( 'NONE', ( #26044 ), #25335, .T. ) ;
#10961=ORIENTED_EDGE ( 'NONE', *, *, #67549, .T. ) ;
#10969=EDGE_CURVE ( 'NONE', #30449, #6262, #29871, .T. ) ;
#10973=EDGE_CURVE ( 'NONE', #48678, #54850, #8409, .T. ) ;
#10976=CARTESIAN_POINT ( 'NONE',  ( -7.839518282750262301, 3.417780618358531530, 455.0000000000000568 ) ) ;
#10992=DIRECTION ( 'NONE',  ( 2.135044278125299371E-15, 1.000000000000000000, 0.000000000000000000 ) ) ;
#11003=VECTOR ( 'NONE', #51352, 1000.000000000000000 ) ;
#11006=EDGE_CURVE ( 'NONE', #50458, #46020, #57391, .T. ) ;
#11013=DIRECTION ( 'NONE',  ( -0.000000000000000000, 3.673940397442059868E-16, -1.000000000000000000 ) ) ;
#11016=ORIENTED_EDGE ( 'NONE', *, *, #59598, .F. ) ;
#11025=CARTESIAN_POINT ( 'NONE',  ( -10.73351654964664981, -1.690483450353293948, 195.0000000000000284 ) ) ;
#11027=DIRECTION ( 'NONE',  ( -0.6414496315691494699, 0.7671651518153064231, 0.000000000000000000 ) ) ;
#11034=DIRECTION ( 'NONE',  ( 1.000000000000000000, 0.000000000000000000, 0.000000000000000000 ) ) ;
#11036=FACE_OUTER_BOUND ( 'NONE', #25111, .T. ) ;
#11038=DIRECTION ( 'NONE',  ( -0.000000000000000000, -0.000000000000000000, -1.000000000000000000 ) ) ;
#11040=VERTEX_POINT ( 'NONE', #19910 ) ;
#11045=AXIS2_PLACEMENT_3D ( 'NONE', #38465, #64988, #28522 ) ;
#11050=AXIS2_PLACEMENT_3D ( 'NONE', #25603, #47167, #47503 ) ;
#11056=EDGE_CURVE ( 'NONE', #39844, #35101, #52092, .T. ) ;
#11059=VECTOR ( 'NONE', #49941, 1000.000000000000000 ) ;
#11060=VECTOR ( 'NONE', #19708, 1000.000000000000000 ) ;
#11067=FACE_OUTER_BOUND ( 'NONE', #18579, .T. ) ;
#11069=CARTESIAN_POINT ( 'NONE',  ( 6.006483450353379716, -6.006483450353394815, 195.0000000000000284 ) ) ;
#11079=DIRECTION ( 'NONE',  ( 0.000000000000000000, 0.000000000000000000, 1.000000000000000000 ) ) ;
#11081=FACE_OUTER_BOUND ( 'NONE', #17674, .T. ) ;
#11082=ORIENTED_EDGE ( 'NONE', *, *, #64107, .F. ) ;
#11086=LINE ( 'NONE', #17080, #30054 ) ;
#11087=VECTOR ( 'NONE', #65790, 1000.000000000000000 ) ;
#11089=FACE_OUTER_BOUND ( 'NONE', #27635, .T. ) ;
#11094=DIRECTION ( 'NONE',  ( 3.491481338843133355E-15, 1.000000000000000000, 1.836970198721029934E-16 ) ) ;
#11106=CARTESIAN_POINT ( 'NONE',  ( 12.00648345035338060, -7.826483450353491023, 455.0000000000000568 ) ) ;
#11115=LINE ( 'NONE', #16428, #10888 ) ;
#11120=ORIENTED_EDGE ( 'NONE', *, *, #57355, .F. ) ;
#11122=ADVANCED_FACE ( 'NONE', ( #16353 ), #20605, .F. ) ;
#11130=DIRECTION ( 'NONE',  ( -1.000000000000000000, 3.491481338843132961E-15, 0.000000000000000000 ) ) ;
#11133=ORIENTED_EDGE ( 'NONE', *, *, #57437, .F. ) ;
#11140=VERTEX_POINT ( 'NONE', #30873 ) ;
#11145=LINE ( 'NONE', #17839, #23409 ) ;
#11147=VECTOR ( 'NONE', #13588, 1000.000000000000000 ) ;
#11150=ORIENTED_EDGE ( 'NONE', *, *, #53046, .F. ) ;
#11152=AXIS2_PLACEMENT_3D ( 'NONE', #6303, #54746, #60729 ) ;
#11164=ADVANCED_FACE ( 'NONE', ( #25934 ), #14963, .F. ) ;
#11168=DIRECTION ( 'NONE',  ( -0.000000000000000000, -0.000000000000000000, -1.000000000000000000 ) ) ;
#11172=VERTEX_POINT ( 'NONE', #69400 ) ;
#11175=CARTESIAN_POINT ( 'NONE',  ( 10.20488345035338007, -11.08848345035339733, 195.0000000000000284 ) ) ;
#11183=CIRCLE ( 'NONE', #64252, 0.1999999999999987899 ) ;
#11184=ORIENTED_EDGE ( 'NONE', *, *, #55372, .F. ) ;
#11192=EDGE_CURVE ( 'NONE', #38308, #35023, #69764, .T. ) ;
#11194=EDGE_CURVE ( 'NONE', #7925, #9482, #21318, .T. ) ;
#11195=ADVANCED_FACE ( 'NONE', ( #53852 ), #44950, .F. ) ;
#11200=ORIENTED_EDGE ( 'NONE', *, *, #43061, .F. ) ;
#11208=ORIENTED_EDGE ( 'NONE', *, *, #26741, .T. ) ;
#11215=VERTEX_POINT ( 'NONE', #5755 ) ;
#11223=LINE ( 'NONE', #66359, #21578 ) ;
#11231=CIRCLE ( 'NONE', #24768, 0.2000000000000005107 ) ;
#11237=DIRECTION ( 'NONE',  ( 1.836970198721029934E-16, 1.836970198721010706E-16, -1.000000000000000000 ) ) ;
#11239=CARTESIAN_POINT ( 'NONE',  ( -4.734785091274032354, -5.393625297349961656, 455.0000000000000568 ) ) ;
#11243=CARTESIAN_POINT ( 'NONE',  ( -5.993516549646711766, 3.593516549646603497, 455.0000000000000568 ) ) ;
#11252=EDGE_CURVE ( 'NONE', #27223, #41334, #1817, .T. ) ;
#11253=AXIS2_PLACEMENT_3D ( 'NONE', #23842, #28787, #45399 ) ;
#11257=ADVANCED_FACE ( 'NONE', ( #449 ), #28337, .T. ) ;
#11259=VERTEX_POINT ( 'NONE', #27321 ) ;
#11261=CARTESIAN_POINT ( 'NONE',  ( -9.791916549646712653, 11.07551654964660415, 455.0000000000000568 ) ) ;
#11262=FACE_OUTER_BOUND ( 'NONE', #19134, .T. ) ;
#11272=ORIENTED_EDGE ( 'NONE', *, *, #26395, .T. ) ;
#11273=CARTESIAN_POINT ( 'NONE',  ( -4.173516549646666185, 11.99351654964658920, 195.0000000000000284 ) ) ;
#11275=DIRECTION ( 'NONE',  ( 8.673617379884051249E-15, 1.000000000000000000, 0.000000000000000000 ) ) ;
#11276=DIRECTION ( 'NONE',  ( -0.000000000000000000, 3.673940397442059868E-16, -1.000000000000000000 ) ) ;
#11279=PLANE ( 'NONE',  #2354 ) ;
#11294=CARTESIAN_POINT ( 'NONE',  ( -7.813516549646839948, -12.00648345035340903, 455.0000000000000568 ) ) ;
#11297=VECTOR ( 'NONE', #7686, 1000.000000000000000 ) ;
#11299=VECTOR ( 'NONE', #57753, 1000.000000000000000 ) ;
#11305=ADVANCED_FACE ( 'NONE', ( #23033 ), #38952, .F. ) ;
#11313=DIRECTION ( 'NONE',  ( 8.673617379884087537E-15, 1.000000000000000000, 0.000000000000000000 ) ) ;
#11331=CARTESIAN_POINT ( 'NONE',  ( 7.852485183456924034, 3.417780618358489786, 455.0000000000000568 ) ) ;
#11356=CARTESIAN_POINT ( 'NONE',  ( -5.993516549646711766, 5.993516549646603409, 455.0000000000000568 ) ) ;
#11361=ORIENTED_EDGE ( 'NONE', *, *, #8887, .T. ) ;
#11367=DIRECTION ( 'NONE',  ( -0.000000000000000000, 3.673940397442059868E-16, -1.000000000000000000 ) ) ;
#11373=CARTESIAN_POINT ( 'NONE',  ( 6.006483450353401921, 5.993516549646582092, 455.0000000000000568 ) ) ;
#11377=CARTESIAN_POINT ( 'NONE',  ( 2.765062094116041980, -9.955011587777228499, 195.0000000000000284 ) ) ;
#11378=DIRECTION ( 'NONE',  ( 0.000000000000000000, 1.000000000000000000, 0.000000000000000000 ) ) ;
#11382=ORIENTED_EDGE ( 'NONE', *, *, #9461, .F. ) ;
#11393=EDGE_CURVE ( 'NONE', #65422, #56927, #3506, .T. ) ;
#11394=AXIS2_PLACEMENT_3D ( 'NONE', #12023, #34280, #49531 ) ;
#11396=DIRECTION ( 'NONE',  ( -1.000000000000000000, 0.000000000000000000, 0.000000000000000000 ) ) ;
#11401=VECTOR ( 'NONE', #21373, 1000.000000000000000 ) ;
#11415=DIRECTION ( 'NONE',  ( 0.000000000000000000, 1.000000000000000000, 0.000000000000000000 ) ) ;
#11422=CARTESIAN_POINT ( 'NONE',  ( 12.00648345035338060, -7.826483450353491023, 455.0000000000000568 ) ) ;
#11423=VECTOR ( 'NONE', #36992, 1000.000000000000114 ) ;
#11425=DIRECTION ( 'NONE',  ( -1.000000000000000000, 0.000000000000000000, 0.000000000000000000 ) ) ;
#11427=EDGE_LOOP ( 'NONE', ( #49255, #48462, #27236, #58028 ) ) ;
#11428=ORIENTED_EDGE ( 'NONE', *, *, #13777, .F. ) ;
#11431=AXIS2_PLACEMENT_3D ( 'NONE', #27347, #54222, #27684 ) ;
#11452=CARTESIAN_POINT ( 'NONE',  ( 11.12648345035340647, 7.793516549646564151, 455.0000000000000568 ) ) ;
#11457=DIRECTION ( 'NONE',  ( -0.000000000000000000, -0.000000000000000000, -1.000000000000000000 ) ) ;
#11462=CARTESIAN_POINT ( 'NONE',  ( 11.78648345035337996, 4.393516549646516722, 455.0000000000000568 ) ) ;
#11469=FACE_OUTER_BOUND ( 'NONE', #14526, .T. ) ;
#11474=ORIENTED_EDGE ( 'NONE', *, *, #17896, .T. ) ;
#11477=CARTESIAN_POINT ( 'NONE',  ( -4.173516549646837603, -11.78648345035344214, 455.0000000000000568 ) ) ;
#11492=CARTESIAN_POINT ( 'NONE',  ( 11.08848345035341865, 11.07551654964652776, 455.0000000000000568 ) ) ;
#11493=ORIENTED_EDGE ( 'NONE', *, *, #8042, .F. ) ;
#11494=LINE ( 'NONE', #44023, #5376 ) ;
#11495=VECTOR ( 'NONE', #59, 1000.000000000000000 ) ;
#11513=EDGE_CURVE ( 'NONE', #37177, #65043, #58652, .T. ) ;
#11517=DIRECTION ( 'NONE',  ( 1.836970198721029934E-16, 1.836970198721010706E-16, -1.000000000000000000 ) ) ;
#11528=CARTESIAN_POINT ( 'NONE',  ( 7.272650909786602114, 4.188533722949199678, 455.0000000000000568 ) ) ;
#11533=ORIENTED_EDGE ( 'NONE', *, *, #40175, .T. ) ;
#11537=DIRECTION ( 'NONE',  ( 1.000000000000000000, 0.000000000000000000, -0.000000000000000000 ) ) ;
#11543=DIRECTION ( 'NONE',  ( 0.000000000000000000, 1.000000000000000000, 0.000000000000000000 ) ) ;
#11555=DIRECTION ( 'NONE',  ( -0.000000000000000000, 3.673940397442059868E-16, -1.000000000000000000 ) ) ;
#11558=ORIENTED_EDGE ( 'NONE', *, *, #25907, .F. ) ;
#11576=CARTESIAN_POINT ( 'NONE',  ( 11.08848345035341687, 10.19191654964656379, 455.0000000000000568 ) ) ;
#11577=DIRECTION ( 'NONE',  ( 1.214636490590110272E-14, 1.000000000000000000, 1.836970198721032892E-16 ) ) ;
#11580=DIRECTION ( 'NONE',  ( 8.673617379884030739E-15, 1.000000000000000000, 0.000000000000000000 ) ) ;
#11582=CARTESIAN_POINT ( 'NONE',  ( 10.74648345035334529, 1.077516549646528876, 455.0000000000000568 ) ) ;
#11587=DIRECTION ( 'NONE',  ( 0.000000000000000000, 1.000000000000000000, 0.000000000000000000 ) ) ;
#11601=EDGE_CURVE ( 'NONE', #2273, #3545, #57938, .T. ) ;
#11611=CARTESIAN_POINT ( 'NONE',  ( 7.272650909786597673, 7.798499376343980494, 195.0000000000000284 ) ) ;
#11613=VERTEX_POINT ( 'NONE', #50715 ) ;
#11614=VERTEX_POINT ( 'NONE', #7581 ) ;
#11620=CARTESIAN_POINT ( 'NONE',  ( 4.740315990920131561, -4.201500623656145628, 455.0000000000000568 ) ) ;
#11625=DIRECTION ( 'NONE',  ( -4.336808689942006692E-15, -1.000000000000000000, 0.000000000000000000 ) ) ;
#11636=VECTOR ( 'NONE', #13101, 1000.000000000000000 ) ;
#11644=CARTESIAN_POINT ( 'NONE',  ( 4.206483450353343478, -11.12648345035347575, 455.0000000000000568 ) ) ;
#11649=AXIS2_PLACEMENT_3D ( 'NONE', #24646, #46195, #67769 ) ;
#11651=FACE_OUTER_BOUND ( 'NONE', #43404, .T. ) ;
#11657=DIRECTION ( 'NONE',  ( 1.000000000000000000, 0.000000000000000000, 0.000000000000000000 ) ) ;
#11662=VECTOR ( 'NONE', #60143, 1000.000000000000000 ) ;
#11674=ORIENTED_EDGE ( 'NONE', *, *, #39777, .T. ) ;
#11679=ORIENTED_EDGE ( 'NONE', *, *, #13200, .F. ) ;
#11680=DIRECTION ( 'NONE',  ( -1.836970198721029934E-16, -1.836970198721010706E-16, 1.000000000000000000 ) ) ;
#11689=AXIS2_PLACEMENT_3D ( 'NONE', #4330, #21281, #37538 ) ;
#11708=ORIENTED_EDGE ( 'NONE', *, *, #29301, .F. ) ;
#11709=DIRECTION ( 'NONE',  ( 1.000000000000000000, 0.000000000000000000, 0.000000000000000000 ) ) ;
#11713=DIRECTION ( 'NONE',  ( -1.000000000000000000, 1.671920889371702854E-15, 6.142537696789956391E-31 ) ) ;
#11716=CARTESIAN_POINT ( 'NONE',  ( -11.07551654964667520, 11.07551654964660237, 195.0000000000000284 ) ) ;
#11728=ADVANCED_FACE ( 'NONE', ( #34096 ), #52123, .F. ) ;
#11729=CYLINDRICAL_SURFACE ( 'NONE', #45564, 0.1999999999999987899 ) ;
#11736=LINE ( 'NONE', #13832, #47760 ) ;
#11738=ADVANCED_FACE ( 'NONE', ( #69085 ), #36203, .F. ) ;
#11752=DIRECTION ( 'NONE',  ( -1.000000000000000000, 0.000000000000000000, 0.000000000000000000 ) ) ;
#11753=CARTESIAN_POINT ( 'NONE',  ( -11.31351654964670850, 7.793516549646603231, 455.0000000000000568 ) ) ;
#11760=CARTESIAN_POINT ( 'NONE',  ( 9.417013320880792904, -1.866219381641561759, 455.0000000000000568 ) ) ;
#11763=CIRCLE ( 'NONE', #1613, 2.204799999999998761 ) ;
#11764=CARTESIAN_POINT ( 'NONE',  ( 2.765062094116059743, 9.942044687070495712, 195.0000000000000284 ) ) ;
#11782=DIRECTION ( 'NONE',  ( -4.121462285523434458E-16, -1.000000000000000000, 0.000000000000000000 ) ) ;
#11783=CARTESIAN_POINT ( 'NONE',  ( 2.706483450353370124, 10.08346604330780671, 195.0000000000000284 ) ) ;
#11784=DIRECTION ( 'NONE',  ( 0.000000000000000000, 1.000000000000000000, 0.000000000000000000 ) ) ;
#11786=LINE ( 'NONE', #32338, #61041 ) ;
#11794=DIRECTION ( 'NONE',  ( 0.7671651518152962090, 0.6414496315691619044, 2.356647714346269254E-16 ) ) ;
#11797=VECTOR ( 'NONE', #33344, 999.9999999999998863 ) ;
#11805=EDGE_CURVE ( 'NONE', #65042, #64711, #30556, .T. ) ;
#11813=VERTEX_POINT ( 'NONE', #68035 ) ;
#11814=VERTEX_POINT ( 'NONE', #14643 ) ;
#11815=ORIENTED_EDGE ( 'NONE', *, *, #8381, .T. ) ;
#11820=DIRECTION ( 'NONE',  ( 1.836970198721029934E-16, 1.836970198721010706E-16, -1.000000000000000000 ) ) ;
#11822=DIRECTION ( 'NONE',  ( -0.7071067811865446862, 0.7071067811865503483, 0.000000000000000000 ) ) ;
#11823=DIRECTION ( 'NONE',  ( 0.000000000000000000, 3.673940397442059868E-16, -1.000000000000000000 ) ) ;
#11842=CARTESIAN_POINT ( 'NONE',  ( 6.006483450353401921, 5.993516549646582092, 455.0000000000000568 ) ) ;
#11854=ADVANCED_FACE ( 'NONE', ( #19243 ), #4046, .F. ) ;
#11856=EDGE_CURVE ( 'NONE', #60174, #56003, #35491, .T. ) ;
#11859=CARTESIAN_POINT ( 'NONE',  ( -11.31351654964670850, 4.193516549646605363, 195.0000000000000284 ) ) ;
#11862=CARTESIAN_POINT ( 'NONE',  ( -7.813516549646711162, 11.99351654964660341, 455.0000000000000568 ) ) ;
#11866=LINE ( 'NONE', #43720, #49753 ) ;
#11871=DIRECTION ( 'NONE',  ( -0.7071067811865530128, -0.7071067811865421326, 0.000000000000000000 ) ) ;
#11872=VECTOR ( 'NONE', #40030, 1000.000000000000000 ) ;
#11873=EDGE_LOOP ( 'NONE', ( #52247, #4941, #63653, #25312 ) ) ;
#11879=ORIENTED_EDGE ( 'NONE', *, *, #34876, .F. ) ;
#11880=DIRECTION ( 'NONE',  ( 8.612436249475772606E-15, 1.000000000000000000, 0.000000000000000000 ) ) ;
#11881=CARTESIAN_POINT ( 'NONE',  ( -11.99351654964671354, 4.173516549646604901, 455.0000000000000568 ) ) ;
#11882=LINE ( 'NONE', #27473, #57331 ) ;
#11883=VECTOR ( 'NONE', #11820, 1000.000000000000000 ) ;
#11885=VECTOR ( 'NONE', #31419, 1000.000000000000000 ) ;
#11889=CARTESIAN_POINT ( 'NONE',  ( 4.406483450353373854, 11.77351654964663119, 195.0000000000000284 ) ) ;
#11892=VERTEX_POINT ( 'NONE', #4740 ) ;
#11897=VERTEX_POINT ( 'NONE', #53535 ) ;
#11900=CARTESIAN_POINT ( 'NONE',  ( 11.12648345035337627, -9.106483450353398013, 195.0000000000000284 ) ) ;
#11907=CARTESIAN_POINT ( 'NONE',  ( 9.955011587777271131, 9.234937905883876752, 455.0000000000000568 ) ) ;
#11916=VERTEX_POINT ( 'NONE', #31961 ) ;
#11918=PLANE ( 'NONE',  #28475 ) ;
#11921=CARTESIAN_POINT ( 'NONE',  ( -6.331612867284154511, 8.393516549646601987, 455.0000000000000568 ) ) ;
#11926=CARTESIAN_POINT ( 'NONE',  ( -9.942044687070668019, -9.247904806590694804, 455.0000000000000568 ) ) ;
#11933=AXIS2_PLACEMENT_3D ( 'NONE', #12997, #23967, #45525 ) ;
#11941=CARTESIAN_POINT ( 'NONE',  ( 9.955011587777271131, 9.234937905883876752, 455.0000000000000568 ) ) ;
#11942=VECTOR ( 'NONE', #26722, 1000.000000000000000 ) ;
#11944=CARTESIAN_POINT ( 'NONE',  ( 4.201500623656003519, -7.272650909786698037, 455.0000000000000568 ) ) ;
#11948=ORIENTED_EDGE ( 'NONE', *, *, #13761, .F. ) ;
#11949=CARTESIAN_POINT ( 'NONE',  ( 1.090483450353418426, 10.73351654964659829, 455.0000000000000568 ) ) ;
#11950=ORIENTED_EDGE ( 'NONE', *, *, #18982, .T. ) ;
#11961=PRODUCT_DEFINITION_CONTEXT ( 'detailed design', #12833, 'design' ) ;
#11965=EDGE_CURVE ( 'NONE', #67463, #40219, #5790, .T. ) ;
#11969=CARTESIAN_POINT ( 'NONE',  ( -11.11351654964671098, 7.793516549646603231, 195.0000000000000284 ) ) ;
#11971=ORIENTED_EDGE ( 'NONE', *, *, #53810, .F. ) ;
#11975=EDGE_CURVE ( 'NONE', #48554, #69020, #52455, .T. ) ;
#11978=CYLINDRICAL_SURFACE ( 'NONE', #50254, 0.3999999999999993006 ) ;
#11979=AXIS2_PLACEMENT_3D ( 'NONE', #28031, #16378, #43933 ) ;
#12001=CARTESIAN_POINT ( 'NONE',  ( -9.293516549646771097, -10.09643294401451108, 195.0000000000000284 ) ) ;
#12002=ORIENTED_EDGE ( 'NONE', *, *, #60929, .T. ) ;
#12006=CARTESIAN_POINT ( 'NONE',  ( 6.006483450353379716, -6.006483450353394815, 195.0000000000000284 ) ) ;
#12016=EDGE_LOOP ( 'NONE', ( #49529, #65574, #33024, #41497 ) ) ;
#12023=CARTESIAN_POINT ( 'NONE',  ( -5.993516549646776603, -6.006483450353426790, 455.0000000000000568 ) ) ;
#12033=VECTOR ( 'NONE', #45782, 1000.000000000000000 ) ;
#12034=AXIS2_PLACEMENT_3D ( 'NONE', #27577, #38209, #59060 ) ;
#12035=CARTESIAN_POINT ( 'NONE',  ( 11.78648345035337819, -7.826483450353395988, 195.0000000000000284 ) ) ;
#12037=AXIS2_PLACEMENT_3D ( 'NONE', #23546, #18234, #35541 ) ;
#12044=DIRECTION ( 'NONE',  ( -1.260948829465470062E-14, -1.000000000000000000, -1.836970198721033878E-16 ) ) ;
#12049=EDGE_CURVE ( 'NONE', #36255, #37762, #55602, .T. ) ;
#12051=ORIENTED_EDGE ( 'NONE', *, *, #3869, .F. ) ;
#12058=CARTESIAN_POINT ( 'NONE',  ( -11.11351654964674118, -4.206483450353336373, 455.0000000000000568 ) ) ;
#12064=CARTESIAN_POINT ( 'NONE',  ( -11.77351654964670935, 7.813516549646603693, 455.0000000000000568 ) ) ;
#12065=LINE ( 'NONE', #66505, #22164 ) ;
#12071=ORIENTED_EDGE ( 'NONE', *, *, #26359, .T. ) ;
#12073=EDGE_CURVE ( 'NONE', #30271, #22374, #28374, .T. ) ;
#12085=CIRCLE ( 'NONE', #15498, 1.399999999999999245 ) ;
#12096=LINE ( 'NONE', #61210, #13699 ) ;
#12108=CARTESIAN_POINT ( 'NONE',  ( -7.798499376344067535, 7.259684009079840017, 455.0000000000000568 ) ) ;
#12119=CARTESIAN_POINT ( 'NONE',  ( -11.77351654964679284, -7.826483450353365789, 455.0000000000000568 ) ) ;
#12125=EDGE_CURVE ( 'NONE', #16233, #29457, #49939, .T. ) ;
#12131=EDGE_CURVE ( 'NONE', #30539, #16082, #1176, .T. ) ;
#12132=CARTESIAN_POINT ( 'NONE',  ( 11.19368345035336709, -12.00648345035339659, 195.0000000000000284 ) ) ;
#12136=ADVANCED_FACE ( 'NONE', ( #1499 ), #23068, .F. ) ;
#12139=DIRECTION ( 'NONE',  ( 0.000000000000000000, 1.000000000000000000, 0.000000000000000000 ) ) ;
#12167=ORIENTED_EDGE ( 'NONE', *, *, #54589, .T. ) ;
#12169=EDGE_LOOP ( 'NONE', ( #13914, #54255, #65125, #54923 ) ) ;
#12174=PLANE ( 'NONE',  #14239 ) ;
#12181=CARTESIAN_POINT ( 'NONE',  ( -11.07551654964678711, -11.48848345035328933, 195.0000000000000284 ) ) ;
#12195=LINE ( 'NONE', #50379, #68145 ) ;
#12197=CYLINDRICAL_SURFACE ( 'NONE', #41229, 0.1999999999999987899 ) ;
#12209=LINE ( 'NONE', #39092, #7936 ) ;
#12210=ADVANCED_FACE ( 'NONE', ( #31189 ), #36121, .F. ) ;
#12212=LINE ( 'NONE', #59631, #39045 ) ;
#12213=CARTESIAN_POINT ( 'NONE',  ( 2.906483450353343656, -10.92648345035336810, 195.0000000000000284 ) ) ;
#12214=EDGE_CURVE ( 'NONE', #20060, #32671, #16403, .T. ) ;
#12215=DIRECTION ( 'NONE',  ( -1.836970198721029934E-16, 1.836970198721036344E-16, -1.000000000000000000 ) ) ;
#12229=CIRCLE ( 'NONE', #66450, 0.1999999999999987899 ) ;
#12230=DIRECTION ( 'NONE',  ( 1.836970198721029934E-16, 1.836970198721010706E-16, -1.000000000000000000 ) ) ;
#12232=VERTEX_POINT ( 'NONE', #51702 ) ;
#12241=CARTESIAN_POINT ( 'NONE',  ( -7.798499376344157241, -7.272650909786626983, 455.0000000000000568 ) ) ;
#12254=PLANE ( 'NONE',  #42799 ) ;
#12259=ORIENTED_EDGE ( 'NONE', *, *, #62299, .T. ) ;
#12266=ORIENTED_EDGE ( 'NONE', *, *, #23176, .F. ) ;
#12269=DIRECTION ( 'NONE',  ( -1.836970198721029934E-16, 1.836970198721036344E-16, -1.000000000000000000 ) ) ;
#12271=LINE ( 'NONE', #38147, #12985 ) ;
#12273=CARTESIAN_POINT ( 'NONE',  ( -6.606374702650169795, 4.734785091273855606, 455.0000000000000568 ) ) ;
#12277=LINE ( 'NONE', #39507, #38848 ) ;
#12279=ORIENTED_EDGE ( 'NONE', *, *, #2696, .F. ) ;
#12280=CYLINDRICAL_SURFACE ( 'NONE', #54892, 1.399999999999998579 ) ;
#12282=AXIS2_PLACEMENT_3D ( 'NONE', #7431, #2133, #61885 ) ;
#12296=CARTESIAN_POINT ( 'NONE',  ( -11.18071654964669648, 11.18071654964658812, 455.0000000000000568 ) ) ;
#12304=ORIENTED_EDGE ( 'NONE', *, *, #32892, .T. ) ;
#12313=ORIENTED_EDGE ( 'NONE', *, *, #3145, .F. ) ;
#12323=CARTESIAN_POINT ( 'NONE',  ( -7.593516549646711411, 11.31351654964660014, 455.0000000000000568 ) ) ;
#12324=ORIENTED_EDGE ( 'NONE', *, *, #59021, .F. ) ;
#12332=LINE ( 'NONE', #7038, #12754 ) ;
#12338=DIRECTION ( 'NONE',  ( 0.000000000000000000, -3.673940397442059868E-16, 1.000000000000000000 ) ) ;
#12341=VERTEX_POINT ( 'NONE', #20562 ) ;
#12343=AXIS2_PLACEMENT_3D ( 'NONE', #48359, #21825, #32091 ) ;
#12357=FACE_OUTER_BOUND ( 'NONE', #67318, .T. ) ;
#12359=DIRECTION ( 'NONE',  ( 0.4999999999999755196, -0.8660254037844526964, 0.000000000000000000 ) ) ;
#12360=CARTESIAN_POINT ( 'NONE',  ( 2.906483450353372522, 11.11351654964663638, 195.0000000000000284 ) ) ;
#12362=LINE ( 'NONE', #39595, #18756 ) ;
#12366=CIRCLE ( 'NONE', #48546, 0.1999999999999987899 ) ;
#12367=AXIS2_PLACEMENT_3D ( 'NONE', #13286, #67028, #23196 ) ;
#12373=FACE_OUTER_BOUND ( 'NONE', #56033, .T. ) ;
#12386=EDGE_CURVE ( 'NONE', #41004, #38597, #37533, .T. ) ;
#12390=EDGE_CURVE ( 'NONE', #61399, #11259, #59091, .T. ) ;
#12392=CIRCLE ( 'NONE', #51940, 0.2000000000000005107 ) ;
#12394=LINE ( 'NONE', #67562, #27515 ) ;
#12398=CIRCLE ( 'NONE', #37326, 0.1999999999999987899 ) ;
#12404=VERTEX_POINT ( 'NONE', #53110 ) ;
#12406=CARTESIAN_POINT ( 'NONE',  ( 8.406483450353379183, -5.668387132716048882, 455.0000000000000568 ) ) ;
#12408=AXIS2_PLACEMENT_3D ( 'NONE', #18958, #52541, #40517 ) ;
#12415=EDGE_CURVE ( 'NONE', #43836, #34688, #7336, .T. ) ;
#12424=LINE ( 'NONE', #19139, #40251 ) ;
#12432=DIRECTION ( 'NONE',  ( 1.000000000000000000, -1.356437060717834379E-15, -1.836970198721032646E-16 ) ) ;
#12434=AXIS2_PLACEMENT_3D ( 'NONE', #39181, #44130, #1689 ) ;
#12438=ORIENTED_EDGE ( 'NONE', *, *, #5492, .T. ) ;
#12439=PLANE ( 'NONE',  #48453 ) ;
#12440=CARTESIAN_POINT ( 'NONE',  ( -11.31351654964678843, -7.606483450353371367, 455.0000000000000568 ) ) ;
#12441=EDGE_LOOP ( 'NONE', ( #14083, #46950, #61343, #60943 ) ) ;
#12447=EDGE_CURVE ( 'NONE', #24763, #24032, #17332, .T. ) ;
#12460=CARTESIAN_POINT ( 'NONE',  ( -7.603567055985545942, 8.393516549646601987, 455.0000000000000568 ) ) ;
#12465=VERTEX_POINT ( 'NONE', #60467 ) ;
#12470=ORIENTED_EDGE ( 'NONE', *, *, #162, .T. ) ;
#12477=VECTOR ( 'NONE', #68901, 1000.000000000000000 ) ;
#12480=EDGE_CURVE ( 'NONE', #44460, #43261, #49179, .T. ) ;
#12483=CARTESIAN_POINT ( 'NONE',  ( -10.08346604330787777, 9.093516549646603053, 195.0000000000000284 ) ) ;
#12489=CARTESIAN_POINT ( 'NONE',  ( 7.272650909786602114, 4.188533722949199678, 455.0000000000000568 ) ) ;
#12495=LINE ( 'NONE', #43986, #53620 ) ;
#12498=CARTESIAN_POINT ( 'NONE',  ( -11.18071654964682615, -12.00648345035337350, 455.0000000000000568 ) ) ;
#12503=AXIS2_PLACEMENT_3D ( 'NONE', #42036, #21514, #69954 ) ;
#12505=ORIENTED_EDGE ( 'NONE', *, *, #1300, .T. ) ;
#12506=ORIENTED_EDGE ( 'NONE', *, *, #39906, .F. ) ;
#12523=CARTESIAN_POINT ( 'NONE',  ( 11.08848345035342042, 11.47551654964652812, 455.0000000000000568 ) ) ;
#12526=VECTOR ( 'NONE', #69245, 1000.000000000000000 ) ;
#12533=AXIS2_PLACEMENT_3D ( 'NONE', #62462, #34550, #18285 ) ;
#12539=VECTOR ( 'NONE', #38434, 1000.000000000000000 ) ;
#12544=ORIENTED_EDGE ( 'NONE', *, *, #38807, .F. ) ;
#12550=CARTESIAN_POINT ( 'NONE',  ( -7.593516549646838421, -11.78648345035340839, 455.0000000000000568 ) ) ;
#12551=ORIENTED_EDGE ( 'NONE', *, *, #25118, .F. ) ;
#12552=FACE_OUTER_BOUND ( 'NONE', #65866, .T. ) ;
#12556=CARTESIAN_POINT ( 'NONE',  ( 7.616533956692197016, 8.393516549646621527, 195.0000000000000284 ) ) ;
#12559=VERTEX_POINT ( 'NONE', #67529 ) ;
#12564=ORIENTED_EDGE ( 'NONE', *, *, #50774, .F. ) ;
#12568=EDGE_LOOP ( 'NONE', ( #12962, #46430, #65470, #34328 ) ) ;
#12570=CARTESIAN_POINT ( 'NONE',  ( 2.290483450353367534, 9.828310488885982465, 195.0000000000000284 ) ) ;
#12572=PLANE ( 'NONE',  #12367 ) ;
#12578=DIRECTION ( 'NONE',  ( -0.7671651518152895477, 0.6414496315691698980, -2.309356642088442522E-17 ) ) ;
#12579=ORIENTED_EDGE ( 'NONE', *, *, #48950, .F. ) ;
#12580=EDGE_LOOP ( 'NONE', ( #30065, #27149, #9383, #8485 ) ) ;
#12585=DIRECTION ( 'NONE',  ( -6.508391731846281342E-15, -1.000000000000000000, -1.836970198721024757E-16 ) ) ;
#12594=VECTOR ( 'NONE', #14120, 1000.000000000000000 ) ;
#12598=DIRECTION ( 'NONE',  ( 0.7671651518152895477, -0.6414496315691698980, 0.000000000000000000 ) ) ;
#12611=CYLINDRICAL_SURFACE ( 'NONE', #129, 0.3999999999999993006 ) ;
#12612=LINE ( 'NONE', #60723, #66972 ) ;
#12623=ORIENTED_EDGE ( 'NONE', *, *, #45719, .T. ) ;
#12626=ORIENTED_EDGE ( 'NONE', *, *, #42234, .T. ) ;
#12628=VECTOR ( 'NONE', #11871, 1000.000000000000000 ) ;
#12631=LINE ( 'NONE', #11944, #10455 ) ;
#12634=ORIENTED_EDGE ( 'NONE', *, *, #48084, .T. ) ;
#12641=LINE ( 'NONE', #56833, #66402 ) ;
#12645=DIRECTION ( 'NONE',  ( 1.047444401652939849E-14, 1.000000000000000000, 1.836970198721029934E-16 ) ) ;
#12658=CARTESIAN_POINT ( 'NONE',  ( -11.31351654964670850, 4.193516549646605363, 455.0000000000000568 ) ) ;
#12659=ORIENTED_EDGE ( 'NONE', *, *, #48414, .F. ) ;
#12665=PLANE ( 'NONE',  #68285 ) ;
#12677=VERTEX_POINT ( 'NONE', #67160 ) ;
#12679=DIRECTION ( 'NONE',  ( -1.836970198721029934E-16, 1.836970198721036344E-16, -1.000000000000000000 ) ) ;
#12685=EDGE_CURVE ( 'NONE', #49587, #49641, #1742, .T. ) ;
#12689=ORIENTED_EDGE ( 'NONE', *, *, #7858, .F. ) ;
#12691=ORIENTED_EDGE ( 'NONE', *, *, #34163, .F. ) ;
#12693=CARTESIAN_POINT ( 'NONE',  ( 7.811466277050736373, -7.272650909786728235, 455.0000000000000568 ) ) ;
#12694=AXIS2_PLACEMENT_3D ( 'NONE', #36861, #9272, #47108 ) ;
#12699=DIRECTION ( 'NONE',  ( -1.000000000000000000, 0.000000000000000000, 0.000000000000000000 ) ) ;
#12712=VECTOR ( 'NONE', #59884, 1000.000000000000000 ) ;
#12714=CARTESIAN_POINT ( 'NONE',  ( -10.19191654964671301, 11.47551654964660450, 195.0000000000000284 ) ) ;
#12725=EDGE_CURVE ( 'NONE', #51349, #25131, #53366, .T. ) ;
#12726=EDGE_CURVE ( 'NONE', #5737, #25046, #64962, .T. ) ;
#12733=ORIENTED_EDGE ( 'NONE', *, *, #40526, .T. ) ;
#12739=CARTESIAN_POINT ( 'NONE',  ( 10.92648345035337343, -9.306483450353493225, 455.0000000000000568 ) ) ;
#12750=ADVANCED_FACE ( 'NONE', ( #48046 ), #64652, .T. ) ;
#12751=VECTOR ( 'NONE', #3768, 1000.000000000000000 ) ;
#12752=DIRECTION ( 'NONE',  ( -0.000000000000000000, -0.000000000000000000, -1.000000000000000000 ) ) ;
#12754=VECTOR ( 'NONE', #54803, 1000.000000000000000 ) ;
#12756=ORIENTED_EDGE ( 'NONE', *, *, #6405, .T. ) ;
#12763=CARTESIAN_POINT ( 'NONE',  ( -7.813516549646839948, -12.00648345035340903, 455.0000000000000568 ) ) ;
#12768=EDGE_CURVE ( 'NONE', #48721, #25046, #65010, .T. ) ;
#12771=VECTOR ( 'NONE', #41651, 1000.000000000000000 ) ;
#12772=ORIENTED_EDGE ( 'NONE', *, *, #26621, .F. ) ;
#12776=EDGE_CURVE ( 'NONE', #57591, #64137, #32134, .T. ) ;
#12794=VECTOR ( 'NONE', #12983, 1000.000000000000000 ) ;
#12799=ORIENTED_EDGE ( 'NONE', *, *, #56914, .T. ) ;
#12808=VERTEX_POINT ( 'NONE', #10914 ) ;
#12810=FACE_OUTER_BOUND ( 'NONE', #60582, .T. ) ;
#12813=CARTESIAN_POINT ( 'NONE',  ( 11.34648345035330053, 1.077516549646569066, 195.0000000000000284 ) ) ;
#12817=ORIENTED_EDGE ( 'NONE', *, *, #13777, .T. ) ;
#12823=CYLINDRICAL_SURFACE ( 'NONE', #45903, 2.204799999999996540 ) ;
#12826=EDGE_CURVE ( 'NONE', #23956, #46196, #3989, .T. ) ;
#12833=APPLICATION_CONTEXT ( 'automotive_design' ) ;
#12835=DIRECTION ( 'NONE',  ( 1.000000000000000000, -0.000000000000000000, 0.000000000000000000 ) ) ;
#12865=EDGE_CURVE ( 'NONE', #3828, #29489, #12271, .T. ) ;
#12886=CARTESIAN_POINT ( 'NONE',  ( -9.093516549646828651, -11.12648345035338870, 455.0000000000000568 ) ) ;
#12888=FACE_OUTER_BOUND ( 'NONE', #4498, .T. ) ;
#12895=CARTESIAN_POINT ( 'NONE',  ( -4.188533722949335569, 4.727349090213398775, 455.0000000000000568 ) ) ;
#12899=DIRECTION ( 'NONE',  ( -0.000000000000000000, -0.000000000000000000, -1.000000000000000000 ) ) ;
#12901=ORIENTED_EDGE ( 'NONE', *, *, #36507, .F. ) ;
#12904=EDGE_CURVE ( 'NONE', #33631, #15862, #16575, .T. ) ;
#12910=DIRECTION ( 'NONE',  ( 1.836970198721029934E-16, 1.836970198721010706E-16, -1.000000000000000000 ) ) ;
#12911=EDGE_CURVE ( 'NONE', #18339, #40441, #48049, .T. ) ;
#12918=DIRECTION ( 'NONE',  ( -4.336808689942006692E-15, -1.000000000000000000, 0.000000000000000000 ) ) ;
#12920=LINE ( 'NONE', #29895, #32521 ) ;
#12926=CARTESIAN_POINT ( 'NONE',  ( -1.677516549646676625, 10.73351654964656987, 455.0000000000000568 ) ) ;
#12946=AXIS2_PLACEMENT_3D ( 'NONE', #56339, #55643, #62331 ) ;
#12959=DIRECTION ( 'NONE',  ( 0.6414496315691473605, 0.7671651518153083105, 0.000000000000000000 ) ) ;
#12962=ORIENTED_EDGE ( 'NONE', *, *, #30122, .T. ) ;
#12972=DIRECTION ( 'NONE',  ( 0.7071067811865486830, 0.7071067811865464625, 0.000000000000000000 ) ) ;
#12973=AXIS2_PLACEMENT_3D ( 'NONE', #41453, #68323, #24497 ) ;
#12975=DIRECTION ( 'NONE',  ( -1.836970198721029934E-16, -1.836970198721010706E-16, 1.000000000000000000 ) ) ;
#12983=DIRECTION ( 'NONE',  ( -1.836970198721029934E-16, 1.836970198721036344E-16, -1.000000000000000000 ) ) ;
#12984=VECTOR ( 'NONE', #52184, 1000.000000000000000 ) ;
#12985=VECTOR ( 'NONE', #61061, 1000.000000000000000 ) ;
#12989=VERTEX_POINT ( 'NONE', #2033 ) ;
#12993=CIRCLE ( 'NONE', #27713, 0.5999999999999998668 ) ;
#12997=CARTESIAN_POINT ( 'NONE',  ( 9.841277389592722358, -2.290483450353490547, 455.0000000000000568 ) ) ;
#12998=EDGE_LOOP ( 'NONE', ( #48214, #10590, #2660, #35621 ) ) ;
#13002=CARTESIAN_POINT ( 'NONE',  ( -4.393516549646835578, -11.78648345035344214, 455.0000000000000568 ) ) ;
#13005=DIRECTION ( 'NONE',  ( 0.000000000000000000, 0.000000000000000000, 1.000000000000000000 ) ) ;
#13006=CARTESIAN_POINT ( 'NONE',  ( 10.20488345035340494, 9.791916549646614953, 195.0000000000000284 ) ) ;
#13014=CARTESIAN_POINT ( 'NONE',  ( 7.428221114745000797, 3.593516549646565750, 455.0000000000000568 ) ) ;
#13020=DIRECTION ( 'NONE',  ( 1.836970198721029934E-16, 1.836970198721010706E-16, -1.000000000000000000 ) ) ;
#13021=DIRECTION ( 'NONE',  ( 1.088659024508174257E-14, 1.000000000000000000, 1.836970198721030674E-16 ) ) ;
#13022=ORIENTED_EDGE ( 'NONE', *, *, #24978, .F. ) ;
#13025=CARTESIAN_POINT ( 'NONE',  ( -11.99351654964671354, 4.173516549646604901, 455.0000000000000568 ) ) ;
#13034=EDGE_LOOP ( 'NONE', ( #2352, #31351, #15126, #13603 ) ) ;
#13036=VECTOR ( 'NONE', #18882, 1000.000000000000000 ) ;
#13039=DIRECTION ( 'NONE',  ( -1.000000000000000000, 8.728482790395504563E-15, 0.000000000000000000 ) ) ;
#13040=DIRECTION ( 'NONE',  ( -1.000000000000000000, 1.185108578570163402E-14, 1.836970198721051628E-16 ) ) ;
#13045=VERTEX_POINT ( 'NONE', #61404 ) ;
#13048=AXIS2_PLACEMENT_3D ( 'NONE', #13709, #29972, #56836 ) ;
#13053=CIRCLE ( 'NONE', #35615, 2.204799999999997873 ) ;
#13059=DIRECTION ( 'NONE',  ( -0.7671651518153006499, -0.6414496315691565753, -2.356647714346250026E-16 ) ) ;
#13060=VERTEX_POINT ( 'NONE', #29588 ) ;
#13065=CARTESIAN_POINT ( 'NONE',  ( -11.07551654964667520, 9.791916549646639822, 455.0000000000000568 ) ) ;
#13076=EDGE_LOOP ( 'NONE', ( #45935, #20950, #28467, #42499 ) ) ;
#13078=ORIENTED_EDGE ( 'NONE', *, *, #10666, .F. ) ;
#13095=AXIS2_PLACEMENT_3D ( 'NONE', #63073, #42200, #63783 ) ;
#13101=DIRECTION ( 'NONE',  ( 1.000000000000000000, -1.047444401652940007E-14, 1.836970198721010706E-16 ) ) ;
#13103=CARTESIAN_POINT ( 'NONE',  ( -8.452095193409485674, -7.757955312929543545, 455.0000000000000568 ) ) ;
#13104=AXIS2_PLACEMENT_3D ( 'NONE', #14637, #57768, #58494 ) ;
#13105=VECTOR ( 'NONE', #53842, 1000.000000000000000 ) ;
#13108=DIRECTION ( 'NONE',  ( 1.836970198721029934E-16, -1.836970198721036344E-16, 1.000000000000000000 ) ) ;
#13109=VERTEX_POINT ( 'NONE', #68127 ) ;
#13127=CARTESIAN_POINT ( 'NONE',  ( 4.186483450353337687, -11.78648345035347589, 455.0000000000000568 ) ) ;
#13132=EDGE_LOOP ( 'NONE', ( #54151, #29116, #69210, #55000 ) ) ;
#13139=CARTESIAN_POINT ( 'NONE',  ( 11.12648345035336384, 2.893516549646526048, 455.0000000000000568 ) ) ;
#13145=FACE_OUTER_BOUND ( 'NONE', #48087, .T. ) ;
#13152=VECTOR ( 'NONE', #43403, 1000.000000000000000 ) ;
#13157=VECTOR ( 'NONE', #48562, 999.9999999999998863 ) ;
#13175=CARTESIAN_POINT ( 'NONE',  ( 10.20488345035345645, 11.47551654964653167, 455.0000000000000568 ) ) ;
#13179=ORIENTED_EDGE ( 'NONE', *, *, #65837, .T. ) ;
#13182=EDGE_LOOP ( 'NONE', ( #30974, #56816, #26406, #62352 ) ) ;
#13187=EDGE_CURVE ( 'NONE', #705, #39630, #41608, .T. ) ;
#13189=DIRECTION ( 'NONE',  ( 1.000000000000000000, 0.000000000000000000, 0.000000000000000000 ) ) ;
#13193=VERTEX_POINT ( 'NONE', #59266 ) ;
#13195=VERTEX_POINT ( 'NONE', #69181 ) ;
#13197=VECTOR ( 'NONE', #52287, 1000.000000000000000 ) ;
#13199=FACE_OUTER_BOUND ( 'NONE', #45729, .T. ) ;
#13200=EDGE_CURVE ( 'NONE', #15780, #34574, #69530, .T. ) ;
#13201=DIRECTION ( 'NONE',  ( 1.000000000000000000, -1.678252938371784572E-14, 1.836970198720999119E-16 ) ) ;
#13206=CARTESIAN_POINT ( 'NONE',  ( 7.428221114744952835, 3.593516549646614155, 195.0000000000000284 ) ) ;
#13209=ORIENTED_EDGE ( 'NONE', *, *, #63946, .T. ) ;
#13218=CARTESIAN_POINT ( 'NONE',  ( 11.48848345035334617, -11.08848345035339733, 195.0000000000000284 ) ) ;
#13227=EDGE_LOOP ( 'NONE', ( #49246, #19097, #26472, #6127 ) ) ;
#13230=CARTESIAN_POINT ( 'NONE',  ( 9.804883450353379715, -11.08848345035349325, 455.0000000000000568 ) ) ;
#13233=VERTEX_POINT ( 'NONE', #31375 ) ;
#13242=CARTESIAN_POINT ( 'NONE',  ( 12.00648345035338238, 4.173516549646515195, 455.0000000000000568 ) ) ;
#13243=ORIENTED_EDGE ( 'NONE', *, *, #33765, .F. ) ;
#13251=CIRCLE ( 'NONE', #22315, 0.1999999999999987899 ) ;
#13254=DIRECTION ( 'NONE',  ( -1.836970198721029934E-16, 1.836970198721036344E-16, -1.000000000000000000 ) ) ;
#13258=AXIS2_PLACEMENT_3D ( 'NONE', #62148, #3813, #8051 ) ;
#13270=AXIS2_PLACEMENT_3D ( 'NONE', #11842, #59259, #49357 ) ;
#13272=EDGE_CURVE ( 'NONE', #56475, #14148, #62776, .T. ) ;
#13278=ORIENTED_EDGE ( 'NONE', *, *, #5140, .T. ) ;
#13279=CARTESIAN_POINT ( 'NONE',  ( -8.693516549646711056, 11.11351654964659730, 195.0000000000000284 ) ) ;
#13284=DIRECTION ( 'NONE',  ( 1.000000000000000000, -1.047444401652940007E-14, 1.836970198721010706E-16 ) ) ;
#13285=ADVANCED_FACE ( 'NONE', ( #4834 ), #53626, .F. ) ;
#13286=CARTESIAN_POINT ( 'NONE',  ( 7.811466277050743479, 4.727349090213326832, 455.0000000000000568 ) ) ;
#13287=DIRECTION ( 'NONE',  ( -0.000000000000000000, -0.000000000000000000, -1.000000000000000000 ) ) ;
#13292=LINE ( 'NONE', #51830, #23719 ) ;
#13297=LINE ( 'NONE', #44764, #7875 ) ;
#13308=CIRCLE ( 'NONE', #12037, 2.204799999999998761 ) ;
#13319=VERTEX_POINT ( 'NONE', #64927 ) ;
#13324=PLANE ( 'NONE',  #21228 ) ;
#13343=CARTESIAN_POINT ( 'NONE',  ( -7.793516549646783531, -11.32648345035335780, 195.0000000000000284 ) ) ;
#13344=ADVANCED_FACE ( 'NONE', ( #33087 ), #567, .T. ) ;
#13352=VECTOR ( 'NONE', #42419, 1000.000000000000114 ) ;
#13354=ORIENTED_EDGE ( 'NONE', *, *, #59914, .F. ) ;
#13364=EDGE_LOOP ( 'NONE', ( #68735, #34228, #67473, #5585 ) ) ;
#13365=DIRECTION ( 'NONE',  ( -1.836970198721029934E-16, 1.836970198721036344E-16, -1.000000000000000000 ) ) ;
#13371=CARTESIAN_POINT ( 'NONE',  ( 6.344579767990853547, 8.393516549646580671, 455.0000000000000568 ) ) ;
#13374=VERTEX_POINT ( 'NONE', #7235 ) ;
#13389=ORIENTED_EDGE ( 'NONE', *, *, #102, .F. ) ;
#13393=VECTOR ( 'NONE', #47227, 1000.000000000000000 ) ;
#13402=DIRECTION ( 'NONE',  ( 1.836970198721029934E-16, 1.836970198721010706E-16, -1.000000000000000000 ) ) ;
#13411=DIRECTION ( 'NONE',  ( -1.836970198721029934E-16, 1.836970198721036344E-16, -1.000000000000000000 ) ) ;
#13418=CARTESIAN_POINT ( 'NONE',  ( -11.77351654964670935, 7.593516549646604830, 455.0000000000000568 ) ) ;
#13420=CIRCLE ( 'NONE', #33754, 0.3999999999999993006 ) ;
#13423=ORIENTED_EDGE ( 'NONE', *, *, #49985, .T. ) ;
#13433=LINE ( 'NONE', #31113, #2968 ) ;
#13438=PLANE ( 'NONE',  #27011 ) ;
#13444=DIRECTION ( 'NONE',  ( -0.000000000000000000, 3.673940397442059868E-16, -1.000000000000000000 ) ) ;
#13454=LINE ( 'NONE', #6755, #37720 ) ;
#13456=EDGE_LOOP ( 'NONE', ( #27828, #2561, #13840, #61249 ) ) ;
#13465=ORIENTED_EDGE ( 'NONE', *, *, #2811, .T. ) ;
#13467=CARTESIAN_POINT ( 'NONE',  ( 11.12648345035337982, -4.206483450353492692, 455.0000000000000568 ) ) ;
#13470=EDGE_LOOP ( 'NONE', ( #11474, #36297, #8923, #36206 ) ) ;
#13477=CARTESIAN_POINT ( 'NONE',  ( 6.619341603356875936, 7.252248008019321901, 455.0000000000000568 ) ) ;
#13479=VERTEX_POINT ( 'NONE', #61327 ) ;
#13491=EDGE_CURVE ( 'NONE', #68617, #28757, #57702, .T. ) ;
#13513=DIRECTION ( 'NONE',  ( 1.062171939662867618E-14, 1.000000000000000000, 0.000000000000000000 ) ) ;
#13514=ORIENTED_EDGE ( 'NONE', *, *, #8700, .F. ) ;
#13515=VECTOR ( 'NONE', #50577, 1000.000000000000114 ) ;
#13518=VECTOR ( 'NONE', #15978, 1000.000000000000000 ) ;
#13520=EDGE_LOOP ( 'NONE', ( #50074, #53896, #20397, #60905 ) ) ;
#13526=EDGE_LOOP ( 'NONE', ( #64602, #24884, #69296, #38841 ) ) ;
#13534=ORIENTED_EDGE ( 'NONE', *, *, #12073, .T. ) ;
#13535=ADVANCED_FACE ( 'NONE', ( #48497 ), #54504, .F. ) ;
#13536=DIRECTION ( 'NONE',  ( -1.836970198721029934E-16, 1.836970198721036344E-16, -1.000000000000000000 ) ) ;
#13537=FACE_OUTER_BOUND ( 'NONE', #31300, .T. ) ;
#13538=LINE ( 'NONE', #18845, #57217 ) ;
#13553=AXIS2_PLACEMENT_3D ( 'NONE', #18221, #2317, #67013 ) ;
#13554=VECTOR ( 'NONE', #31405, 1000.000000000000000 ) ;
#13559=ORIENTED_EDGE ( 'NONE', *, *, #20675, .T. ) ;
#13563=VERTEX_POINT ( 'NONE', #20919 ) ;
#13566=VECTOR ( 'NONE', #58239, 1000.000000000000000 ) ;
#13568=DIRECTION ( 'NONE',  ( -1.000000000000000000, 8.359604446858499085E-15, 3.071268848394973203E-30 ) ) ;
#13572=EDGE_LOOP ( 'NONE', ( #62703, #7615, #23075, #52233 ) ) ;
#13575=EDGE_CURVE ( 'NONE', #40712, #47459, #43874, .T. ) ;
#13582=VECTOR ( 'NONE', #21398, 1000.000000000000000 ) ;
#13588=DIRECTION ( 'NONE',  ( 1.000000000000000000, -7.304098846218132892E-15, -2.683482381803073952E-30 ) ) ;
#13593=EDGE_LOOP ( 'NONE', ( #69636, #49214, #48372, #29285 ) ) ;
#13603=ORIENTED_EDGE ( 'NONE', *, *, #36265, .T. ) ;
#13607=VECTOR ( 'NONE', #69724, 1000.000000000000000 ) ;
#13611=LINE ( 'NONE', #2307, #17445 ) ;
#13616=DIRECTION ( 'NONE',  ( -0.000000000000000000, -0.000000000000000000, -1.000000000000000000 ) ) ;
#13618=DIRECTION ( 'NONE',  ( -0.000000000000000000, 3.673940397442059868E-16, -1.000000000000000000 ) ) ;
#13621=LINE ( 'NONE', #3029, #53758 ) ;
#13622=ORIENTED_EDGE ( 'NONE', *, *, #16510, .F. ) ;
#13635=AXIS2_PLACEMENT_3D ( 'NONE', #274, #31768, #63939 ) ;
#13644=LINE ( 'NONE', #30273, #65493 ) ;
#13658=DIRECTION ( 'NONE',  ( 0.000000000000000000, -1.000000000000000000, -3.673940397442059868E-16 ) ) ;
#13670=LINE ( 'NONE', #40184, #17419 ) ;
#13678=ORIENTED_EDGE ( 'NONE', *, *, #59901, .T. ) ;
#13690=VERTEX_POINT ( 'NONE', #12714 ) ;
#13695=DIRECTION ( 'NONE',  ( -1.000000000000000000, 0.000000000000000000, 0.000000000000000000 ) ) ;
#13699=VECTOR ( 'NONE', #6784, 1000.000000000000000 ) ;
#13701=FACE_OUTER_BOUND ( 'NONE', #55451, .T. ) ;
#13709=CARTESIAN_POINT ( 'NONE',  ( 8.406483450353379183, -7.616533956692325802, 455.0000000000000568 ) ) ;
#13710=ORIENTED_EDGE ( 'NONE', *, *, #3857, .F. ) ;
#13714=ORIENTED_EDGE ( 'NONE', *, *, #15116, .F. ) ;
#13721=VECTOR ( 'NONE', #36937, 1000.000000000000000 ) ;
#13723=CARTESIAN_POINT ( 'NONE',  ( 11.12648345035340647, 9.093516549646563973, 455.0000000000000568 ) ) ;
#13742=CARTESIAN_POINT ( 'NONE',  ( -10.19191654964685156, -9.804883450353383267, 455.0000000000000568 ) ) ;
#13747=VECTOR ( 'NONE', #69333, 1000.000000000000114 ) ;
#13761=EDGE_CURVE ( 'NONE', #67569, #41004, #55869, .T. ) ;
#13770=CARTESIAN_POINT ( 'NONE',  ( -9.404046420174113408, -1.866219381641437636, 455.0000000000000568 ) ) ;
#13777=EDGE_CURVE ( 'NONE', #43815, #51738, #12362, .T. ) ;
#13782=DIRECTION ( 'NONE',  ( -1.836970198721029934E-16, -1.836970198721010706E-16, 1.000000000000000000 ) ) ;
#13788=LINE ( 'NONE', #40314, #67477 ) ;
#13793=VERTEX_POINT ( 'NONE', #60132 ) ;
#13806=AXIS2_PLACEMENT_3D ( 'NONE', #11716, #33303, #54881 ) ;
#13810=ORIENTED_EDGE ( 'NONE', *, *, #12726, .F. ) ;
#13814=ORIENTED_EDGE ( 'NONE', *, *, #52579, .F. ) ;
#13817=EDGE_CURVE ( 'NONE', #63555, #21380, #67326, .T. ) ;
#13822=ORIENTED_EDGE ( 'NONE', *, *, #34479, .T. ) ;
#13828=ORIENTED_EDGE ( 'NONE', *, *, #34039, .F. ) ;
#13832=CARTESIAN_POINT ( 'NONE',  ( 10.20488345035338185, -9.804883450353528929, 455.0000000000000568 ) ) ;
#13835=EDGE_CURVE ( 'NONE', #43261, #56939, #13433, .T. ) ;
#13836=LINE ( 'NONE', #56624, #20078 ) ;
#13838=DIRECTION ( 'NONE',  ( -0.7071067811865474617, -0.7071067811865474617, -0.000000000000000000 ) ) ;
#13839=ORIENTED_EDGE ( 'NONE', *, *, #25037, .T. ) ;
#13840=ORIENTED_EDGE ( 'NONE', *, *, #7858, .T. ) ;
#13863=DIRECTION ( 'NONE',  ( -2.135044278125299371E-15, -1.000000000000000000, 0.000000000000000000 ) ) ;
#13868=ORIENTED_EDGE ( 'NONE', *, *, #58761, .T. ) ;
#13878=AXIS2_PLACEMENT_3D ( 'NONE', #24728, #19755, #52303 ) ;
#13879=DIRECTION ( 'NONE',  ( -1.000000000000000000, 0.000000000000000000, 0.000000000000000000 ) ) ;
#13880=ORIENTED_EDGE ( 'NONE', *, *, #24403, .F. ) ;
#13888=PLANE ( 'NONE',  #47859 ) ;
#13895=AXIS2_PLACEMENT_3D ( 'NONE', #55698, #40116, #50392 ) ;
#13905=CARTESIAN_POINT ( 'NONE',  ( -10.91351654964666906, -2.906483450353290809, 195.0000000000000284 ) ) ;
#13912=ORIENTED_EDGE ( 'NONE', *, *, #6735, .T. ) ;
#13914=ORIENTED_EDGE ( 'NONE', *, *, #44980, .F. ) ;
#13924=DIRECTION ( 'NONE',  ( -0.6414496315691592399, 0.7671651518152985405, 2.587583378555133228E-16 ) ) ;
#13926=VECTOR ( 'NONE', #1104, 1000.000000000000000 ) ;
#13930=CYLINDRICAL_SURFACE ( 'NONE', #41923, 2.204799999999998761 ) ;
#13936=LINE ( 'NONE', #57066, #58605 ) ;
#13938=DIRECTION ( 'NONE',  ( -0.5000000000000038858, -0.8660254037844363761, 0.000000000000000000 ) ) ;
#13939=CARTESIAN_POINT ( 'NONE',  ( -11.99351654964671354, 11.18071654964658990, 455.0000000000000568 ) ) ;
#13951=DIRECTION ( 'NONE',  ( -1.000000000000000000, 0.000000000000000000, 0.000000000000000000 ) ) ;
#13952=CARTESIAN_POINT ( 'NONE',  ( -6.606374702650169795, 7.252248008019353875, 195.0000000000000284 ) ) ;
#13954=CARTESIAN_POINT ( 'NONE',  ( -5.993516549646711766, 3.593516549646603497, 195.0000000000000284 ) ) ;
#13956=ORIENTED_EDGE ( 'NONE', *, *, #49363, .T. ) ;
#13992=ORIENTED_EDGE ( 'NONE', *, *, #38863, .T. ) ;
#13995=CARTESIAN_POINT ( 'NONE',  ( 9.841277389592722358, -1.690483450353395201, 195.0000000000000284 ) ) ;
#14003=CARTESIAN_POINT ( 'NONE',  ( -4.727349090213511573, -7.811466277050747919, 195.0000000000000284 ) ) ;
#14006=CIRCLE ( 'NONE', #24166, 2.204799999999997873 ) ;
#14015=EDGE_CURVE ( 'NONE', #22396, #52737, #67376, .T. ) ;
#14016=EDGE_CURVE ( 'NONE', #68360, #43734, #59017, .T. ) ;
#14023=CARTESIAN_POINT ( 'NONE',  ( 1.866219381641437192, 9.404046420174054788, 195.0000000000000284 ) ) ;
#14024=ORIENTED_EDGE ( 'NONE', *, *, #631, .T. ) ;
#14026=DIRECTION ( 'NONE',  ( 1.000000000000000000, -6.308085367188446447E-15, 0.000000000000000000 ) ) ;
#14035=PLANE ( 'NONE',  #12533 ) ;
#14045=VERTEX_POINT ( 'NONE', #42406 ) ;
#14050=CARTESIAN_POINT ( 'NONE',  ( 7.852485183456924034, 3.417780618358489786, 455.0000000000000568 ) ) ;
#14058=VERTEX_POINT ( 'NONE', #37804 ) ;
#14060=DIRECTION ( 'NONE',  ( 1.000000000000000000, 0.000000000000000000, 0.000000000000000000 ) ) ;
#14069=LINE ( 'NONE', #52623, #7861 ) ;
#14074=EDGE_CURVE ( 'NONE', #52876, #18487, #37461, .T. ) ;
#14083=ORIENTED_EDGE ( 'NONE', *, *, #50402, .F. ) ;
#14087=VECTOR ( 'NONE', #64480, 1000.000000000000000 ) ;
#14089=ORIENTED_EDGE ( 'NONE', *, *, #6011, .T. ) ;
#14095=DIRECTION ( 'NONE',  ( -0.000000000000000000, -0.000000000000000000, -1.000000000000000000 ) ) ;
#14105=CARTESIAN_POINT ( 'NONE',  ( 4.201500623656003519, -4.740315990920286104, 455.0000000000000568 ) ) ;
#14109=EDGE_CURVE ( 'NONE', #4070, #44826, #35599, .T. ) ;
#14120=DIRECTION ( 'NONE',  ( 0.000000000000000000, 1.000000000000000000, 3.673940397442059868E-16 ) ) ;
#14123=EDGE_CURVE ( 'NONE', #27624, #47490, #5289, .T. ) ;
#14141=EDGE_CURVE ( 'NONE', #55545, #9367, #2043, .T. ) ;
#14143=PLANE ( 'NONE',  #5036 ) ;
#14148=VERTEX_POINT ( 'NONE', #43797 ) ;
#14154=ORIENTED_EDGE ( 'NONE', *, *, #22871, .F. ) ;
#14157=CARTESIAN_POINT ( 'NONE',  ( 6.344579767990853547, 8.393516549646580671, 455.0000000000000568 ) ) ;
#14159=DIRECTION ( 'NONE',  ( -1.836970198721029934E-16, -1.836970198721010706E-16, 1.000000000000000000 ) ) ;
#14160=ORIENTED_EDGE ( 'NONE', *, *, #62136, .F. ) ;
#14167=EDGE_CURVE ( 'NONE', #48590, #55190, #65709, .T. ) ;
#14170=VECTOR ( 'NONE', #57398, 1000.000000000000000 ) ;
#14172=ORIENTED_EDGE ( 'NONE', *, *, #33836, .T. ) ;
#14174=AXIS2_PLACEMENT_3D ( 'NONE', #33111, #27464, #22514 ) ;
#14195=DIRECTION ( 'NONE',  ( 0.5000000000000004441, -0.8660254037844383745, 0.000000000000000000 ) ) ;
#14201=CARTESIAN_POINT ( 'NONE',  ( 4.622483450353394474, 3.593516549646586622, 455.0000000000000568 ) ) ;
#14203=DIRECTION ( 'NONE',  ( -1.000000000000000000, 1.610765207321970913E-14, 1.836970198721059516E-16 ) ) ;
#14204=ORIENTED_EDGE ( 'NONE', *, *, #46094, .F. ) ;
#14213=ORIENTED_EDGE ( 'NONE', *, *, #39662, .T. ) ;
#14215=CARTESIAN_POINT ( 'NONE',  ( 1.690483450353351458, -9.841277389592704594, 195.0000000000000284 ) ) ;
#14217=VECTOR ( 'NONE', #37373, 1000.000000000000000 ) ;
#14225=DIRECTION ( 'NONE',  ( 1.836970198721029934E-16, 1.836970198721010706E-16, -1.000000000000000000 ) ) ;
#14230=PLANE ( 'NONE',  #8716 ) ;
#14239=AXIS2_PLACEMENT_3D ( 'NONE', #6864, #28432, #1565 ) ;
#14243=VERTEX_POINT ( 'NONE', #50481 ) ;
#14246=EDGE_CURVE ( 'NONE', #34313, #58981, #28555, .T. ) ;
#14248=AXIS2_PLACEMENT_3D ( 'NONE', #3675, #58488, #15333 ) ;
#14249=DIRECTION ( 'NONE',  ( 4.336808689942043768E-15, 1.000000000000000000, 0.000000000000000000 ) ) ;
#14251=DIRECTION ( 'NONE',  ( -0.7671651518153105309, 0.6414496315691445849, 2.356647714346206145E-16 ) ) ;
#14253=FACE_BOUND ( 'NONE', #59773, .T. ) ;
#14254=VECTOR ( 'NONE', #12269, 1000.000000000000000 ) ;
#14257=CARTESIAN_POINT ( 'NONE',  ( 10.09643294401457858, 9.293516549646566816, 455.0000000000000568 ) ) ;
#14258=ORIENTED_EDGE ( 'NONE', *, *, #50558, .T. ) ;
#14259=VERTEX_POINT ( 'NONE', #18640 ) ;
#14269=ORIENTED_EDGE ( 'NONE', *, *, #63737, .F. ) ;
#14271=CARTESIAN_POINT ( 'NONE',  ( -7.415254214038299097, -3.006483450353353515, 195.0000000000000284 ) ) ;
#14274=CARTESIAN_POINT ( 'NONE',  ( 7.265214908726123078, -6.619341603356961201, 455.0000000000000568 ) ) ;
#14287=LINE ( 'NONE', #47502, #31840 ) ;
#14289=DIRECTION ( 'NONE',  ( 1.836970198721029934E-16, 1.836970198721010706E-16, -1.000000000000000000 ) ) ;
#14290=ORIENTED_EDGE ( 'NONE', *, *, #1156, .F. ) ;
#14292=VECTOR ( 'NONE', #69078, 1000.000000000000000 ) ;
#14300=LINE ( 'NONE', #31280, #19064 ) ;
#14312=CARTESIAN_POINT ( 'NONE',  ( -2.752095193409461071, -9.955011587777271131, 195.0000000000000284 ) ) ;
#14313=EDGE_CURVE ( 'NONE', #32701, #16734, #57528, .T. ) ;
#14314=FACE_OUTER_BOUND ( 'NONE', #52292, .T. ) ;
#14333=CARTESIAN_POINT ( 'NONE',  ( -8.452095193409485674, -7.757955312929543545, 455.0000000000000568 ) ) ;
#14338=LINE ( 'NONE', #30249, #67364 ) ;
#14343=ORIENTED_EDGE ( 'NONE', *, *, #32827, .T. ) ;
#14344=AXIS2_PLACEMENT_3D ( 'NONE', #21844, #47327, #5251 ) ;
#14350=LINE ( 'NONE', #40853, #22452 ) ;
#14352=EDGE_CURVE ( 'NONE', #9482, #15805, #35652, .T. ) ;
#14355=ORIENTED_EDGE ( 'NONE', *, *, #33705, .F. ) ;
#14359=ORIENTED_EDGE ( 'NONE', *, *, #24633, .T. ) ;
#14367=DIRECTION ( 'NONE',  ( -0.7071067811865527908, -0.7071067811865422437, 0.000000000000000000 ) ) ;
#14378=AXIS2_PLACEMENT_3D ( 'NONE', #45106, #18233, #6928 ) ;
#14386=CARTESIAN_POINT ( 'NONE',  ( -11.99351654964671354, 7.813516549646603693, 455.0000000000000568 ) ) ;
#14387=EDGE_CURVE ( 'NONE', #14943, #15805, #31385, .T. ) ;
#14393=EDGE_CURVE ( 'NONE', #47898, #65081, #59277, .T. ) ;
#14407=PLANE ( 'NONE',  #45877 ) ;
#14411=VERTEX_POINT ( 'NONE', #5195 ) ;
#14415=CARTESIAN_POINT ( 'NONE',  ( 1.866219381641426533, -9.417013320880776917, 195.0000000000000284 ) ) ;
#14426=CARTESIAN_POINT ( 'NONE',  ( 4.747751991980625696, -5.393625297350043368, 455.0000000000000568 ) ) ;
#14436=ORIENTED_EDGE ( 'NONE', *, *, #10969, .F. ) ;
#14438=CARTESIAN_POINT ( 'NONE',  ( -2.893516549646828473, -10.92648345035345514, 455.0000000000000568 ) ) ;
#14443=PLANE ( 'NONE',  #69455 ) ;
#14445=DIRECTION ( 'NONE',  ( 1.000000000000000000, -7.304098846218132892E-15, -2.683482381803073952E-30 ) ) ;
#14447=ORIENTED_EDGE ( 'NONE', *, *, #27982, .F. ) ;
#14454=PLANE ( 'NONE',  #40694 ) ;
#14465=VECTOR ( 'NONE', #17701, 1000.000000000000000 ) ;
#14469=EDGE_LOOP ( 'NONE', ( #29180, #22375, #4614, #54037, #19234, #2335, #55858, #29162, #25032, #1318, #3750, #47366, #2590, #8961, #61178, #21812, #57229, #13022, #53493, #61918, #58444, #63381, #42948, #19083, #6360, #13622, #52640, #27366, #1281, #61411, #62296, #18077, #11428, #57955, #3907, #43646, #52370, #36360, #68429, #4182, #53457, #4785, #45288, #23081, #35906, #30957, #28238, #22961, #22591, #63515, #45594, #66309, #51555, #16430, #37388, #57051, #55269, #59538, #39035, #63940, #53119, #44967, #51615, #31360, #6021, #66567, #57705, #8457, #59571, #37257, #42075, #59387, #32876, #50169, #22609, #28832, #18740, #55304, #21762, #62487, #27999, #37081, #17197, #42546, #38125, #32532, #61626, #24915, #19046, #12551, #32823, #29463, #8676, #66677, #43931, #11708, #66342, #5412, #5284, #64124, #45299, #53434, #19652, #55833, #40230, #35134, #62459, #36981, #52009, #28359, #35790, #499, #45770, #9034, #63131, #10625, #21347, #13810, #26301, #56706, #69919, #63751, #4930, #69945, #25728, #5690, #58185, #8575, #65462, #52786, #55999, #31421, #4572, #47015, #16334, #54397, #46403, #65243, #57304, #38109, #13880, #66629, #20339, #65680, #59709, #12279, #64552, #1853, #35127, #50742, #28500, #4195, #57308, #31984, #49572, #11150, #53237, #68508, #50467, #24434, #27747, #3542, #18438, #32039, #26471, #46396, #54479, #40924, #14269, #23269, #7716, #6818, #54958, #60452, #57238, #2799, #242, #54705, #45216, #37092, #37298, #16875, #40126, #3276, #59176, #28100, #35429, #67456, #29495, #11971, #67208, #54490, #18465, #28702, #46168, #8925, #15588, #56538, #15178, #48798, #39807, #18165, #55010, #56584, #49653, #68217, #47370, #33269, #22650, #24202, #22676, #69843, #19480, #49990 ) ) ;
#14487=ORIENTED_EDGE ( 'NONE', *, *, #14742, .T. ) ;
#14489=DIRECTION ( 'NONE',  ( -0.4999999999999755196, 0.8660254037844526964, 2.509347957447861534E-16 ) ) ;
#14493=LINE ( 'NONE', #24747, #34947 ) ;
#14495=CIRCLE ( 'NONE', #68664, 0.6000000000000006439 ) ;
#14497=ORIENTED_EDGE ( 'NONE', *, *, #66042, .T. ) ;
#14498=LINE ( 'NONE', #51976, #19229 ) ;
#14512=DIRECTION ( 'NONE',  ( 1.836970198721029934E-16, 1.836970198721010706E-16, -1.000000000000000000 ) ) ;
#14523=CIRCLE ( 'NONE', #31503, 0.2000000000000005107 ) ;
#14525=EDGE_LOOP ( 'NONE', ( #66547, #37289, #45653, #7520 ) ) ;
#14526=EDGE_LOOP ( 'NONE', ( #40088, #40278, #65874, #32208 ) ) ;
#14527=CIRCLE ( 'NONE', #23551, 0.6000000000000006439 ) ;
#14528=ADVANCED_FACE ( 'NONE', ( #32418 ), #58592, .T. ) ;
#14532=VERTEX_POINT ( 'NONE', #15796 ) ;
#14538=LINE ( 'NONE', #15248, #67368 ) ;
#14541=ORIENTED_EDGE ( 'NONE', *, *, #12725, .T. ) ;
#14543=PLANE ( 'NONE',  #7257 ) ;
#14558=DIRECTION ( 'NONE',  ( 1.011922027653139155E-14, 1.000000000000000000, 0.000000000000000000 ) ) ;
#14564=EDGE_CURVE ( 'NONE', #40478, #50332, #12212, .T. ) ;
#14573=CARTESIAN_POINT ( 'NONE',  ( -5.993516549646728642, -6.006483450353378828, 195.0000000000000284 ) ) ;
#14576=AXIS2_PLACEMENT_3D ( 'NONE', #42563, #32652, #15344 ) ;
#14582=CARTESIAN_POINT ( 'NONE',  ( -7.393516549646710345, 5.993516549646603409, 455.0000000000000568 ) ) ;
#14595=DIRECTION ( 'NONE',  ( 0.5000000000000129896, 0.8660254037844311581, 0.000000000000000000 ) ) ;
#14615=VECTOR ( 'NONE', #23471, 1000.000000000000000 ) ;
#14616=ORIENTED_EDGE ( 'NONE', *, *, #24120, .F. ) ;
#14625=CARTESIAN_POINT ( 'NONE',  ( 12.00648345035336284, 7.813516549646607245, 195.0000000000000284 ) ) ;
#14626=EDGE_CURVE ( 'NONE', #54865, #57591, #44730, .T. ) ;
#14627=LINE ( 'NONE', #25954, #68507 ) ;
#14635=ADVANCED_FACE ( 'NONE', ( #55036 ), #60666, .F. ) ;
#14636=EDGE_CURVE ( 'NONE', #29083, #67623, #9693, .T. ) ;
#14637=CARTESIAN_POINT ( 'NONE',  ( 3.006483450353369502, -7.428221114744997244, 195.0000000000000284 ) ) ;
#14642=EDGE_CURVE ( 'NONE', #28515, #55190, #17178, .T. ) ;
#14643=CARTESIAN_POINT ( 'NONE',  ( -11.11351654964666835, -2.906483450353287257, 195.0000000000000284 ) ) ;
#14649=VECTOR ( 'NONE', #7578, 1000.000000000000000 ) ;
#14653=CARTESIAN_POINT ( 'NONE',  ( 9.804883450353454322, 10.19191654964656912, 455.0000000000000568 ) ) ;
#14660=CARTESIAN_POINT ( 'NONE',  ( 6.006483450353401921, 5.993516549646582092, 455.0000000000000568 ) ) ;
#14665=DIRECTION ( 'NONE',  ( 8.339399738404099512E-15, 1.000000000000000000, 1.836970198721025990E-16 ) ) ;
#14669=ORIENTED_EDGE ( 'NONE', *, *, #23119, .F. ) ;
#14673=AXIS2_PLACEMENT_3D ( 'NONE', #39874, #13005, #56843 ) ;
#14682=ORIENTED_EDGE ( 'NONE', *, *, #12865, .F. ) ;
#14683=VERTEX_POINT ( 'NONE', #56745 ) ;
#14690=CIRCLE ( 'NONE', #54229, 1.399999999999998579 ) ;
#14695=EDGE_CURVE ( 'NONE', #40478, #4544, #2906, .T. ) ;
#14699=VECTOR ( 'NONE', #36260, 1000.000000000000000 ) ;
#14703=VERTEX_POINT ( 'NONE', #68061 ) ;
#14708=CARTESIAN_POINT ( 'NONE',  ( 4.206483450353341702, -11.32648345035347504, 455.0000000000000568 ) ) ;
#14742=EDGE_CURVE ( 'NONE', #36372, #38001, #43599, .T. ) ;
#14758=ORIENTED_EDGE ( 'NONE', *, *, #58761, .F. ) ;
#14759=ORIENTED_EDGE ( 'NONE', *, *, #60399, .F. ) ;
#14768=ORIENTED_EDGE ( 'NONE', *, *, #47551, .T. ) ;
#14772=ORIENTED_EDGE ( 'NONE', *, *, #48481, .T. ) ;
#14775=LINE ( 'NONE', #15820, #45128 ) ;
#14778=CARTESIAN_POINT ( 'NONE',  ( -10.73351654964668533, -1.090483450353341155, 455.0000000000000568 ) ) ;
#14785=EDGE_LOOP ( 'NONE', ( #69795, #50182, #55279, #29530 ) ) ;
#14795=CARTESIAN_POINT ( 'NONE',  ( 8.211283450353379365, -6.006483450353490738, 455.0000000000000568 ) ) ;
#14798=AXIS2_PLACEMENT_3D ( 'NONE', #34746, #28743, #12139 ) ;
#14801=PLANE ( 'NONE',  #9155 ) ;
#14804=AXIS2_PLACEMENT_3D ( 'NONE', #38141, #49768, #1334 ) ;
#14815=VERTEX_POINT ( 'NONE', #52873 ) ;
#14817=ORIENTED_EDGE ( 'NONE', *, *, #24545, .F. ) ;
#14826=VECTOR ( 'NONE', #18797, 1000.000000000000114 ) ;
#14834=DIRECTION ( 'NONE',  ( -0.6414496315691484707, 0.7671651518153074223, 2.309356642088893343E-17 ) ) ;
#14838=DIRECTION ( 'NONE',  ( -0.000000000000000000, -0.000000000000000000, -1.000000000000000000 ) ) ;
#14849=CARTESIAN_POINT ( 'NONE',  ( -11.31351654964669429, -4.206483450353285747, 195.0000000000000284 ) ) ;
#14862=LINE ( 'NONE', #35345, #52136 ) ;
#14864=VERTEX_POINT ( 'NONE', #4768 ) ;
#14868=CARTESIAN_POINT ( 'NONE',  ( 11.78648345035337996, 4.173516549646518747, 455.0000000000000568 ) ) ;
#14873=FACE_OUTER_BOUND ( 'NONE', #14968, .T. ) ;
#14886=VERTEX_POINT ( 'NONE', #16071 ) ;
#14907=FACE_OUTER_BOUND ( 'NONE', #16530, .T. ) ;
#14909=DIRECTION ( 'NONE',  ( 1.000000000000000000, -5.626525616968433909E-15, -1.836970198721040534E-16 ) ) ;
#14926=EDGE_CURVE ( 'NONE', #5249, #8722, #65213, .T. ) ;
#14927=VERTEX_POINT ( 'NONE', #12132 ) ;
#14937=DIRECTION ( 'NONE',  ( 1.836970198721029934E-16, 1.836970198721010706E-16, -1.000000000000000000 ) ) ;
#14943=VERTEX_POINT ( 'NONE', #44305 ) ;
#14953=FACE_OUTER_BOUND ( 'NONE', #30246, .T. ) ;
#14958=ORIENTED_EDGE ( 'NONE', *, *, #3970, .F. ) ;
#14960=DIRECTION ( 'NONE',  ( 1.000000000000000000, 3.016910393003147986E-15, 1.108394896831706469E-30 ) ) ;
#14963=PLANE ( 'NONE',  #50058 ) ;
#14967=EDGE_CURVE ( 'NONE', #28585, #31147, #60227, .T. ) ;
#14968=EDGE_LOOP ( 'NONE', ( #20161, #19548, #27066, #34329 ) ) ;
#14975=EDGE_CURVE ( 'NONE', #60260, #67402, #37992, .T. ) ;
#14977=VERTEX_POINT ( 'NONE', #33368 ) ;
#14979=ADVANCED_FACE ( 'NONE', ( #59551 ), #49626, .F. ) ;
#14981=VECTOR ( 'NONE', #67434, 1000.000000000000000 ) ;
#14982=FACE_OUTER_BOUND ( 'NONE', #69027, .T. ) ;
#14987=DIRECTION ( 'NONE',  ( -1.836970198721029934E-16, -1.836970198721010706E-16, 1.000000000000000000 ) ) ;
#14993=LINE ( 'NONE', #68739, #14292 ) ;
#14994=CARTESIAN_POINT ( 'NONE',  ( 10.74648345035335240, 1.677516549646529409, 455.0000000000000568 ) ) ;
#15005=ORIENTED_EDGE ( 'NONE', *, *, #43223, .T. ) ;
#15009=CARTESIAN_POINT ( 'NONE',  ( -11.11351654964671098, 7.793516549646603231, 455.0000000000000568 ) ) ;
#15020=AXIS2_PLACEMENT_3D ( 'NONE', #18832, #61962, #51353 ) ;
#15026=VERTEX_POINT ( 'NONE', #64054 ) ;
#15027=CARTESIAN_POINT ( 'NONE',  ( 11.12648345035340647, 9.093516549646563973, 455.0000000000000568 ) ) ;
#15033=ORIENTED_EDGE ( 'NONE', *, *, #32569, .F. ) ;
#15034=VECTOR ( 'NONE', #14445, 1000.000000000000000 ) ;
#15038=ORIENTED_EDGE ( 'NONE', *, *, #67950, .T. ) ;
#15046=ORIENTED_EDGE ( 'NONE', *, *, #8428, .F. ) ;
#15059=EDGE_CURVE ( 'NONE', #7017, #41637, #64394, .T. ) ;
#15072=LINE ( 'NONE', #58204, #33796 ) ;
#15087=DIRECTION ( 'NONE',  ( -0.7671651518153131954, -0.6414496315691415873, 0.000000000000000000 ) ) ;
#15103=CARTESIAN_POINT ( 'NONE',  ( 4.201500623656039934, 7.259684009079806266, 455.0000000000000568 ) ) ;
#15113=ORIENTED_EDGE ( 'NONE', *, *, #31773, .T. ) ;
#15116=EDGE_CURVE ( 'NONE', #8498, #61197, #15252, .T. ) ;
#15118=CARTESIAN_POINT ( 'NONE',  ( -4.188533722949335569, 7.259684009079808931, 195.0000000000000284 ) ) ;
#15126=ORIENTED_EDGE ( 'NONE', *, *, #18723, .F. ) ;
#15138=VERTEX_POINT ( 'NONE', #39569 ) ;
#15141=ORIENTED_EDGE ( 'NONE', *, *, #20857, .T. ) ;
#15146=VERTEX_POINT ( 'NONE', #59772 ) ;
#15147=EDGE_CURVE ( 'NONE', #12989, #20073, #43498, .T. ) ;
#15149=VECTOR ( 'NONE', #55442, 1000.000000000000114 ) ;
#15150=VECTOR ( 'NONE', #24163, 1000.000000000000000 ) ;
#15161=FACE_OUTER_BOUND ( 'NONE', #30181, .T. ) ;
#15164=EDGE_CURVE ( 'NONE', #19912, #30539, #28945, .T. ) ;
#15167=CARTESIAN_POINT ( 'NONE',  ( 4.622483450353380263, -3.606483450353395792, 195.0000000000000284 ) ) ;
#15177=PLANE ( 'NONE',  #54539 ) ;
#15178=ORIENTED_EDGE ( 'NONE', *, *, #17311, .F. ) ;
#15180=DIRECTION ( 'NONE',  ( 0.000000000000000000, -3.673940397442059868E-16, 1.000000000000000000 ) ) ;
#15202=ORIENTED_EDGE ( 'NONE', *, *, #64387, .F. ) ;
#15204=DIRECTION ( 'NONE',  ( 0.6414496315691445849, -0.7671651518153106419, 0.000000000000000000 ) ) ;
#15206=ORIENTED_EDGE ( 'NONE', *, *, #5144, .T. ) ;
#15211=CYLINDRICAL_SURFACE ( 'NONE', #10653, 1.399999999999998579 ) ;
#15213=CARTESIAN_POINT ( 'NONE',  ( -7.798499376344157241, -7.272650909786626983, 455.0000000000000568 ) ) ;
#15220=DIRECTION ( 'NONE',  ( -1.836970198721029934E-16, 1.836970198721036344E-16, -1.000000000000000000 ) ) ;
#15230=ORIENTED_EDGE ( 'NONE', *, *, #51136, .T. ) ;
#15232=ADVANCED_FACE ( 'NONE', ( #16986 ), #60796, .T. ) ;
#15248=CARTESIAN_POINT ( 'NONE',  ( -11.77351654964670935, 7.593516549646604830, 455.0000000000000568 ) ) ;
#15252=LINE ( 'NONE', #21602, #59454 ) ;
#15255=VECTOR ( 'NONE', #704, 1000.000000000000000 ) ;
#15259=FACE_OUTER_BOUND ( 'NONE', #62644, .T. ) ;
#15261=DIRECTION ( 'NONE',  ( 0.7071067811865348052, -0.7071067811865602293, -3.278703137324831017E-30 ) ) ;
#15264=SURFACE_STYLE_FILL_AREA ( #42120 ) ;
#15280=EDGE_CURVE ( 'NONE', #47767, #14864, #33918, .T. ) ;
#15281=LINE ( 'NONE', #31207, #40923 ) ;
#15282=EDGE_CURVE ( 'NONE', #8019, #64293, #66455, .T. ) ;
#15289=LINE ( 'NONE', #32849, #9689 ) ;
#15307=VERTEX_POINT ( 'NONE', #44536 ) ;
#15315=ORIENTED_EDGE ( 'NONE', *, *, #64373, .T. ) ;
#15318=AXIS2_PLACEMENT_3D ( 'NONE', #43167, #69713, #65773 ) ;
#15325=ORIENTED_EDGE ( 'NONE', *, *, #17771, .F. ) ;
#15326=CARTESIAN_POINT ( 'NONE',  ( 11.48848345035341900, 10.19191654964656202, 455.0000000000000568 ) ) ;
#15331=CARTESIAN_POINT ( 'NONE',  ( 10.92648345035340895, 9.093516549646565750, 455.0000000000000568 ) ) ;
#15333=DIRECTION ( 'NONE',  ( 0.7671651518153006499, -0.6414496315691565753, 0.000000000000000000 ) ) ;
#15341=LINE ( 'NONE', #47857, #49670 ) ;
#15342=AXIS2_PLACEMENT_3D ( 'NONE', #66323, #66658, #43716 ) ;
#15344=DIRECTION ( 'NONE',  ( 0.000000000000000000, -1.000000000000000000, 0.000000000000000000 ) ) ;
#15379=CARTESIAN_POINT ( 'NONE',  ( 7.811466277050774565, 7.259684009079793832, 455.0000000000000568 ) ) ;
#15389=DIRECTION ( 'NONE',  ( -0.000000000000000000, 3.673940397442059868E-16, -1.000000000000000000 ) ) ;
#15392=ORIENTED_EDGE ( 'NONE', *, *, #41599, .T. ) ;
#15398=DIRECTION ( 'NONE',  ( -1.000000000000000000, 0.000000000000000000, 0.000000000000000000 ) ) ;
#15418=VECTOR ( 'NONE', #23595, 1000.000000000000000 ) ;
#15419=CARTESIAN_POINT ( 'NONE',  ( -9.942044687070568543, 9.234937905883914055, 455.0000000000000568 ) ) ;
#15448=AXIS2_PLACEMENT_3D ( 'NONE', #61467, #28264, #50176 ) ;
#15454=VECTOR ( 'NONE', #53792, 1000.000000000000000 ) ;
#15461=EDGE_CURVE ( 'NONE', #24433, #27223, #52671, .T. ) ;
#15468=ORIENTED_EDGE ( 'NONE', *, *, #53616, .T. ) ;
#15475=CARTESIAN_POINT ( 'NONE',  ( -7.603567055985589462, -8.606483450353362485, 195.0000000000000284 ) ) ;
#15480=ORIENTED_EDGE ( 'NONE', *, *, #52193, .T. ) ;
#15485=DIRECTION ( 'NONE',  ( 0.000000000000000000, 1.000000000000000000, 3.673940397442059868E-16 ) ) ;
#15491=CARTESIAN_POINT ( 'NONE',  ( 10.74648345035335240, 1.677516549646529409, 455.0000000000000568 ) ) ;
#15497=VERTEX_POINT ( 'NONE', #37100 ) ;
#15498=AXIS2_PLACEMENT_3D ( 'NONE', #2715, #34880, #23936 ) ;
#15506=LINE ( 'NONE', #37074, #45771 ) ;
#15507=FACE_OUTER_BOUND ( 'NONE', #37058, .T. ) ;
#15511=EDGE_CURVE ( 'NONE', #51738, #33976, #25593, .T. ) ;
#15514=CARTESIAN_POINT ( 'NONE',  ( 2.706483450353343478, -10.92648345035336632, 195.0000000000000284 ) ) ;
#15517=LINE ( 'NONE', #10197, #62894 ) ;
#15518=ADVANCED_FACE ( 'NONE', ( #30384 ), #31091, .F. ) ;
#15524=DIRECTION ( 'NONE',  ( -0.7071067811865474617, -0.7071067811865474617, 0.000000000000000000 ) ) ;
#15525=VERTEX_POINT ( 'NONE', #3867 ) ;
#15528=EDGE_CURVE ( 'NONE', #44833, #53484, #57950, .T. ) ;
#15533=EDGE_CURVE ( 'NONE', #14243, #2424, #4573, .T. ) ;
#15540=EDGE_CURVE ( 'NONE', #49641, #53142, #57252, .T. ) ;
#15541=FACE_OUTER_BOUND ( 'NONE', #5100, .T. ) ;
#15554=ORIENTED_EDGE ( 'NONE', *, *, #463, .F. ) ;
#15557=CIRCLE ( 'NONE', #68589, 1.399999999999999245 ) ;
#15563=CIRCLE ( 'NONE', #6516, 0.1999999999999987899 ) ;
#15567=PLANE ( 'NONE',  #46468 ) ;
#15575=ORIENTED_EDGE ( 'NONE', *, *, #53138, .T. ) ;
#15579=ORIENTED_EDGE ( 'NONE', *, *, #38462, .T. ) ;
#15588=ORIENTED_EDGE ( 'NONE', *, *, #68324, .F. ) ;
#15596=ORIENTED_EDGE ( 'NONE', *, *, #8172, .F. ) ;
#15598=FACE_OUTER_BOUND ( 'NONE', #63323, .T. ) ;
#15605=ADVANCED_FACE ( 'NONE', ( #10559 ), #5611, .F. ) ;
#15606=CARTESIAN_POINT ( 'NONE',  ( -9.791916549646819234, -11.08848345035330496, 195.0000000000000284 ) ) ;
#15610=LINE ( 'NONE', #22297, #61126 ) ;
#15615=AXIS2_PLACEMENT_3D ( 'NONE', #61848, #34955, #19058 ) ;
#15622=VERTEX_POINT ( 'NONE', #32131 ) ;
#15627=CARTESIAN_POINT ( 'NONE',  ( 11.48848345035334617, -11.08848345035339733, 195.0000000000000284 ) ) ;
#15641=EDGE_LOOP ( 'NONE', ( #37478, #9410, #27827, #39628 ) ) ;
#15642=CARTESIAN_POINT ( 'NONE',  ( 8.211283450353352720, 5.993516549646621172, 195.0000000000000284 ) ) ;
#15648=LINE ( 'NONE', #48865, #32913 ) ;
#15651=CIRCLE ( 'NONE', #55155, 0.1999999999999987899 ) ;
#15653=LINE ( 'NONE', #58077, #55767 ) ;
#15655=VECTOR ( 'NONE', #45053, 1000.000000000000000 ) ;
#15658=DIRECTION ( 'NONE',  ( 1.047444401652939849E-14, 1.000000000000000000, 1.836970198721029934E-16 ) ) ;
#15659=ORIENTED_EDGE ( 'NONE', *, *, #1441, .T. ) ;
#15669=ORIENTED_EDGE ( 'NONE', *, *, #14642, .T. ) ;
#15674=ORIENTED_EDGE ( 'NONE', *, *, #35566, .F. ) ;
#15676=LINE ( 'NONE', #31251, #27704 ) ;
#15677=EDGE_CURVE ( 'NONE', #31474, #59188, #27868, .T. ) ;
#15680=CARTESIAN_POINT ( 'NONE',  ( 9.417013320880721849, 1.853252480934663771, 195.0000000000000284 ) ) ;
#15685=VERTEX_POINT ( 'NONE', #40192 ) ;
#15689=DIRECTION ( 'NONE',  ( -1.836970198721029934E-16, -1.836970198721010706E-16, 1.000000000000000000 ) ) ;
#15690=EDGE_LOOP ( 'NONE', ( #47157, #59496, #46745, #52179 ) ) ;
#15696=AXIS2_PLACEMENT_3D ( 'NONE', #39456, #56419, #61014 ) ;
#15700=CIRCLE ( 'NONE', #24713, 0.2000000000000005107 ) ;
#15705=LINE ( 'NONE', #48232, #34004 ) ;
#15710=LINE ( 'NONE', #69445, #69513 ) ;
#15715=CARTESIAN_POINT ( 'NONE',  ( 9.955011587777235604, -9.247904806590705462, 195.0000000000000284 ) ) ;
#15717=EDGE_CURVE ( 'NONE', #52016, #42601, #12085, .T. ) ;
#15720=VECTOR ( 'NONE', #15261, 1000.000000000000000 ) ;
#15726=EDGE_CURVE ( 'NONE', #13793, #39563, #19972, .T. ) ;
#15729=ORIENTED_EDGE ( 'NONE', *, *, #39004, .F. ) ;
#15731=ORIENTED_EDGE ( 'NONE', *, *, #22871, .T. ) ;
#15737=DIRECTION ( 'NONE',  ( -1.836970198721029934E-16, 1.836970198721036344E-16, -1.000000000000000000 ) ) ;
#15741=EDGE_LOOP ( 'NONE', ( #35224, #44170, #57479, #53587 ) ) ;
#15742=CARTESIAN_POINT ( 'NONE',  ( -11.11351654964671098, 7.793516549646603231, 195.0000000000000284 ) ) ;
#15744=CARTESIAN_POINT ( 'NONE',  ( 10.20488345035338007, -11.48848345035349361, 455.0000000000000568 ) ) ;
#15747=EDGE_LOOP ( 'NONE', ( #48444, #37406, #19384, #19376 ) ) ;
#15769=EDGE_CURVE ( 'NONE', #56637, #37049, #50468, .T. ) ;
#15770=CARTESIAN_POINT ( 'NONE',  ( 11.32648345035338089, 4.393516549646522051, 455.0000000000000568 ) ) ;
#15771=DIRECTION ( 'NONE',  ( 0.000000000000000000, -3.673940397442059868E-16, 1.000000000000000000 ) ) ;
#15775=DIRECTION ( 'NONE',  ( 1.836970198721029934E-16, -1.836970198721036344E-16, 1.000000000000000000 ) ) ;
#15778=FACE_OUTER_BOUND ( 'NONE', #69135, .T. ) ;
#15780=VERTEX_POINT ( 'NONE', #45494 ) ;
#15782=LINE ( 'NONE', #10476, #18088 ) ;
#15784=AXIS2_PLACEMENT_3D ( 'NONE', #11881, #11537, #22175 ) ;
#15796=CARTESIAN_POINT ( 'NONE',  ( 4.740315990920131561, -7.811466277050838514, 455.0000000000000568 ) ) ;
#15803=AXIS2_PLACEMENT_3D ( 'NONE', #14573, #25186, #31209 ) ;
#15805=VERTEX_POINT ( 'NONE', #1667 ) ;
#15809=CARTESIAN_POINT ( 'NONE',  ( 9.306483450353379538, -10.92648345035339119, 195.0000000000000284 ) ) ;
#15810=VECTOR ( 'NONE', #31277, 1000.000000000000000 ) ;
#15814=CARTESIAN_POINT ( 'NONE',  ( -7.813516549646711162, 11.77351654964660277, 195.0000000000000284 ) ) ;
#15816=ORIENTED_EDGE ( 'NONE', *, *, #8336, .T. ) ;
#15819=LINE ( 'NONE', #24774, #41018 ) ;
#15820=CARTESIAN_POINT ( 'NONE',  ( -8.513516549646713116, 11.29351654964659701, 455.0000000000000568 ) ) ;
#15827=VERTEX_POINT ( 'NONE', #56123 ) ;
#15832=CIRCLE ( 'NONE', #6780, 0.2000000000000005107 ) ;
#15834=ORIENTED_EDGE ( 'NONE', *, *, #30121, .F. ) ;
#15838=DIRECTION ( 'NONE',  ( -0.6414496315691526895, -0.7671651518153038696, 0.000000000000000000 ) ) ;
#15846=ORIENTED_EDGE ( 'NONE', *, *, #67229, .T. ) ;
#15860=DIRECTION ( 'NONE',  ( -0.7071067811865475727, 0.7071067811865475727, 0.000000000000000000 ) ) ;
#15862=VERTEX_POINT ( 'NONE', #68124 ) ;
#15863=DIRECTION ( 'NONE',  ( -0.000000000000000000, -1.000000000000000000, -0.000000000000000000 ) ) ;
#15867=CARTESIAN_POINT ( 'NONE',  ( -7.252248008019509307, -5.393625297349935011, 455.0000000000000568 ) ) ;
#15868=CARTESIAN_POINT ( 'NONE',  ( 8.606483450353406894, 7.603567055985405609, 455.0000000000000568 ) ) ;
#15885=CARTESIAN_POINT ( 'NONE',  ( -7.798499376344062206, -4.740315990920112021, 195.0000000000000284 ) ) ;
#15888=CIRCLE ( 'NONE', #42979, 0.1999999999999987899 ) ;
#15892=VECTOR ( 'NONE', #35044, 1000.000000000000000 ) ;
#15901=AXIS2_PLACEMENT_3D ( 'NONE', #58866, #68416, #36957 ) ;
#15902=CARTESIAN_POINT ( 'NONE',  ( 11.78648345035337819, -4.406483450353490205, 455.0000000000000568 ) ) ;
#15908=EDGE_LOOP ( 'NONE', ( #64929, #11133, #44219, #891 ) ) ;
#15917=CIRCLE ( 'NONE', #45260, 0.1999999999999996503 ) ;
#15922=EDGE_LOOP ( 'NONE', ( #17155, #39043, #58807, #24493 ) ) ;
#15929=EDGE_CURVE ( 'NONE', #4544, #17779, #69176, .T. ) ;
#15939=VECTOR ( 'NONE', #19238, 1000.000000000000000 ) ;
#15941=ADVANCED_FACE ( 'NONE', ( #4140 ), #36649, .F. ) ;
#15945=DIRECTION ( 'NONE',  ( -1.000000000000000000, 0.000000000000000000, 0.000000000000000000 ) ) ;
#15948=ORIENTED_EDGE ( 'NONE', *, *, #36418, .T. ) ;
#15955=AXIS2_PLACEMENT_3D ( 'NONE', #34743, #34378, #13879 ) ;
#15958=CYLINDRICAL_SURFACE ( 'NONE', #4471, 1.399999999999998579 ) ;
#15965=DIRECTION ( 'NONE',  ( -8.728482790395504563E-15, -1.000000000000000000, 0.000000000000000000 ) ) ;
#15967=ORIENTED_EDGE ( 'NONE', *, *, #67389, .F. ) ;
#15968=DIRECTION ( 'NONE',  ( -0.7071067811865474617, -0.7071067811865474617, -0.000000000000000000 ) ) ;
#15978=DIRECTION ( 'NONE',  ( -1.261617073437657735E-14, -1.000000000000000000, 0.000000000000000000 ) ) ;
#15979=ORIENTED_EDGE ( 'NONE', *, *, #69083, .F. ) ;
#15980=EDGE_CURVE ( 'NONE', #34688, #32863, #4830, .T. ) ;
#15986=EDGE_CURVE ( 'NONE', #57095, #10322, #21783, .T. ) ;
#15987=CARTESIAN_POINT ( 'NONE',  ( 7.428221114745000797, 3.593516549646565750, 455.0000000000000568 ) ) ;
#15990=VECTOR ( 'NONE', #25248, 1000.000000000000000 ) ;
#15991=DIRECTION ( 'NONE',  ( -0.000000000000000000, -0.000000000000000000, -1.000000000000000000 ) ) ;
#15993=ORIENTED_EDGE ( 'NONE', *, *, #14015, .F. ) ;
#16002=LINE ( 'NONE', #21996, #2723 ) ;
#16019=ORIENTED_EDGE ( 'NONE', *, *, #32730, .F. ) ;
#16028=CARTESIAN_POINT ( 'NONE',  ( 11.12648345035336384, 2.893516549646526048, 455.0000000000000568 ) ) ;
#16035=DIRECTION ( 'NONE',  ( -1.000000000000000000, 0.000000000000000000, 0.000000000000000000 ) ) ;
#16039=FACE_OUTER_BOUND ( 'NONE', #10281, .T. ) ;
#16046=ORIENTED_EDGE ( 'NONE', *, *, #55043, .T. ) ;
#16048=DIRECTION ( 'NONE',  ( -0.7071067811865412445, 0.7071067811865537900, 0.000000000000000000 ) ) ;
#16058=EDGE_CURVE ( 'NONE', #24181, #37207, #38393, .T. ) ;
#16062=EDGE_CURVE ( 'NONE', #59053, #33806, #15557, .T. ) ;
#16067=EDGE_LOOP ( 'NONE', ( #56955, #8422, #3984, #65561 ) ) ;
#16071=CARTESIAN_POINT ( 'NONE',  ( 3.606483450353380249, -4.622483450353491286, 455.0000000000000568 ) ) ;
#16072=CARTESIAN_POINT ( 'NONE',  ( 4.201500623656004407, 4.727349090213385452, 195.0000000000000284 ) ) ;
#16080=CYLINDRICAL_SURFACE ( 'NONE', #47023, 0.2000000000000000944 ) ;
#16082=VERTEX_POINT ( 'NONE', #24485 ) ;
#16084=VECTOR ( 'NONE', #3781, 1000.000000000000000 ) ;
#16089=LINE ( 'NONE', #48616, #43341 ) ;
#16094=CIRCLE ( 'NONE', #295, 0.1999999999999987899 ) ;
#16095=DIRECTION ( 'NONE',  ( 1.047444401652939849E-14, 1.000000000000000000, 0.000000000000000000 ) ) ;
#16110=EDGE_CURVE ( 'NONE', #56637, #14683, #69758, .T. ) ;
#16119=DIRECTION ( 'NONE',  ( 1.836970198721029934E-16, -1.836970198721036344E-16, 1.000000000000000000 ) ) ;
#16121=EDGE_LOOP ( 'NONE', ( #17887, #5342, #23515, #41306 ) ) ;
#16122=CARTESIAN_POINT ( 'NONE',  ( 7.616533956692213003, -8.606483450353492159, 455.0000000000000568 ) ) ;
#16124=CARTESIAN_POINT ( 'NONE',  ( 7.606483450353424658, 11.77351654964657435, 455.0000000000000568 ) ) ;
#16128=CARTESIAN_POINT ( 'NONE',  ( 4.186483450353375879, 11.77351654964663119, 195.0000000000000284 ) ) ;
#16129=CIRCLE ( 'NONE', #64684, 0.5999999999999989786 ) ;
#16132=EDGE_CURVE ( 'NONE', #58549, #22374, #24122, .T. ) ;
#16135=LINE ( 'NONE', #64242, #17250 ) ;
#16139=VERTEX_POINT ( 'NONE', #51341 ) ;
#16145=CARTESIAN_POINT ( 'NONE',  ( -9.942044687070568543, 2.752095193409294982, 455.0000000000000568 ) ) ;
#16150=ORIENTED_EDGE ( 'NONE', *, *, #15282, .T. ) ;
#16153=EDGE_CURVE ( 'NONE', #27405, #30268, #18819, .T. ) ;
#16160=CARTESIAN_POINT ( 'NONE',  ( 11.34648345035338046, -1.090483450353395334, 195.0000000000000284 ) ) ;
#16167=ORIENTED_EDGE ( 'NONE', *, *, #26858, .T. ) ;
#16168=CARTESIAN_POINT ( 'NONE',  ( 9.804883450353409913, 11.07551654964657928, 195.0000000000000284 ) ) ;
#16170=DIRECTION ( 'NONE',  ( 0.000000000000000000, -1.000000000000000000, 0.000000000000000000 ) ) ;
#16174=CARTESIAN_POINT ( 'NONE',  ( 11.78648345035333200, 4.173516549646566709, 195.0000000000000284 ) ) ;
#16175=DIRECTION ( 'NONE',  ( -1.836970198721029934E-16, 1.836970198721036344E-16, -1.000000000000000000 ) ) ;
#16182=CIRCLE ( 'NONE', #35330, 0.5999999999999998668 ) ;
#16193=ORIENTED_EDGE ( 'NONE', *, *, #4315, .F. ) ;
#16194=EDGE_CURVE ( 'NONE', #68881, #10422, #46009, .T. ) ;
#16196=DIRECTION ( 'NONE',  ( -1.000000000000000000, -0.000000000000000000, -0.000000000000000000 ) ) ;
#16199=AXIS2_PLACEMENT_3D ( 'NONE', #21470, #38436, #11880 ) ;
#16202=ORIENTED_EDGE ( 'NONE', *, *, #19130, .T. ) ;
#16205=CARTESIAN_POINT ( 'NONE',  ( 4.186483450353422953, 11.77351654964658501, 455.0000000000000568 ) ) ;
#16208=DIRECTION ( 'NONE',  ( 8.673617379884051249E-15, 1.000000000000000000, 0.000000000000000000 ) ) ;
#16212=ORIENTED_EDGE ( 'NONE', *, *, #4662, .F. ) ;
#16214=CARTESIAN_POINT ( 'NONE',  ( 4.622483450353346512, 3.593516549646634584, 195.0000000000000284 ) ) ;
#16223=DIRECTION ( 'NONE',  ( -1.836970198721029934E-16, 1.836970198721036344E-16, -1.000000000000000000 ) ) ;
#16231=EDGE_LOOP ( 'NONE', ( #13534, #40130, #31145, #41556 ) ) ;
#16233=VERTEX_POINT ( 'NONE', #8198 ) ;
#16235=ORIENTED_EDGE ( 'NONE', *, *, #47993, .F. ) ;
#16263=VERTEX_POINT ( 'NONE', #26228 ) ;
#16264=VECTOR ( 'NONE', #43075, 1000.000000000000000 ) ;
#16267=DIRECTION ( 'NONE',  ( 1.000000000000000000, 0.000000000000000000, 0.000000000000000000 ) ) ;
#16279=LINE ( 'NONE', #43146, #3410 ) ;
#16281=CARTESIAN_POINT ( 'NONE',  ( 11.08848345035336891, 9.791916549646611401, 195.0000000000000284 ) ) ;
#16296=CARTESIAN_POINT ( 'NONE',  ( -5.993516549646711766, 5.993516549646603409, 455.0000000000000568 ) ) ;
#16299=CARTESIAN_POINT ( 'NONE',  ( -9.942044687070668019, -9.247904806590694804, 455.0000000000000568 ) ) ;
#16305=FACE_OUTER_BOUND ( 'NONE', #69777, .T. ) ;
#16312=DIRECTION ( 'NONE',  ( -0.000000000000000000, 3.673940397442059868E-16, -1.000000000000000000 ) ) ;
#16319=ORIENTED_EDGE ( 'NONE', *, *, #53046, .T. ) ;
#16322=ORIENTED_EDGE ( 'NONE', *, *, #41065, .T. ) ;
#16324=ORIENTED_EDGE ( 'NONE', *, *, #35797, .T. ) ;
#16334=ORIENTED_EDGE ( 'NONE', *, *, #20849, .F. ) ;
#16335=EDGE_CURVE ( 'NONE', #32863, #27141, #53458, .T. ) ;
#16337=CARTESIAN_POINT ( 'NONE',  ( 7.272650909786598561, -4.201500623656027500, 195.0000000000000284 ) ) ;
#16340=CIRCLE ( 'NONE', #43428, 2.204799999999997429 ) ;
#16342=DIRECTION ( 'NONE',  ( -0.8660254037844400399, -0.4999999999999973910, 6.723777587268495961E-17 ) ) ;
#16348=ORIENTED_EDGE ( 'NONE', *, *, #52733, .F. ) ;
#16353=FACE_OUTER_BOUND ( 'NONE', #6627, .T. ) ;
#16363=EDGE_CURVE ( 'NONE', #57794, #22125, #58049, .T. ) ;
#16371=LINE ( 'NONE', #48905, #8768 ) ;
#16376=ORIENTED_EDGE ( 'NONE', *, *, #11601, .F. ) ;
#16378=DIRECTION ( 'NONE',  ( -0.000000000000000000, 3.673940397442059868E-16, -1.000000000000000000 ) ) ;
#16379=EDGE_CURVE ( 'NONE', #68417, #33912, #24109, .T. ) ;
#16389=ADVANCED_FACE ( 'NONE', ( #26933 ), #54152, .F. ) ;
#16393=CARTESIAN_POINT ( 'NONE',  ( -1.853252480934758584, 9.404046420173985510, 455.0000000000000568 ) ) ;
#16395=VECTOR ( 'NONE', #23089, 1000.000000000000000 ) ;
#16397=EDGE_CURVE ( 'NONE', #48542, #17390, #38912, .T. ) ;
#16403=CIRCLE ( 'NONE', #35556, 0.5999999999999998668 ) ;
#16404=CIRCLE ( 'NONE', #55909, 0.1999999999999987899 ) ;
#16406=EDGE_CURVE ( 'NONE', #21711, #1336, #33270, .T. ) ;
#16408=FACE_OUTER_BOUND ( 'NONE', #24871, .T. ) ;
#16410=EDGE_CURVE ( 'NONE', #33631, #2837, #46676, .T. ) ;
#16413=VECTOR ( 'NONE', #22865, 1000.000000000000000 ) ;
#16421=EDGE_CURVE ( 'NONE', #16514, #67467, #64751, .T. ) ;
#16423=DIRECTION ( 'NONE',  ( -1.000000000000000000, -1.570596175624152290E-15, 0.000000000000000000 ) ) ;
#16427=DIRECTION ( 'NONE',  ( -1.000000000000000000, 1.828336019306068695E-14, -1.836970198720996407E-16 ) ) ;
#16428=CARTESIAN_POINT ( 'NONE',  ( -4.193516549646675529, 11.11351654964658842, 455.0000000000000568 ) ) ;
#16430=ORIENTED_EDGE ( 'NONE', *, *, #66758, .F. ) ;
#16437=DIRECTION ( 'NONE',  ( 0.4999999999999973910, -0.8660254037844401509, -2.509347957447878791E-16 ) ) ;
#16442=AXIS2_PLACEMENT_3D ( 'NONE', #32803, #49068, #994 ) ;
#16453=ORIENTED_EDGE ( 'NONE', *, *, #46788, .T. ) ;
#16458=VECTOR ( 'NONE', #59500, 1000.000000000000000 ) ;
#16468=VECTOR ( 'NONE', #21489, 1000.000000000000000 ) ;
#16485=DIRECTION ( 'NONE',  ( 0.6414496315691619044, -0.7671651518152962090, 0.000000000000000000 ) ) ;
#16494=DIRECTION ( 'NONE',  ( -1.000000000000000000, 0.000000000000000000, 0.000000000000000000 ) ) ;
#16498=VECTOR ( 'NONE', #6824, 1000.000000000000000 ) ;
#16500=CYLINDRICAL_SURFACE ( 'NONE', #58814, 0.3999999999999993006 ) ;
#16506=VERTEX_POINT ( 'NONE', #8110 ) ;
#16507=CARTESIAN_POINT ( 'NONE',  ( 7.606483450353424658, 11.77351654964657435, 455.0000000000000568 ) ) ;
#16510=EDGE_CURVE ( 'NONE', #6826, #13374, #52346, .T. ) ;
#16511=AXIS2_PLACEMENT_3D ( 'NONE', #68813, #58907, #52919 ) ;
#16514=VERTEX_POINT ( 'NONE', #8460 ) ;
#16530=EDGE_LOOP ( 'NONE', ( #9629, #47628, #41732, #6184 ) ) ;
#16534=CARTESIAN_POINT ( 'NONE',  ( 1.690483450353344352, -10.74648345035345720, 455.0000000000000568 ) ) ;
#16547=ADVANCED_FACE ( 'NONE', ( #23679 ), #24742, .F. ) ;
#16550=DIRECTION ( 'NONE',  ( 1.836970198721029934E-16, 1.836970198721010706E-16, -1.000000000000000000 ) ) ;
#16557=VECTOR ( 'NONE', #48850, 999.9999999999998863 ) ;
#16569=AXIS2_PLACEMENT_3D ( 'NONE', #59761, #48814, #11313 ) ;
#16573=DIRECTION ( 'NONE',  ( 1.836970198721029934E-16, 1.836970198721010706E-16, -1.000000000000000000 ) ) ;
#16575=LINE ( 'NONE', #32822, #69500 ) ;
#16589=DIRECTION ( 'NONE',  ( -1.610765207321970913E-14, -1.000000000000000000, -1.836970198721006761E-16 ) ) ;
#16595=CARTESIAN_POINT ( 'NONE',  ( -2.277516549646682709, 9.828310488885916740, 455.0000000000000568 ) ) ;
#16607=AXIS2_PLACEMENT_3D ( 'NONE', #59685, #69941, #64301 ) ;
#16614=CIRCLE ( 'NONE', #69665, 0.2000000000000005107 ) ;
#16618=CARTESIAN_POINT ( 'NONE',  ( -7.593516549646831315, -11.32648345035340931, 455.0000000000000568 ) ) ;
#16631=AXIS2_PLACEMENT_3D ( 'NONE', #23569, #60709, #12598 ) ;
#16633=CIRCLE ( 'NONE', #42612, 1.399999999999998579 ) ;
#16635=ORIENTED_EDGE ( 'NONE', *, *, #50212, .T. ) ;
#16646=PLANE ( 'NONE',  #7490 ) ;
#16649=DIRECTION ( 'NONE',  ( -0.000000000000000000, 3.673940397442059868E-16, -1.000000000000000000 ) ) ;
#16669=CARTESIAN_POINT ( 'NONE',  ( 10.92648345035340895, 9.293516549646565039, 455.0000000000000568 ) ) ;
#16670=ORIENTED_EDGE ( 'NONE', *, *, #30793, .F. ) ;
#16674=EDGE_LOOP ( 'NONE', ( #16856, #38623, #48489, #14343 ) ) ;
#16675=CARTESIAN_POINT ( 'NONE',  ( 8.406483450353398723, 5.655420232009111814, 455.0000000000000568 ) ) ;
#16676=LINE ( 'NONE', #37889, #63339 ) ;
#16679=CARTESIAN_POINT ( 'NONE',  ( -7.798499376344067535, 7.259684009079840017, 195.0000000000000284 ) ) ;
#16694=CARTESIAN_POINT ( 'NONE',  ( 9.247904806590677040, 9.942044687070474396, 195.0000000000000284 ) ) ;
#16697=DIRECTION ( 'NONE',  ( 0.000000000000000000, 0.000000000000000000, 1.000000000000000000 ) ) ;
#16699=DIRECTION ( 'NONE',  ( -1.000000000000000000, 0.000000000000000000, 0.000000000000000000 ) ) ;
#16712=VECTOR ( 'NONE', #34295, 1000.000000000000000 ) ;
#16714=CARTESIAN_POINT ( 'NONE',  ( -1.077516549646825750, -10.74648345035347852, 455.0000000000000568 ) ) ;
#16716=AXIS2_PLACEMENT_3D ( 'NONE', #12693, #33248, #22973 ) ;
#16719=PLANE ( 'NONE',  #30558 ) ;
#16724=ORIENTED_EDGE ( 'NONE', *, *, #8172, .T. ) ;
#16726=DIRECTION ( 'NONE',  ( 1.000000000000000000, 0.000000000000000000, 0.000000000000000000 ) ) ;
#16728=EDGE_CURVE ( 'NONE', #29102, #56223, #9179, .T. ) ;
#16734=VERTEX_POINT ( 'NONE', #9531 ) ;
#16737=CARTESIAN_POINT ( 'NONE',  ( 10.92648345035340895, 9.093516549646565750, 455.0000000000000568 ) ) ;
#16742=EDGE_CURVE ( 'NONE', #40491, #38948, #68221, .T. ) ;
#16748=DIRECTION ( 'NONE',  ( 1.836970198721029934E-16, 1.836970198721010706E-16, -1.000000000000000000 ) ) ;
#16752=CARTESIAN_POINT ( 'NONE',  ( -11.07551654964683330, -11.48848345035333907, 455.0000000000000568 ) ) ;
#16753=ORIENTED_EDGE ( 'NONE', *, *, #41560, .F. ) ;
#16765=DIRECTION ( 'NONE',  ( -0.000000000000000000, 3.673940397442059868E-16, -1.000000000000000000 ) ) ;
#16769=CYLINDRICAL_SURFACE ( 'NONE', #4651, 0.2000000000000000944 ) ;
#16777=EDGE_LOOP ( 'NONE', ( #5991, #16670, #10113, #15669 ) ) ;
#16778=CARTESIAN_POINT ( 'NONE',  ( 8.406483450353348985, 5.655420232009159776, 195.0000000000000284 ) ) ;
#16780=ORIENTED_EDGE ( 'NONE', *, *, #24857, .F. ) ;
#16792=EDGE_CURVE ( 'NONE', #11614, #66887, #42750, .T. ) ;
#16801=ORIENTED_EDGE ( 'NONE', *, *, #60194, .F. ) ;
#16808=CARTESIAN_POINT ( 'NONE',  ( -10.19191654964671301, 11.47551654964660450, 195.0000000000000284 ) ) ;
#16828=CARTESIAN_POINT ( 'NONE',  ( 9.417013320880792904, -1.866219381641466057, 195.0000000000000284 ) ) ;
#16831=ORIENTED_EDGE ( 'NONE', *, *, #3376, .F. ) ;
#16837=DIRECTION ( 'NONE',  ( -0.000000000000000000, 3.673940397442059868E-16, -1.000000000000000000 ) ) ;
#16853=VECTOR ( 'NONE', #18805, 1000.000000000000000 ) ;
#16854=DIRECTION ( 'NONE',  ( -1.000000000000000000, 3.491481338843132961E-15, 0.000000000000000000 ) ) ;
#16856=ORIENTED_EDGE ( 'NONE', *, *, #64283, .T. ) ;
#16863=VERTEX_POINT ( 'NONE', #59707 ) ;
#16866=CARTESIAN_POINT ( 'NONE',  ( -7.813516549646791098, -12.00648345035336284, 195.0000000000000284 ) ) ;
#16875=ORIENTED_EDGE ( 'NONE', *, *, #31040, .F. ) ;
#16886=CIRCLE ( 'NONE', #27076, 0.2000000000000000944 ) ;
#16887=ORIENTED_EDGE ( 'NONE', *, *, #19970, .T. ) ;
#16892=EDGE_CURVE ( 'NONE', #55579, #62792, #45507, .T. ) ;
#16896=EDGE_CURVE ( 'NONE', #60141, #49441, #12277, .T. ) ;
#16903=AXIS2_PLACEMENT_3D ( 'NONE', #30736, #7756, #61860 ) ;
#16917=CARTESIAN_POINT ( 'NONE',  ( 8.606483450353380249, -4.396432944014657451, 455.0000000000000568 ) ) ;
#16927=CARTESIAN_POINT ( 'NONE',  ( -4.188533722949335569, 4.727349090213398775, 455.0000000000000568 ) ) ;
#16929=EDGE_CURVE ( 'NONE', #52471, #40712, #54662, .T. ) ;
#16935=ORIENTED_EDGE ( 'NONE', *, *, #69083, .T. ) ;
#16938=ADVANCED_FACE ( 'NONE', ( #17941 ), #66032, .F. ) ;
#16944=ORIENTED_EDGE ( 'NONE', *, *, #56914, .F. ) ;
#16957=VECTOR ( 'NONE', #69266, 1000.000000000000000 ) ;
#16963=CARTESIAN_POINT ( 'NONE',  ( -4.173516549646666185, 11.99351654964658920, 455.0000000000000568 ) ) ;
#16972=AXIS2_PLACEMENT_3D ( 'NONE', #27052, #38698, #17132 ) ;
#16979=ORIENTED_EDGE ( 'NONE', *, *, #36737, .F. ) ;
#16986=FACE_OUTER_BOUND ( 'NONE', #41758, .T. ) ;
#16989=DIRECTION ( 'NONE',  ( -1.836970198721029934E-16, 1.836970198721036344E-16, -1.000000000000000000 ) ) ;
#17005=ORIENTED_EDGE ( 'NONE', *, *, #67855, .F. ) ;
#17009=AXIS2_PLACEMENT_3D ( 'NONE', #4846, #4506, #31728 ) ;
#17013=CARTESIAN_POINT ( 'NONE',  ( -7.593516549646711411, 11.77351654964660277, 195.0000000000000284 ) ) ;
#17032=LINE ( 'NONE', #66497, #5546 ) ;
#17046=CARTESIAN_POINT ( 'NONE',  ( -11.77351654964674132, -4.186483450353323477, 455.0000000000000568 ) ) ;
#17047=AXIS2_PLACEMENT_3D ( 'NONE', #50364, #29491, #61302 ) ;
#17057=VECTOR ( 'NONE', #26428, 1000.000000000000000 ) ;
#17060=DIRECTION ( 'NONE',  ( -0.000000000000000000, -0.000000000000000000, -1.000000000000000000 ) ) ;
#17063=DIRECTION ( 'NONE',  ( -4.336808689942043768E-15, -1.000000000000000000, 0.000000000000000000 ) ) ;
#17066=ORIENTED_EDGE ( 'NONE', *, *, #61297, .F. ) ;
#17069=ADVANCED_FACE ( 'NONE', ( #57524 ), #3784, .T. ) ;
#17074=EDGE_CURVE ( 'NONE', #31922, #29982, #46209, .T. ) ;
#17080=CARTESIAN_POINT ( 'NONE',  ( -7.593516549646831315, -11.32648345035340931, 455.0000000000000568 ) ) ;
#17081=VECTOR ( 'NONE', #40521, 1000.000000000000000 ) ;
#17084=LINE ( 'NONE', #31970, #60808 ) ;
#17085=ORIENTED_EDGE ( 'NONE', *, *, #62125, .F. ) ;
#17092=DIRECTION ( 'NONE',  ( -1.836970198721029934E-16, 1.836970198721036344E-16, -1.000000000000000000 ) ) ;
#17098=DIRECTION ( 'NONE',  ( 1.000000000000000000, 0.000000000000000000, 0.000000000000000000 ) ) ;
#17100=AXIS2_PLACEMENT_3D ( 'NONE', #15987, #5732, #33287 ) ;
#17104=DIRECTION ( 'NONE',  ( -0.7671651518153006499, 0.6414496315691565753, -0.000000000000000000 ) ) ;
#17112=ORIENTED_EDGE ( 'NONE', *, *, #65745, .F. ) ;
#17124=LINE ( 'NONE', #49643, #3832 ) ;
#17130=ORIENTED_EDGE ( 'NONE', *, *, #15528, .T. ) ;
#17132=DIRECTION ( 'NONE',  ( -1.000000000000000000, 0.000000000000000000, 0.000000000000000000 ) ) ;
#17143=CARTESIAN_POINT ( 'NONE',  ( 9.106483450353380249, -10.09643294401465852, 455.0000000000000568 ) ) ;
#17151=ORIENTED_EDGE ( 'NONE', *, *, #42005, .F. ) ;
#17155=ORIENTED_EDGE ( 'NONE', *, *, #45062, .T. ) ;
#17175=CARTESIAN_POINT ( 'NONE',  ( -10.91351654964666373, -2.706483450353290632, 195.0000000000000284 ) ) ;
#17178=LINE ( 'NONE', #39433, #49207 ) ;
#17182=ORIENTED_EDGE ( 'NONE', *, *, #40628, .T. ) ;
#17184=DIRECTION ( 'NONE',  ( 0.000000000000000000, 1.000000000000000000, 0.000000000000000000 ) ) ;
#17188=AXIS2_PLACEMENT_3D ( 'NONE', #23723, #66850, #29370 ) ;
#17191=VECTOR ( 'NONE', #9378, 1000.000000000000000 ) ;
#17194=ORIENTED_EDGE ( 'NONE', *, *, #38807, .T. ) ;
#17195=CARTESIAN_POINT ( 'NONE',  ( -11.29351654964668583, 8.513516549646642062, 455.0000000000000568 ) ) ;
#17197=ORIENTED_EDGE ( 'NONE', *, *, #25331, .F. ) ;
#17200=LINE ( 'NONE', #38438, #44033 ) ;
#17201=CARTESIAN_POINT ( 'NONE',  ( 2.290483450353350658, -9.841277389592804070, 455.0000000000000568 ) ) ;
#17204=EDGE_LOOP ( 'NONE', ( #29439, #39522, #29152, #43388 ) ) ;
#17206=VECTOR ( 'NONE', #64656, 1000.000000000000000 ) ;
#17208=ORIENTED_EDGE ( 'NONE', *, *, #59192, .F. ) ;
#17214=VERTEX_POINT ( 'NONE', #48671 ) ;
#17220=ADVANCED_FACE ( 'NONE', ( #59629 ), #54328, .F. ) ;
#17224=EDGE_CURVE ( 'NONE', #62302, #49054, #32416, .T. ) ;
#17225=DIRECTION ( 'NONE',  ( -1.836970198721029934E-16, 1.836970198721036344E-16, -1.000000000000000000 ) ) ;
#17231=CIRCLE ( 'NONE', #9377, 1.399999999999998579 ) ;
#17240=DIRECTION ( 'NONE',  ( 1.280238727658158432E-15, 1.000000000000000000, -0.000000000000000000 ) ) ;
#17246=LINE ( 'NONE', #38487, #7704 ) ;
#17248=LINE ( 'NONE', #28212, #45410 ) ;
#17250=VECTOR ( 'NONE', #69877, 1000.000000000000000 ) ;
#17262=LINE ( 'NONE', #1355, #30847 ) ;
#17279=EDGE_CURVE ( 'NONE', #39563, #56637, #58931, .T. ) ;
#17281=ORIENTED_EDGE ( 'NONE', *, *, #26621, .T. ) ;
#17290=ORIENTED_EDGE ( 'NONE', *, *, #30941, .T. ) ;
#17295=DIRECTION ( 'NONE',  ( 0.8660254037844322683, -0.5000000000000111022, 6.723777587268230953E-17 ) ) ;
#17311=EDGE_CURVE ( 'NONE', #29254, #60848, #13611, .T. ) ;
#17313=FACE_OUTER_BOUND ( 'NONE', #17533, .T. ) ;
#17324=LINE ( 'NONE', #42817, #15454 ) ;
#17327=CARTESIAN_POINT ( 'NONE',  ( 12.00648345035337883, -11.19368345035338308, 195.0000000000000284 ) ) ;
#17329=CARTESIAN_POINT ( 'NONE',  ( 9.841277389592693936, 1.677516549646539623, 455.0000000000000568 ) ) ;
#17330=CARTESIAN_POINT ( 'NONE',  ( -9.791916549646712653, 11.07551654964660415, 195.0000000000000284 ) ) ;
#17332=LINE ( 'NONE', #28632, #58138 ) ;
#17336=VERTEX_POINT ( 'NONE', #18924 ) ;
#17341=CARTESIAN_POINT ( 'NONE',  ( -11.18071654964669648, 11.18071654964658812, 195.0000000000000284 ) ) ;
#17345=CARTESIAN_POINT ( 'NONE',  ( 11.08848345035334404, -10.20488345035343336, 195.0000000000000284 ) ) ;
#17348=LINE ( 'NONE', #60483, #4411 ) ;
#17355=VECTOR ( 'NONE', #63963, 999.9999999999998863 ) ;
#17363=ADVANCED_FACE ( 'NONE', ( #6583 ), #62039, .F. ) ;
#17364=EDGE_LOOP ( 'NONE', ( #51597, #58737, #37414, #47368 ) ) ;
#17365=ORIENTED_EDGE ( 'NONE', *, *, #46194, .F. ) ;
#17370=ADVANCED_FACE ( 'NONE', ( #39770 ), #2647, .F. ) ;
#17377=EDGE_LOOP ( 'NONE', ( #30040, #58550, #21594, #55961 ) ) ;
#17383=ORIENTED_EDGE ( 'NONE', *, *, #35709, .T. ) ;
#17389=ORIENTED_EDGE ( 'NONE', *, *, #9919, .T. ) ;
#17390=VERTEX_POINT ( 'NONE', #44378 ) ;
#17392=DIRECTION ( 'NONE',  ( 0.000000000000000000, 1.000000000000000000, 0.000000000000000000 ) ) ;
#17396=VECTOR ( 'NONE', #25220, 1000.000000000000000 ) ;
#17397=DIRECTION ( 'NONE',  ( -1.000000000000000000, 0.000000000000000000, 0.000000000000000000 ) ) ;
#17400=ORIENTED_EDGE ( 'NONE', *, *, #51134, .F. ) ;
#17406=DIRECTION ( 'NONE',  ( -4.336808689942025625E-15, -1.000000000000000000, 0.000000000000000000 ) ) ;
#17413=EDGE_LOOP ( 'NONE', ( #47758, #17587, #4100, #55326 ) ) ;
#17419=VECTOR ( 'NONE', #29574, 1000.000000000000000 ) ;
#17420=ADVANCED_FACE ( 'NONE', ( #12552 ), #55700, .F. ) ;
#17423=CARTESIAN_POINT ( 'NONE',  ( 5.393625297349902148, 4.734785091273877811, 195.0000000000000284 ) ) ;
#17426=VERTEX_POINT ( 'NONE', #30578 ) ;
#17430=CARTESIAN_POINT ( 'NONE',  ( -7.252248008019455128, 6.606374702650072983, 195.0000000000000284 ) ) ;
#17434=CARTESIAN_POINT ( 'NONE',  ( -11.77351654964670935, 7.813516549646603693, 195.0000000000000284 ) ) ;
#17437=VECTOR ( 'NONE', #36546, 1000.000000000000000 ) ;
#17440=CARTESIAN_POINT ( 'NONE',  ( 10.20488345035345645, 11.07551654964652954, 455.0000000000000568 ) ) ;
#17445=VECTOR ( 'NONE', #56394, 1000.000000000000000 ) ;
#17447=LINE ( 'NONE', #28399, #65358 ) ;
#17450=CARTESIAN_POINT ( 'NONE',  ( -8.452095193409402185, 4.242044687070461784, 455.0000000000000568 ) ) ;
#17452=ADVANCED_FACE ( 'NONE', ( #67702 ), #63459, .F. ) ;
#17468=AXIS2_PLACEMENT_3D ( 'NONE', #5444, #24975, #59162 ) ;
#17469=ORIENTED_EDGE ( 'NONE', *, *, #14109, .F. ) ;
#17474=ORIENTED_EDGE ( 'NONE', *, *, #15511, .T. ) ;
#17479=LINE ( 'NONE', #55325, #58242 ) ;
#17481=CARTESIAN_POINT ( 'NONE',  ( 7.428221114744952835, 3.593516549646614155, 195.0000000000000284 ) ) ;
#17484=VECTOR ( 'NONE', #11276, 1000.000000000000000 ) ;
#17486=AXIS2_PLACEMENT_3D ( 'NONE', #33020, #39696, #17098 ) ;
#17491=ORIENTED_EDGE ( 'NONE', *, *, #6029, .T. ) ;
#17494=VECTOR ( 'NONE', #18683, 1000.000000000000000 ) ;
#17498=VECTOR ( 'NONE', #68259, 1000.000000000000114 ) ;
#17520=DIRECTION ( 'NONE',  ( -1.000000000000000000, 0.000000000000000000, 0.000000000000000000 ) ) ;
#17521=ORIENTED_EDGE ( 'NONE', *, *, #24120, .T. ) ;
#17522=CARTESIAN_POINT ( 'NONE',  ( 4.406483450353335662, -11.78648345035347766, 455.0000000000000568 ) ) ;
#17532=AXIS2_PLACEMENT_3D ( 'NONE', #61423, #45168, #67803 ) ;
#17533=EDGE_LOOP ( 'NONE', ( #4720, #17708, #51546, #23615 ) ) ;
#17537=ORIENTED_EDGE ( 'NONE', *, *, #27414, .F. ) ;
#17543=AXIS2_PLACEMENT_3D ( 'NONE', #26026, #68096, #47579 ) ;
#17550=VECTOR ( 'NONE', #29613, 1000.000000000000000 ) ;
#17553=ORIENTED_EDGE ( 'NONE', *, *, #23665, .T. ) ;
#17554=ORIENTED_EDGE ( 'NONE', *, *, #1802, .T. ) ;
#17557=EDGE_CURVE ( 'NONE', #30268, #22923, #49150, .T. ) ;
#17562=CARTESIAN_POINT ( 'NONE',  ( 9.804883450353379715, -11.08848345035339733, 195.0000000000000284 ) ) ;
#17563=CARTESIAN_POINT ( 'NONE',  ( -2.693516549646682190, 10.08346604330774454, 195.0000000000000284 ) ) ;
#17571=DIRECTION ( 'NONE',  ( 0.8660254037844363761, -0.5000000000000038858, -1.836970198721044232E-16 ) ) ;
#17575=ORIENTED_EDGE ( 'NONE', *, *, #3846, .T. ) ;
#17583=ADVANCED_FACE ( 'NONE', ( #27026 ), #37290, .T. ) ;
#17586=ADVANCED_FACE ( 'NONE', ( #5111 ), #43968, .F. ) ;
#17587=ORIENTED_EDGE ( 'NONE', *, *, #24974, .F. ) ;
#17589=PLANE ( 'NONE',  #29344 ) ;
#17603=CARTESIAN_POINT ( 'NONE',  ( -3.593516549646714520, -4.622483450353405132, 195.0000000000000284 ) ) ;
#17609=CARTESIAN_POINT ( 'NONE',  ( 7.272650909786597673, 7.798499376343980494, 195.0000000000000284 ) ) ;
#17610=FACE_OUTER_BOUND ( 'NONE', #40695, .T. ) ;
#17624=LINE ( 'NONE', #13002, #9288 ) ;
#17626=EDGE_CURVE ( 'NONE', #325, #44836, #69817, .T. ) ;
#17636=ORIENTED_EDGE ( 'NONE', *, *, #25504, .T. ) ;
#17644=FACE_OUTER_BOUND ( 'NONE', #51818, .T. ) ;
#17645=AXIS2_PLACEMENT_3D ( 'NONE', #44272, #5078, #5779 ) ;
#17649=ORIENTED_EDGE ( 'NONE', *, *, #24208, .T. ) ;
#17653=AXIS2_PLACEMENT_3D ( 'NONE', #28033, #6793, #49593 ) ;
#17661=VERTEX_POINT ( 'NONE', #48941 ) ;
#17664=AXIS2_PLACEMENT_3D ( 'NONE', #2610, #24184, #24543 ) ;
#17665=CARTESIAN_POINT ( 'NONE',  ( 3.606483450353369147, -7.428221114745098497, 455.0000000000000568 ) ) ;
#17668=CARTESIAN_POINT ( 'NONE',  ( -4.734785091274032354, -5.393625297349961656, 455.0000000000000568 ) ) ;
#17669=EDGE_CURVE ( 'NONE', #62844, #23208, #48591, .T. ) ;
#17670=DIRECTION ( 'NONE',  ( 1.000000000000000000, -6.508391731846280553E-15, -1.836970198721042260E-16 ) ) ;
#17674=EDGE_LOOP ( 'NONE', ( #67475, #41583, #37656, #65747 ) ) ;
#17675=CARTESIAN_POINT ( 'NONE',  ( -6.331612867284154511, 8.393516549646601987, 455.0000000000000568 ) ) ;
#17683=CARTESIAN_POINT ( 'NONE',  ( 12.00648345035338060, -4.186483450353492231, 455.0000000000000568 ) ) ;
#17694=CARTESIAN_POINT ( 'NONE',  ( -1.853252480934834745, -9.417013320880835536, 195.0000000000000284 ) ) ;
#17695=EDGE_CURVE ( 'NONE', #37001, #4376, #54801, .T. ) ;
#17701=DIRECTION ( 'NONE',  ( -0.000000000000000000, -0.000000000000000000, 1.000000000000000000 ) ) ;
#17706=VERTEX_POINT ( 'NONE', #44647 ) ;
#17708=ORIENTED_EDGE ( 'NONE', *, *, #25504, .F. ) ;
#17710=CARTESIAN_POINT ( 'NONE',  ( -5.380658396643233310, 7.252248008019342329, 455.0000000000000568 ) ) ;
#17733=ORIENTED_EDGE ( 'NONE', *, *, #46302, .F. ) ;
#17736=EDGE_CURVE ( 'NONE', #57882, #31408, #51008, .T. ) ;
#17739=DIRECTION ( 'NONE',  ( -1.836970198721029934E-16, 1.836970198721036344E-16, -1.000000000000000000 ) ) ;
#17742=EDGE_LOOP ( 'NONE', ( #9546, #42734, #37942, #8250 ) ) ;
#17743=CARTESIAN_POINT ( 'NONE',  ( -2.693516549646820746, -10.09643294401462832, 455.0000000000000568 ) ) ;
#17747=ORIENTED_EDGE ( 'NONE', *, *, #9658, .T. ) ;
#17749=FACE_OUTER_BOUND ( 'NONE', #44408, .T. ) ;
#17759=CARTESIAN_POINT ( 'NONE',  ( 9.247904806590689475, -9.955011587777349291, 455.0000000000000568 ) ) ;
#17770=DIRECTION ( 'NONE',  ( 0.7071067811865398012, -0.7071067811865552333, 0.000000000000000000 ) ) ;
#17771=EDGE_CURVE ( 'NONE', #16082, #7775, #22750, .T. ) ;
#17774=CARTESIAN_POINT ( 'NONE',  ( 11.08848345035342042, 11.47551654964652812, 455.0000000000000568 ) ) ;
#17777=CYLINDRICAL_SURFACE ( 'NONE', #176, 0.1999999999999987899 ) ;
#17779=VERTEX_POINT ( 'NONE', #12813 ) ;
#17793=AXIS2_PLACEMENT_3D ( 'NONE', #60288, #19167, #39077 ) ;
#17796=CARTESIAN_POINT ( 'NONE',  ( 2.706483450353418085, 10.08346604330775875, 455.0000000000000568 ) ) ;
#17797=VERTEX_POINT ( 'NONE', #65879 ) ;
#17800=VECTOR ( 'NONE', #65127, 1000.000000000000000 ) ;
#17803=CYLINDRICAL_SURFACE ( 'NONE', #17893, 2.204799999999998761 ) ;
#17809=CIRCLE ( 'NONE', #39254, 0.1999999999999996503 ) ;
#17812=CARTESIAN_POINT ( 'NONE',  ( 4.201500623656003519, -4.740315990920191069, 195.0000000000000284 ) ) ;
#17816=EDGE_CURVE ( 'NONE', #14532, #46696, #34741, .T. ) ;
#17821=ADVANCED_FACE ( 'NONE', ( #29435 ), #18129, .F. ) ;
#17824=AXIS2_PLACEMENT_3D ( 'NONE', #4825, #47955, #33432 ) ;
#17825=EDGE_CURVE ( 'NONE', #4470, #53071, #66915, .T. ) ;
#17839=CARTESIAN_POINT ( 'NONE',  ( 7.826483450353421745, 11.99351654964657499, 455.0000000000000568 ) ) ;
#17848=VECTOR ( 'NONE', #685, 1000.000000000000000 ) ;
#17856=CIRCLE ( 'NONE', #26915, 0.2000000000000005107 ) ;
#17860=ORIENTED_EDGE ( 'NONE', *, *, #68876, .T. ) ;
#17862=DIRECTION ( 'NONE',  ( -1.000000000000000000, 2.135044278125299371E-15, 0.000000000000000000 ) ) ;
#17867=DIRECTION ( 'NONE',  ( -0.000000000000000000, 1.000000000000000000, 3.673940397442059868E-16 ) ) ;
#17869=DIRECTION ( 'NONE',  ( 0.000000000000000000, 0.000000000000000000, 1.000000000000000000 ) ) ;
#17878=ORIENTED_EDGE ( 'NONE', *, *, #4217, .T. ) ;
#17880=ADVANCED_FACE ( 'NONE', ( #36494 ), #40750, .F. ) ;
#17881=CARTESIAN_POINT ( 'NONE',  ( 10.09643294401457858, 9.093516549646567526, 455.0000000000000568 ) ) ;
#17884=DIRECTION ( 'NONE',  ( 0.6414496315691645689, 0.7671651518152939886, 2.309356642088551606E-17 ) ) ;
#17886=LINE ( 'NONE', #40138, #48109 ) ;
#17887=ORIENTED_EDGE ( 'NONE', *, *, #29698, .F. ) ;
#17892=PLANE ( 'NONE',  #56864 ) ;
#17893=AXIS2_PLACEMENT_3D ( 'NONE', #27117, #48683, #34046 ) ;
#17896=EDGE_CURVE ( 'NONE', #41587, #68671, #35432, .T. ) ;
#17901=DIRECTION ( 'NONE',  ( -1.000000000000000000, 8.540177112501197482E-15, 3.137610169492823463E-30 ) ) ;
#17902=ORIENTED_EDGE ( 'NONE', *, *, #38579, .T. ) ;
#17903=ORIENTED_EDGE ( 'NONE', *, *, #62111, .F. ) ;
#17906=CARTESIAN_POINT ( 'NONE',  ( 11.12648345035337982, -4.206483450353396769, 195.0000000000000284 ) ) ;
#17910=LINE ( 'NONE', #61032, #140 ) ;
#17911=ORIENTED_EDGE ( 'NONE', *, *, #15540, .F. ) ;
#17915=DIRECTION ( 'NONE',  ( -9.799566706031580591E-15, -1.000000000000000000, 0.000000000000000000 ) ) ;
#17918=CARTESIAN_POINT ( 'NONE',  ( -4.188533722949421723, -7.272650909786664286, 455.0000000000000568 ) ) ;
#17920=ORIENTED_EDGE ( 'NONE', *, *, #3145, .T. ) ;
#17927=EDGE_CURVE ( 'NONE', #31474, #15026, #9633, .T. ) ;
#17932=PLANE ( 'NONE',  #54219 ) ;
#17937=DIRECTION ( 'NONE',  ( 1.000000000000000000, -1.047444401652940007E-14, 1.836970198721010706E-16 ) ) ;
#17941=FACE_OUTER_BOUND ( 'NONE', #41223, .T. ) ;
#17947=CARTESIAN_POINT ( 'NONE',  ( 11.08848345035334404, -10.20488345035352928, 455.0000000000000568 ) ) ;
#17957=ORIENTED_EDGE ( 'NONE', *, *, #63946, .F. ) ;
#17960=CARTESIAN_POINT ( 'NONE',  ( 5.393625297349901260, -4.747751991980658559, 195.0000000000000284 ) ) ;
#17961=ORIENTED_EDGE ( 'NONE', *, *, #46835, .T. ) ;
#17969=CARTESIAN_POINT ( 'NONE',  ( 7.826483450353380000, -11.78648345035349010, 455.0000000000000568 ) ) ;
#17977=DIRECTION ( 'NONE',  ( -1.836970198721029934E-16, 1.836970198721036344E-16, -1.000000000000000000 ) ) ;
#17978=EDGE_CURVE ( 'NONE', #23956, #65820, #47116, .T. ) ;
#17982=EDGE_CURVE ( 'NONE', #58549, #5389, #63891, .T. ) ;
#17987=AXIS2_PLACEMENT_3D ( 'NONE', #44488, #57204, #14060 ) ;
#17992=ORIENTED_EDGE ( 'NONE', *, *, #62195, .F. ) ;
#17996=CIRCLE ( 'NONE', #42848, 0.3999999999999993006 ) ;
#17997=LINE ( 'NONE', #65078, #53430 ) ;
#18000=ORIENTED_EDGE ( 'NONE', *, *, #34549, .T. ) ;
#18006=CARTESIAN_POINT ( 'NONE',  ( -4.383466043307920224, -8.406483450353396947, 195.0000000000000284 ) ) ;
#18031=EDGE_CURVE ( 'NONE', #66711, #55626, #15289, .T. ) ;
#18035=DIRECTION ( 'NONE',  ( 0.000000000000000000, 1.000000000000000000, 3.673940397442059868E-16 ) ) ;
#18042=AXIS2_PLACEMENT_3D ( 'NONE', #48396, #37442, #47345 ) ;
#18062=LINE ( 'NONE', #49228, #69615 ) ;
#18074=ORIENTED_EDGE ( 'NONE', *, *, #65103, .F. ) ;
#18077=ORIENTED_EDGE ( 'NONE', *, *, #15511, .F. ) ;
#18081=VECTOR ( 'NONE', #61207, 1000.000000000000000 ) ;
#18082=ORIENTED_EDGE ( 'NONE', *, *, #8478, .T. ) ;
#18086=ORIENTED_EDGE ( 'NONE', *, *, #33156, .T. ) ;
#18088=VECTOR ( 'NONE', #32049, 1000.000000000000000 ) ;
#18089=LINE ( 'NONE', #60539, #5173 ) ;
#18097=LINE ( 'NONE', #55940, #51850 ) ;
#18098=AXIS2_PLACEMENT_3D ( 'NONE', #5433, #58816, #37944 ) ;
#18110=AXIS2_PLACEMENT_3D ( 'NONE', #59581, #38361, #11130 ) ;
#18122=ORIENTED_EDGE ( 'NONE', *, *, #52638, .T. ) ;
#18129=PLANE ( 'NONE',  #28783 ) ;
#18137=ORIENTED_EDGE ( 'NONE', *, *, #2230, .T. ) ;
#18141=DIRECTION ( 'NONE',  ( 1.000000000000000000, 0.000000000000000000, 0.000000000000000000 ) ) ;
#18143=CARTESIAN_POINT ( 'NONE',  ( -5.993516549646711766, 5.993516549646603409, 195.0000000000000284 ) ) ;
#18148=ORIENTED_EDGE ( 'NONE', *, *, #6154, .F. ) ;
#18149=VECTOR ( 'NONE', #50047, 1000.000000000000000 ) ;
#18150=VECTOR ( 'NONE', #23278, 1000.000000000000000 ) ;
#18151=VERTEX_POINT ( 'NONE', #62475 ) ;
#18158=EDGE_CURVE ( 'NONE', #51358, #31939, #56831, .T. ) ;
#18165=ORIENTED_EDGE ( 'NONE', *, *, #23247, .F. ) ;
#18170=ORIENTED_EDGE ( 'NONE', *, *, #16194, .T. ) ;
#18173=VECTOR ( 'NONE', #54715, 1000.000000000000000 ) ;
#18175=CARTESIAN_POINT ( 'NONE',  ( -1.677516549646826061, -10.74648345035347141, 455.0000000000000568 ) ) ;
#18184=ADVANCED_FACE ( 'NONE', ( #18650 ), #35610, .F. ) ;
#18188=ORIENTED_EDGE ( 'NONE', *, *, #58314, .T. ) ;
#18210=LINE ( 'NONE', #33443, #9799 ) ;
#18218=EDGE_LOOP ( 'NONE', ( #39993, #44209, #29458, #43362 ) ) ;
#18219=PLANE ( 'NONE',  #4752 ) ;
#18221=CARTESIAN_POINT ( 'NONE',  ( -10.73351654964671198, 1.077516549646603483, 195.0000000000000284 ) ) ;
#18228=ORIENTED_EDGE ( 'NONE', *, *, #332, .T. ) ;
#18230=DIRECTION ( 'NONE',  ( 1.000000000000000000, -5.120954910632640039E-15, 0.000000000000000000 ) ) ;
#18232=CARTESIAN_POINT ( 'NONE',  ( -7.603567055985634759, -8.406483450353409381, 455.0000000000000568 ) ) ;
#18233=DIRECTION ( 'NONE',  ( -0.000000000000000000, -0.000000000000000000, -1.000000000000000000 ) ) ;
#18234=DIRECTION ( 'NONE',  ( 0.000000000000000000, 0.000000000000000000, 1.000000000000000000 ) ) ;
#18240=CARTESIAN_POINT ( 'NONE',  ( -11.99351654964669756, -4.186483450353271074, 195.0000000000000284 ) ) ;
#18243=EDGE_LOOP ( 'NONE', ( #27285, #23541, #27920, #7238 ) ) ;
#18253=VECTOR ( 'NONE', #48491, 1000.000000000000000 ) ;
#18254=CARTESIAN_POINT ( 'NONE',  ( 6.006483450353379716, -6.006483450353394815, 195.0000000000000284 ) ) ;
#18257=EDGE_CURVE ( 'NONE', #45713, #33646, #61795, .T. ) ;
#18260=VECTOR ( 'NONE', #43680, 1000.000000000000000 ) ;
#18263=EDGE_LOOP ( 'NONE', ( #11208, #10948, #8682, #49639 ) ) ;
#18280=DIRECTION ( 'NONE',  ( 1.836970198721029934E-16, 1.836970198721010706E-16, -1.000000000000000000 ) ) ;
#18284=CARTESIAN_POINT ( 'NONE',  ( -2.277516549646768418, -9.841277389592759661, 195.0000000000000284 ) ) ;
#18285=DIRECTION ( 'NONE',  ( -1.000000000000000000, 5.120954910632640039E-15, 0.000000000000000000 ) ) ;
#18290=LINE ( 'NONE', #33528, #5043 ) ;
#18292=DIRECTION ( 'NONE',  ( 0.000000000000000000, -1.000000000000000000, 0.000000000000000000 ) ) ;
#18301=AXIS2_PLACEMENT_3D ( 'NONE', #16917, #60039, #11587 ) ;
#18302=CARTESIAN_POINT ( 'NONE',  ( 2.706483450353350584, -10.09643294401463365, 455.0000000000000568 ) ) ;
#18303=CARTESIAN_POINT ( 'NONE',  ( 7.826483450353421745, 11.99351654964657499, 455.0000000000000568 ) ) ;
#18309=LINE ( 'NONE', #40235, #2198 ) ;
#18321=CIRCLE ( 'NONE', #29634, 0.1999999999999996503 ) ;
#18322=EDGE_LOOP ( 'NONE', ( #24159, #20635, #63016, #20317, #25003, #30501, #57386, #19363 ) ) ;
#18326=AXIS2_PLACEMENT_3D ( 'NONE', #21080, #69171, #32728 ) ;
#18339=VERTEX_POINT ( 'NONE', #14415 ) ;
#18345=ORIENTED_EDGE ( 'NONE', *, *, #59371, .F. ) ;
#18346=AXIS2_PLACEMENT_3D ( 'NONE', #29590, #18280, #51162 ) ;
#18353=EDGE_LOOP ( 'NONE', ( #59361, #38148, #29885, #18228 ) ) ;
#18357=CARTESIAN_POINT ( 'NONE',  ( 5.668387132715920096, 8.393516549646628633, 195.0000000000000284 ) ) ;
#18382=EDGE_LOOP ( 'NONE', ( #58694, #65988, #25084, #9676 ) ) ;
#18383=ORIENTED_EDGE ( 'NONE', *, *, #55114, .T. ) ;
#18388=ORIENTED_EDGE ( 'NONE', *, *, #855, .T. ) ;
#18399=LINE ( 'NONE', #2846, #41221 ) ;
#18412=ORIENTED_EDGE ( 'NONE', *, *, #69529, .T. ) ;
#18420=EDGE_CURVE ( 'NONE', #9547, #11897, #10153, .T. ) ;
#18425=DIRECTION ( 'NONE',  ( -1.836970198721029934E-16, 1.836970198721036344E-16, -1.000000000000000000 ) ) ;
#18427=CARTESIAN_POINT ( 'NONE',  ( 7.272650909786644746, 7.798499376343933420, 455.0000000000000568 ) ) ;
#18437=DIRECTION ( 'NONE',  ( -4.336808689942006692E-15, -1.000000000000000000, 0.000000000000000000 ) ) ;
#18438=ORIENTED_EDGE ( 'NONE', *, *, #62573, .F. ) ;
#18442=DIRECTION ( 'NONE',  ( -1.836970198721029934E-16, 1.836970198721036344E-16, -1.000000000000000000 ) ) ;
#18457=DIRECTION ( 'NONE',  ( -0.000000000000000000, 3.673940397442059868E-16, -1.000000000000000000 ) ) ;
#18465=ORIENTED_EDGE ( 'NONE', *, *, #24942, .F. ) ;
#18469=ORIENTED_EDGE ( 'NONE', *, *, #47204, .F. ) ;
#18473=CARTESIAN_POINT ( 'NONE',  ( 4.740315990920125344, 7.798499376343988487, 195.0000000000000284 ) ) ;
#18478=VERTEX_POINT ( 'NONE', #65303 ) ;
#18483=DIRECTION ( 'NONE',  ( -0.000000000000000000, -0.000000000000000000, -1.000000000000000000 ) ) ;
#18484=CIRCLE ( 'NONE', #37691, 0.2000000000000005107 ) ;
#18487=VERTEX_POINT ( 'NONE', #55045 ) ;
#18492=DIRECTION ( 'NONE',  ( -1.000000000000000000, 0.000000000000000000, 0.000000000000000000 ) ) ;
#18495=DIRECTION ( 'NONE',  ( 1.836970198721029934E-16, 1.836970198721010706E-16, -1.000000000000000000 ) ) ;
#18500=ORIENTED_EDGE ( 'NONE', *, *, #20368, .F. ) ;
#18501=VERTEX_POINT ( 'NONE', #49714 ) ;
#18518=LINE ( 'NONE', #67670, #25056 ) ;
#18522=ORIENTED_EDGE ( 'NONE', *, *, #7853, .T. ) ;
#18525=EDGE_LOOP ( 'NONE', ( #67594, #66974, #47765, #35237 ) ) ;
#18526=EDGE_CURVE ( 'NONE', #59410, #31564, #954, .T. ) ;
#18532=ORIENTED_EDGE ( 'NONE', *, *, #58977, .T. ) ;
#18540=DIRECTION ( 'NONE',  ( 1.000000000000000000, 1.570596175624152093E-15, 0.000000000000000000 ) ) ;
#18550=EDGE_CURVE ( 'NONE', #35182, #35322, #13621, .T. ) ;
#18562=DIRECTION ( 'NONE',  ( 0.000000000000000000, 1.000000000000000000, 0.000000000000000000 ) ) ;
#18568=DIRECTION ( 'NONE',  ( 0.7071067811865515695, 0.7071067811865435759, 0.000000000000000000 ) ) ;
#18574=CIRCLE ( 'NONE', #2778, 0.2000000000000005107 ) ;
#18575=DIRECTION ( 'NONE',  ( -1.000000000000000000, 7.808916176531286882E-15, 0.000000000000000000 ) ) ;
#18579=EDGE_LOOP ( 'NONE', ( #49749, #19795, #43476, #35387 ) ) ;
#18581=CARTESIAN_POINT ( 'NONE',  ( 1.090483450353420425, 11.33351654964659971, 455.0000000000000568 ) ) ;
#18588=DIRECTION ( 'NONE',  ( 1.000000000000000000, -2.309061475090597584E-14, 1.836970198720987533E-16 ) ) ;
#18591=EDGE_CURVE ( 'NONE', #68006, #5476, #67379, .T. ) ;
#18606=ADVANCED_FACE ( 'NONE', ( #66331 ), #39445, .F. ) ;
#18607=DIRECTION ( 'NONE',  ( -0.000000000000000000, -0.000000000000000000, -1.000000000000000000 ) ) ;
#18614=VECTOR ( 'NONE', #47850, 1000.000000000000000 ) ;
#18622=DIRECTION ( 'NONE',  ( 0.6414496315691485817, -0.7671651518153073113, 0.000000000000000000 ) ) ;
#18636=DIRECTION ( 'NONE',  ( 1.836970198721029934E-16, 1.836970198721010706E-16, -1.000000000000000000 ) ) ;
#18640=CARTESIAN_POINT ( 'NONE',  ( 9.306483450353368880, 10.08346604330778362, 195.0000000000000284 ) ) ;
#18643=DIRECTION ( 'NONE',  ( -0.000000000000000000, -0.000000000000000000, -1.000000000000000000 ) ) ;
#18645=LINE ( 'NONE', #8031, #30897 ) ;
#18646=CIRCLE ( 'NONE', #28840, 0.1999999999999987899 ) ;
#18648=VECTOR ( 'NONE', #8783, 1000.000000000000000 ) ;
#18650=FACE_OUTER_BOUND ( 'NONE', #26075, .T. ) ;
#18658=LINE ( 'NONE', #34570, #55965 ) ;
#18666=FACE_OUTER_BOUND ( 'NONE', #4510, .T. ) ;
#18669=ORIENTED_EDGE ( 'NONE', *, *, #54883, .T. ) ;
#18670=MECHANICAL_DESIGN_GEOMETRIC_PRESENTATION_REPRESENTATION('',(#44660),#57092);
#18674=CARTESIAN_POINT ( 'NONE',  ( -5.993516549646711766, 8.198316549646602169, 455.0000000000000568 ) ) ;
#18683=DIRECTION ( 'NONE',  ( -0.000000000000000000, 3.673940397442059868E-16, -1.000000000000000000 ) ) ;
#18686=EDGE_CURVE ( 'NONE', #15026, #60382, #62399, .T. ) ;
#18707=ORIENTED_EDGE ( 'NONE', *, *, #54203, .T. ) ;
#18713=LINE ( 'NONE', #50193, #25672 ) ;
#18715=VECTOR ( 'NONE', #58631, 1000.000000000000000 ) ;
#18716=LINE ( 'NONE', #55515, #40927 ) ;
#18723=EDGE_CURVE ( 'NONE', #11916, #23956, #35529, .T. ) ;
#18725=CARTESIAN_POINT ( 'NONE',  ( -4.173516549646666185, 11.99351654964658920, 195.0000000000000284 ) ) ;
#18726=EDGE_CURVE ( 'NONE', #67203, #8462, #14338, .T. ) ;
#18732=DIRECTION ( 'NONE',  ( -0.000000000000000000, -0.000000000000000000, -1.000000000000000000 ) ) ;
#18740=ORIENTED_EDGE ( 'NONE', *, *, #45807, .F. ) ;
#18746=VECTOR ( 'NONE', #32761, 1000.000000000000000 ) ;
#18750=LINE ( 'NONE', #56922, #32138 ) ;
#18756=VECTOR ( 'NONE', #38581, 1000.000000000000000 ) ;
#18759=CYLINDRICAL_SURFACE ( 'NONE', #45040, 0.2000000000000005107 ) ;
#18779=EDGE_CURVE ( 'NONE', #60848, #12404, #68776, .T. ) ;
#18797=DIRECTION ( 'NONE',  ( -0.6414496315691473605, -0.7671651518153083105, -2.309356642089130002E-17 ) ) ;
#18804=ORIENTED_EDGE ( 'NONE', *, *, #48389, .F. ) ;
#18805=DIRECTION ( 'NONE',  ( -1.000000000000000000, 5.120954910632640039E-15, 1.881408311965255020E-30 ) ) ;
#18807=EDGE_LOOP ( 'NONE', ( #15554, #5294, #26016, #46208 ) ) ;
#18809=AXIS2_PLACEMENT_3D ( 'NONE', #49835, #22624, #66441 ) ;
#18810=DIRECTION ( 'NONE',  ( 0.000000000000000000, 1.000000000000000000, 0.000000000000000000 ) ) ;
#18812=DIRECTION ( 'NONE',  ( -1.000000000000000000, 1.047444401652939849E-14, -1.836970198721010706E-16 ) ) ;
#18816=AXIS2_PLACEMENT_3D ( 'NONE', #57473, #4453, #9752 ) ;
#18819=LINE ( 'NONE', #8903, #27948 ) ;
#18828=CARTESIAN_POINT ( 'NONE',  ( -9.234937905884020637, 9.942044687070460185, 195.0000000000000284 ) ) ;
#18832=CARTESIAN_POINT ( 'NONE',  ( 10.74648345035338082, -1.090483450353395334, 195.0000000000000284 ) ) ;
#18835=CARTESIAN_POINT ( 'NONE',  ( -11.07551654964667520, 11.47551654964660450, 195.0000000000000284 ) ) ;
#18838=ORIENTED_EDGE ( 'NONE', *, *, #63495, .F. ) ;
#18840=LINE ( 'NONE', #56669, #54316 ) ;
#18845=CARTESIAN_POINT ( 'NONE',  ( 11.12648345035338160, 4.193516549646526315, 455.0000000000000568 ) ) ;
#18849=CARTESIAN_POINT ( 'NONE',  ( -1.677516549646768551, -9.841277389592764990, 195.0000000000000284 ) ) ;
#18860=AXIS2_PLACEMENT_3D ( 'NONE', #55963, #7521, #2918 ) ;
#18864=EDGE_CURVE ( 'NONE', #27405, #24080, #11115, .T. ) ;
#18870=VECTOR ( 'NONE', #47951, 1000.000000000000000 ) ;
#18880=LINE ( 'NONE', #36181, #11299 ) ;
#18882=DIRECTION ( 'NONE',  ( 1.000000000000000000, 1.671920889371702854E-15, 6.142537696789956391E-31 ) ) ;
#18887=CIRCLE ( 'NONE', #65192, 0.1999999999999992339 ) ;
#18889=DIRECTION ( 'NONE',  ( -1.836970198721029934E-16, 1.836970198721036344E-16, -1.000000000000000000 ) ) ;
#18890=DIRECTION ( 'NONE',  ( 1.062171939662867618E-14, 1.000000000000000000, 0.000000000000000000 ) ) ;
#18900=ADVANCED_FACE ( 'NONE', ( #32001 ), #33377, .F. ) ;
#18924=CARTESIAN_POINT ( 'NONE',  ( -2.893516549646673930, 11.11351654964657598, 195.0000000000000284 ) ) ;
#18940=EDGE_LOOP ( 'NONE', ( #67020, #3108, #5674, #20386 ) ) ;
#18958=CARTESIAN_POINT ( 'NONE',  ( 7.806483450353379538, -11.32648345035348925, 455.0000000000000568 ) ) ;
#18959=ADVANCED_FACE ( 'NONE', ( #10762 ), #16080, .F. ) ;
#18964=DIRECTION ( 'NONE',  ( 1.000000000000000000, 0.000000000000000000, 0.000000000000000000 ) ) ;
#18982=EDGE_CURVE ( 'NONE', #20667, #26162, #49313, .T. ) ;
#18988=EDGE_CURVE ( 'NONE', #35354, #62970, #13538, .T. ) ;
#18998=FACE_OUTER_BOUND ( 'NONE', #16231, .T. ) ;
#19004=DIRECTION ( 'NONE',  ( -1.836970198721029934E-16, 1.836970198721036344E-16, -1.000000000000000000 ) ) ;
#19005=EDGE_LOOP ( 'NONE', ( #31958, #51655, #2221, #36114, #30356, #34769, #16979, #62050 ) ) ;
#19011=EDGE_CURVE ( 'NONE', #61131, #50332, #44656, .T. ) ;
#19015=AXIS2_PLACEMENT_3D ( 'NONE', #3144, #8066, #2431 ) ;
#19024=ORIENTED_EDGE ( 'NONE', *, *, #6772, .T. ) ;
#19035=VERTEX_POINT ( 'NONE', #45011 ) ;
#19040=CARTESIAN_POINT ( 'NONE',  ( -7.744988412222944874, -8.465062094116097668, 455.0000000000000568 ) ) ;
#19046=ORIENTED_EDGE ( 'NONE', *, *, #38153, .F. ) ;
#19058=DIRECTION ( 'NONE',  ( -1.901462112903060228E-14, -1.000000000000000000, 0.000000000000000000 ) ) ;
#19059=DIRECTION ( 'NONE',  ( 1.836970198721029934E-16, 1.836970198721010706E-16, -1.000000000000000000 ) ) ;
#19064=VECTOR ( 'NONE', #62366, 1000.000000000000114 ) ;
#19070=EDGE_LOOP ( 'NONE', ( #39448, #47236, #28120, #23043, #5066, #11272, #63297, #46383 ) ) ;
#19075=ADVANCED_FACE ( 'NONE', ( #66586 ), #12823, .F. ) ;
#19078=DIRECTION ( 'NONE',  ( -0.000000000000000000, 3.673940397442059868E-16, -1.000000000000000000 ) ) ;
#19083=ORIENTED_EDGE ( 'NONE', *, *, #40375, .F. ) ;
#19097=ORIENTED_EDGE ( 'NONE', *, *, #4359, .F. ) ;
#19103=ORIENTED_EDGE ( 'NONE', *, *, #39358, .T. ) ;
#19104=ORIENTED_EDGE ( 'NONE', *, *, #38579, .F. ) ;
#19105=CARTESIAN_POINT ( 'NONE',  ( -11.07551654964667520, 11.47551654964660450, 455.0000000000000568 ) ) ;
#19109=DIRECTION ( 'NONE',  ( -0.7071067811865474617, 0.7071067811865474617, 2.597868168706479611E-16 ) ) ;
#19111=DIRECTION ( 'NONE',  ( 1.000000000000000000, -7.665540703601094997E-15, -2.816273965919649962E-30 ) ) ;
#19113=VERTEX_POINT ( 'NONE', #51731 ) ;
#19120=ORIENTED_EDGE ( 'NONE', *, *, #4014, .F. ) ;
#19130=EDGE_CURVE ( 'NONE', #5311, #50275, #3285, .T. ) ;
#19131=CIRCLE ( 'NONE', #11253, 0.1999999999999987899 ) ;
#19134=EDGE_LOOP ( 'NONE', ( #62746, #52941, #983, #61208 ) ) ;
#19139=CARTESIAN_POINT ( 'NONE',  ( 9.804883450353456098, 11.07551654964653132, 455.0000000000000568 ) ) ;
#19142=DIRECTION ( 'NONE',  ( 0.7071067811865527908, 0.7071067811865422437, 2.597868168706460875E-16 ) ) ;
#19145=CARTESIAN_POINT ( 'NONE',  ( -11.11351654964671098, 4.193516549646605363, 455.0000000000000568 ) ) ;
#19146=CYLINDRICAL_SURFACE ( 'NONE', #49356, 0.2000000000000005107 ) ;
#19162=CARTESIAN_POINT ( 'NONE',  ( -11.77351654964674665, -7.826483450353317828, 195.0000000000000284 ) ) ;
#19165=CARTESIAN_POINT ( 'NONE',  ( 1.690483450353367889, 9.828310488885986018, 195.0000000000000284 ) ) ;
#19167=DIRECTION ( 'NONE',  ( 0.000000000000000000, -3.673940397442059868E-16, 1.000000000000000000 ) ) ;
#19168=CARTESIAN_POINT ( 'NONE',  ( -3.593516549646790015, -7.428221114745077180, 455.0000000000000568 ) ) ;
#19170=VECTOR ( 'NONE', #60822, 1000.000000000000000 ) ;
#19174=VECTOR ( 'NONE', #29778, 1000.000000000000000 ) ;
#19176=EDGE_CURVE ( 'NONE', #3811, #49314, #9294, .T. ) ;
#19180=VERTEX_POINT ( 'NONE', #35805 ) ;
#19193=CARTESIAN_POINT ( 'NONE',  ( 10.92648345035340895, 9.293516549646565039, 455.0000000000000568 ) ) ;
#19204=LINE ( 'NONE', #7883, #31051 ) ;
#19205=CARTESIAN_POINT ( 'NONE',  ( 6.344579767990823349, -8.406483450353491094, 455.0000000000000568 ) ) ;
#19209=VECTOR ( 'NONE', #52147, 1000.000000000000114 ) ;
#19211=ORIENTED_EDGE ( 'NONE', *, *, #50785, .F. ) ;
#19213=EDGE_CURVE ( 'NONE', #67306, #48721, #26739, .T. ) ;
#19226=CARTESIAN_POINT ( 'NONE',  ( -5.380658396643267949, -4.747751991980631026, 195.0000000000000284 ) ) ;
#19229=VECTOR ( 'NONE', #29692, 1000.000000000000000 ) ;
#19234=ORIENTED_EDGE ( 'NONE', *, *, #11975, .F. ) ;
#19238=DIRECTION ( 'NONE',  ( 1.047444401652940007E-14, 1.000000000000000000, 1.836970198721029934E-16 ) ) ;
#19240=DIRECTION ( 'NONE',  ( 0.000000000000000000, 1.000000000000000000, 0.000000000000000000 ) ) ;
#19242=DIRECTION ( 'NONE',  ( -1.000000000000000000, 0.000000000000000000, 0.000000000000000000 ) ) ;
#19243=FACE_OUTER_BOUND ( 'NONE', #13470, .T. ) ;
#19249=FACE_OUTER_BOUND ( 'NONE', #18218, .T. ) ;
#19257=ADVANCED_FACE ( 'NONE', ( #37428 ), #19146, .F. ) ;
#19275=ORIENTED_EDGE ( 'NONE', *, *, #49299, .F. ) ;
#19286=EDGE_LOOP ( 'NONE', ( #9639, #56450, #67583, #20009 ) ) ;
#19296=VERTEX_POINT ( 'NONE', #26125 ) ;
#19297=ORIENTED_EDGE ( 'NONE', *, *, #20020, .T. ) ;
#19301=ORIENTED_EDGE ( 'NONE', *, *, #56446, .T. ) ;
#19302=CARTESIAN_POINT ( 'NONE',  ( -10.19191654964671301, 11.07551654964660415, 455.0000000000000568 ) ) ;
#19303=DIRECTION ( 'NONE',  ( 3.016910393003147986E-15, -1.000000000000000000, 0.000000000000000000 ) ) ;
#19307=VERTEX_POINT ( 'NONE', #39483 ) ;
#19311=PLANE ( 'NONE',  #66518 ) ;
#19320=VERTEX_POINT ( 'NONE', #38795 ) ;
#19324=VECTOR ( 'NONE', #53893, 1000.000000000000000 ) ;
#19331=CARTESIAN_POINT ( 'NONE',  ( -4.173516549646669738, 11.77351654964658678, 455.0000000000000568 ) ) ;
#19345=EDGE_CURVE ( 'NONE', #3591, #6350, #61579, .T. ) ;
#19355=ORIENTED_EDGE ( 'NONE', *, *, #59192, .T. ) ;
#19363=ORIENTED_EDGE ( 'NONE', *, *, #2364, .T. ) ;
#19366=VECTOR ( 'NONE', #21296, 1000.000000000000114 ) ;
#19375=LINE ( 'NONE', #13723, #22065 ) ;
#19376=ORIENTED_EDGE ( 'NONE', *, *, #42005, .T. ) ;
#19379=ORIENTED_EDGE ( 'NONE', *, *, #4674, .F. ) ;
#19380=ADVANCED_FACE ( 'NONE', ( #55756 ), #7301, .T. ) ;
#19382=CARTESIAN_POINT ( 'NONE',  ( -4.609516549646703432, -3.606483450353393572, 195.0000000000000284 ) ) ;
#19384=ORIENTED_EDGE ( 'NONE', *, *, #631, .F. ) ;
#19408=DIRECTION ( 'NONE',  ( 0.000000000000000000, 1.000000000000000000, 0.000000000000000000 ) ) ;
#19417=CYLINDRICAL_SURFACE ( 'NONE', #45465, 0.1999999999999996503 ) ;
#19419=DIRECTION ( 'NONE',  ( -0.000000000000000000, -0.000000000000000000, -1.000000000000000000 ) ) ;
#19427=DIRECTION ( 'NONE',  ( -1.000000000000000000, 0.000000000000000000, 0.000000000000000000 ) ) ;
#19432=DIRECTION ( 'NONE',  ( -0.7071067811865550112, -0.7071067811865401342, -2.597868168706466299E-16 ) ) ;
#19452=ORIENTED_EDGE ( 'NONE', *, *, #12447, .T. ) ;
#19460=DIRECTION ( 'NONE',  ( 1.000000000000000000, 0.000000000000000000, 0.000000000000000000 ) ) ;
#19465=EDGE_LOOP ( 'NONE', ( #13209, #25824, #32360, #16322 ) ) ;
#19466=EDGE_LOOP ( 'NONE', ( #68746, #261, #26356, #33632, #31933, #54209, #58385, #10131 ) ) ;
#19468=FACE_OUTER_BOUND ( 'NONE', #9167, .T. ) ;
#19480=ORIENTED_EDGE ( 'NONE', *, *, #17224, .F. ) ;
#19517=DIRECTION ( 'NONE',  ( -0.000000000000000000, 3.673940397442059868E-16, -1.000000000000000000 ) ) ;
#19521=EDGE_LOOP ( 'NONE', ( #35765, #13354, #18469, #42523 ) ) ;
#19524=VECTOR ( 'NONE', #28133, 1000.000000000000000 ) ;
#19531=VERTEX_POINT ( 'NONE', #15770 ) ;
#19534=VERTEX_POINT ( 'NONE', #46887 ) ;
#19539=DIRECTION ( 'NONE',  ( -0.000000000000000000, -1.000000000000000000, -0.000000000000000000 ) ) ;
#19541=FACE_BOUND ( 'NONE', #38328, .T. ) ;
#19542=CARTESIAN_POINT ( 'NONE',  ( -3.593516549646762481, -4.622483450353452206, 455.0000000000000568 ) ) ;
#19543=CARTESIAN_POINT ( 'NONE',  ( 6.006483450353379716, -6.006483450353490738, 455.0000000000000568 ) ) ;
#19544=AXIS2_PLACEMENT_3D ( 'NONE', #58519, #57445, #8998 ) ;
#19548=ORIENTED_EDGE ( 'NONE', *, *, #10013, .T. ) ;
#19559=ORIENTED_EDGE ( 'NONE', *, *, #69854, .T. ) ;
#19561=EDGE_CURVE ( 'NONE', #49979, #62970, #39037, .T. ) ;
#19564=ORIENTED_EDGE ( 'NONE', *, *, #8208, .F. ) ;
#19572=DIRECTION ( 'NONE',  ( 0.000000000000000000, -1.000000000000000000, 0.000000000000000000 ) ) ;
#19573=VECTOR ( 'NONE', #757, 1000.000000000000000 ) ;
#19587=CARTESIAN_POINT ( 'NONE',  ( 9.804883450353379715, -10.20488345035343336, 195.0000000000000284 ) ) ;
#19596=DIRECTION ( 'NONE',  ( -1.000000000000000000, 0.000000000000000000, 0.000000000000000000 ) ) ;
#19613=FACE_OUTER_BOUND ( 'NONE', #6438, .T. ) ;
#19652=ORIENTED_EDGE ( 'NONE', *, *, #22333, .F. ) ;
#19658=CIRCLE ( 'NONE', #2754, 0.2000000000000000944 ) ;
#19662=ORIENTED_EDGE ( 'NONE', *, *, #42968, .T. ) ;
#19666=FACE_OUTER_BOUND ( 'NONE', #24953, .T. ) ;
#19667=VECTOR ( 'NONE', #41726, 1000.000000000000000 ) ;
#19668=CARTESIAN_POINT ( 'NONE',  ( 4.747751991980615038, 5.380658396643156038, 195.0000000000000284 ) ) ;
#19672=DIRECTION ( 'NONE',  ( 0.7071067811865486830, 0.7071067811865464625, 0.000000000000000000 ) ) ;
#19674=CARTESIAN_POINT ( 'NONE',  ( -11.11351654964670743, 2.893516549646604208, 195.0000000000000284 ) ) ;
#19675=DIRECTION ( 'NONE',  ( 0.6414496315691494699, 0.7671651518153064231, 0.000000000000000000 ) ) ;
#19676=VECTOR ( 'NONE', #20517, 1000.000000000000000 ) ;
#19677=CARTESIAN_POINT ( 'NONE',  ( -2.893516549646675706, 10.91351654964657669, 455.0000000000000568 ) ) ;
#19682=EDGE_LOOP ( 'NONE', ( #23066, #67827, #65326, #20843 ) ) ;
#19690=FACE_OUTER_BOUND ( 'NONE', #26815, .T. ) ;
#19697=ADVANCED_FACE ( 'NONE', ( #1577 ), #554, .F. ) ;
#19698=VECTOR ( 'NONE', #27105, 1000.000000000000000 ) ;
#19705=EDGE_LOOP ( 'NONE', ( #28321, #12544, #29805, #26820 ) ) ;
#19708=DIRECTION ( 'NONE',  ( 0.7071067811865411334, -0.7071067811865539010, -2.597868168706484541E-16 ) ) ;
#19721=VECTOR ( 'NONE', #33724, 1000.000000000000000 ) ;
#19722=DIRECTION ( 'NONE',  ( -0.7071067811865514585, -0.7071067811865435759, -2.597868168706465806E-16 ) ) ;
#19724=ORIENTED_EDGE ( 'NONE', *, *, #48642, .T. ) ;
#19728=DIRECTION ( 'NONE',  ( -1.000000000000000000, 1.254221251785257731E-14, 1.836970198721053107E-16 ) ) ;
#19729=EDGE_CURVE ( 'NONE', #46020, #32262, #38050, .T. ) ;
#19749=ORIENTED_EDGE ( 'NONE', *, *, #44894, .T. ) ;
#19753=CARTESIAN_POINT ( 'NONE',  ( 11.48848345035337104, 10.19191654964660820, 195.0000000000000284 ) ) ;
#19755=DIRECTION ( 'NONE',  ( 1.836970198721029934E-16, -1.836970198721036344E-16, 1.000000000000000000 ) ) ;
#19771=CARTESIAN_POINT ( 'NONE',  ( 7.806483450353379538, -11.12648345035339226, 195.0000000000000284 ) ) ;
#19772=ORIENTED_EDGE ( 'NONE', *, *, #64922, .T. ) ;
#19780=VECTOR ( 'NONE', #30566, 1000.000000000000114 ) ;
#19787=CARTESIAN_POINT ( 'NONE',  ( 6.619341603356837744, -4.747751991980647901, 195.0000000000000284 ) ) ;
#19789=EDGE_CURVE ( 'NONE', #31070, #21380, #24558, .T. ) ;
#19791=ORIENTED_EDGE ( 'NONE', *, *, #69592, .T. ) ;
#19795=ORIENTED_EDGE ( 'NONE', *, *, #5604, .F. ) ;
#19807=DIRECTION ( 'NONE',  ( 8.673617379884013384E-15, 1.000000000000000000, 0.000000000000000000 ) ) ;
#19814=VECTOR ( 'NONE', #57184, 1000.000000000000000 ) ;
#19845=DIRECTION ( 'NONE',  ( 0.000000000000000000, 0.000000000000000000, 1.000000000000000000 ) ) ;
#19871=AXIS2_PLACEMENT_3D ( 'NONE', #46350, #62607, #36091 ) ;
#19872=CARTESIAN_POINT ( 'NONE',  ( -7.603567055985545942, 8.593516549646603053, 455.0000000000000568 ) ) ;
#19877=VERTEX_POINT ( 'NONE', #25619 ) ;
#19900=EDGE_CURVE ( 'NONE', #46263, #9826, #41155, .T. ) ;
#19903=ORIENTED_EDGE ( 'NONE', *, *, #59136, .F. ) ;
#19905=EDGE_LOOP ( 'NONE', ( #61733, #20619, #18838, #52099 ) ) ;
#19910=CARTESIAN_POINT ( 'NONE',  ( 6.006483450353379716, -4.606483450353397124, 195.0000000000000284 ) ) ;
#19912=VERTEX_POINT ( 'NONE', #46808 ) ;
#19915=DIRECTION ( 'NONE',  ( 1.836970198721029934E-16, 1.836970198721010706E-16, -1.000000000000000000 ) ) ;
#19923=DIRECTION ( 'NONE',  ( -1.836970198721029934E-16, 1.836970198721036344E-16, -1.000000000000000000 ) ) ;
#19931=CIRCLE ( 'NONE', #33455, 2.204799999999997429 ) ;
#19933=LINE ( 'NONE', #62708, #27956 ) ;
#19938=FACE_OUTER_BOUND ( 'NONE', #6178, .T. ) ;
#19941=LINE ( 'NONE', #19587, #15810 ) ;
#19942=CIRCLE ( 'NONE', #5270, 0.1999999999999996503 ) ;
#19948=ORIENTED_EDGE ( 'NONE', *, *, #57347, .T. ) ;
#19949=FACE_OUTER_BOUND ( 'NONE', #15641, .T. ) ;
#19950=CARTESIAN_POINT ( 'NONE',  ( 7.616533956692213003, -8.406483450353396947, 195.0000000000000284 ) ) ;
#19952=ORIENTED_EDGE ( 'NONE', *, *, #61263, .T. ) ;
#19954=CARTESIAN_POINT ( 'NONE',  ( -4.727349090213463612, 4.188533722949258298, 455.0000000000000568 ) ) ;
#19962=ADVANCED_FACE ( 'NONE', ( #20641 ), #42212, .F. ) ;
#19970=EDGE_CURVE ( 'NONE', #4070, #24615, #64491, .T. ) ;
#19972=CIRCLE ( 'NONE', #59503, 1.399999999999998579 ) ;
#19984=CARTESIAN_POINT ( 'NONE',  ( 6.006483450353379716, -6.006483450353490738, 455.0000000000000568 ) ) ;
#19994=AXIS2_PLACEMENT_3D ( 'NONE', #55751, #635, #5933 ) ;
#19996=LINE ( 'NONE', #24945, #44143 ) ;
#19999=( LENGTH_UNIT ( ) NAMED_UNIT ( * ) SI_UNIT ( .MILLI., .METRE. ) );
#20009=ORIENTED_EDGE ( 'NONE', *, *, #17825, .T. ) ;
#20011=DIRECTION ( 'NONE',  ( 0.000000000000000000, -3.673940397442059868E-16, 1.000000000000000000 ) ) ;
#20013=LINE ( 'NONE', #53597, #59420 ) ;
#20020=EDGE_CURVE ( 'NONE', #23208, #30476, #49273, .T. ) ;
#20028=AXIS2_PLACEMENT_3D ( 'NONE', #51403, #66960, #51055 ) ;
#20044=EDGE_CURVE ( 'NONE', #33426, #64234, #11086, .T. ) ;
#20051=CARTESIAN_POINT ( 'NONE',  ( -7.744988412222854279, 8.452095193409293827, 195.0000000000000284 ) ) ;
#20055=FACE_OUTER_BOUND ( 'NONE', #48739, .T. ) ;
#20057=EDGE_CURVE ( 'NONE', #39293, #23736, #1831, .T. ) ;
#20060=VERTEX_POINT ( 'NONE', #60204 ) ;
#20071=DIRECTION ( 'NONE',  ( -1.000000000000000000, -0.000000000000000000, -0.000000000000000000 ) ) ;
#20073=VERTEX_POINT ( 'NONE', #1177 ) ;
#20074=LINE ( 'NONE', #40584, #37512 ) ;
#20078=VECTOR ( 'NONE', #67589, 1000.000000000000000 ) ;
#20084=DIRECTION ( 'NONE',  ( 1.836970198721029934E-16, 1.836970198721010706E-16, -1.000000000000000000 ) ) ;
#20090=CARTESIAN_POINT ( 'NONE',  ( -4.393516549646832914, -11.32648345035344128, 455.0000000000000568 ) ) ;
#20097=ORIENTED_EDGE ( 'NONE', *, *, #49363, .F. ) ;
#20098=VECTOR ( 'NONE', #29854, 1000.000000000000000 ) ;
#20100=DIRECTION ( 'NONE',  ( 0.000000000000000000, -1.000000000000000000, -3.673940397442059868E-16 ) ) ;
#20111=DIRECTION ( 'NONE',  ( 0.6414496315691592399, 0.7671651518152985405, 2.309356642088728176E-17 ) ) ;
#20116=VECTOR ( 'NONE', #31201, 1000.000000000000000 ) ;
#20117=DIRECTION ( 'NONE',  ( -1.836970198721029934E-16, 1.836970198721036344E-16, -1.000000000000000000 ) ) ;
#20127=DIRECTION ( 'NONE',  ( -1.836970198721029934E-16, 1.836970198721036344E-16, -1.000000000000000000 ) ) ;
#20132=CARTESIAN_POINT ( 'NONE',  ( 6.006483450353401921, 5.993516549646582092, 455.0000000000000568 ) ) ;
#20133=CYLINDRICAL_SURFACE ( 'NONE', #55524, 0.5999999999999989786 ) ;
#20134=CARTESIAN_POINT ( 'NONE',  ( 3.606483450353369147, -7.428221114745003462, 195.0000000000000284 ) ) ;
#20144=AXIS2_PLACEMENT_3D ( 'NONE', #58670, #2900, #42394 ) ;
#20149=VERTEX_POINT ( 'NONE', #7501 ) ;
#20153=ORIENTED_EDGE ( 'NONE', *, *, #5169, .T. ) ;
#20157=CARTESIAN_POINT ( 'NONE',  ( -3.593516549646701197, 7.415254214038210279, 195.0000000000000284 ) ) ;
#20160=ADVANCED_FACE ( 'NONE', ( #1858 ), #49940, .F. ) ;
#20161=ORIENTED_EDGE ( 'NONE', *, *, #45546, .F. ) ;
#20166=DIRECTION ( 'NONE',  ( -1.836970198721029934E-16, -1.836970198721010706E-16, 1.000000000000000000 ) ) ;
#20168=CARTESIAN_POINT ( 'NONE',  ( 11.08848345035341687, 9.791916549646563439, 455.0000000000000568 ) ) ;
#20169=ORIENTED_EDGE ( 'NONE', *, *, #40054, .T. ) ;
#20172=DIRECTION ( 'NONE',  ( 0.4999999999999695799, -0.8660254037844563602, -6.723777587269172655E-17 ) ) ;
#20179=AXIS2_PLACEMENT_3D ( 'NONE', #9107, #68512, #20760 ) ;
#20182=VERTEX_POINT ( 'NONE', #61578 ) ;
#20188=DIRECTION ( 'NONE',  ( 1.000000000000000000, -1.047444401652939849E-14, 1.836970198721010706E-16 ) ) ;
#20194=CARTESIAN_POINT ( 'NONE',  ( -7.252248008019485326, -6.619341603356823533, 195.0000000000000284 ) ) ;
#20200=DIRECTION ( 'NONE',  ( -0.000000000000000000, 1.000000000000000000, 3.673940397442059868E-16 ) ) ;
#20208=ORIENTED_EDGE ( 'NONE', *, *, #66271, .F. ) ;
#20210=CARTESIAN_POINT ( 'NONE',  ( 4.747751991980625696, -5.393625297350043368, 455.0000000000000568 ) ) ;
#20214=VERTEX_POINT ( 'NONE', #23769 ) ;
#20226=DIRECTION ( 'NONE',  ( -0.000000000000000000, -0.000000000000000000, -1.000000000000000000 ) ) ;
#20231=CYLINDRICAL_SURFACE ( 'NONE', #30864, 0.5999999999999998668 ) ;
#20251=LINE ( 'NONE', #41815, #31216 ) ;
#20253=EDGE_CURVE ( 'NONE', #1592, #34851, #3251, .T. ) ;
#20256=EDGE_LOOP ( 'NONE', ( #22021, #6771, #17920, #29701 ) ) ;
#20279=EDGE_CURVE ( 'NONE', #18478, #68006, #52769, .T. ) ;
#20283=VECTOR ( 'NONE', #39246, 1000.000000000000000 ) ;
#20284=LINE ( 'NONE', #26645, #47034 ) ;
#20301=CIRCLE ( 'NONE', #56424, 0.1999999999999996503 ) ;
#20304=EDGE_CURVE ( 'NONE', #46696, #31922, #62864, .T. ) ;
#20309=CARTESIAN_POINT ( 'NONE',  ( -7.744988412222854279, 8.452095193409293827, 455.0000000000000568 ) ) ;
#20312=LINE ( 'NONE', #31293, #64319 ) ;
#20317=ORIENTED_EDGE ( 'NONE', *, *, #45495, .T. ) ;
#20322=DIRECTION ( 'NONE',  ( -0.6414496315691592399, -0.7671651518152985405, 0.000000000000000000 ) ) ;
#20324=VERTEX_POINT ( 'NONE', #15627 ) ;
#20325=VECTOR ( 'NONE', #39021, 1000.000000000000000 ) ;
#20328=VECTOR ( 'NONE', #22522, 1000.000000000000000 ) ;
#20334=ORIENTED_EDGE ( 'NONE', *, *, #35690, .T. ) ;
#20339=ORIENTED_EDGE ( 'NONE', *, *, #45193, .F. ) ;
#20343=CIRCLE ( 'NONE', #47398, 0.2000000000000005107 ) ;
#20346=ADVANCED_FACE ( 'NONE', ( #16305 ), #43868, .F. ) ;
#20352=ORIENTED_EDGE ( 'NONE', *, *, #39753, .F. ) ;
#20359=ORIENTED_EDGE ( 'NONE', *, *, #29196, .T. ) ;
#20368=EDGE_CURVE ( 'NONE', #41995, #25935, #6392, .T. ) ;
#20383=DIRECTION ( 'NONE',  ( 1.000000000000000000, -9.050731179009442381E-15, 0.000000000000000000 ) ) ;
#20386=ORIENTED_EDGE ( 'NONE', *, *, #11252, .T. ) ;
#20389=VECTOR ( 'NONE', #42543, 1000.000000000000000 ) ;
#20397=ORIENTED_EDGE ( 'NONE', *, *, #69155, .T. ) ;
#20398=CARTESIAN_POINT ( 'NONE',  ( 6.619341603356837744, -7.265214908726242982, 455.0000000000000568 ) ) ;
#20413=EDGE_CURVE ( 'NONE', #4203, #6649, #43171, .T. ) ;
#20415=CARTESIAN_POINT ( 'NONE',  ( 8.406483450353379183, -4.396432944014562416, 195.0000000000000284 ) ) ;
#20439=ORIENTED_EDGE ( 'NONE', *, *, #1795, .F. ) ;
#20440=DIRECTION ( 'NONE',  ( 1.836970198721029934E-16, 1.836970198721010706E-16, -1.000000000000000000 ) ) ;
#20447=VERTEX_POINT ( 'NONE', #16669 ) ;
#20449=AXIS2_PLACEMENT_3D ( 'NONE', #5606, #55430, #28537 ) ;
#20452=ADVANCED_FACE ( 'NONE', ( #65443 ), #33265, .T. ) ;
#20455=DIRECTION ( 'NONE',  ( -0.000000000000000000, -0.000000000000000000, -1.000000000000000000 ) ) ;
#20457=CARTESIAN_POINT ( 'NONE',  ( -11.07551654964682086, -10.20488345035337296, 455.0000000000000568 ) ) ;
#20467=CARTESIAN_POINT ( 'NONE',  ( 6.006483450353353959, 5.993516549646629166, 195.0000000000000284 ) ) ;
#20471=CARTESIAN_POINT ( 'NONE',  ( -7.593516549646784242, -11.32648345035336312, 195.0000000000000284 ) ) ;
#20491=DIRECTION ( 'NONE',  ( 0.6414496315691494699, -0.7671651518153064231, 0.000000000000000000 ) ) ;
#20496=DIRECTION ( 'NONE',  ( -1.000000000000000000, 7.665540703601094997E-15, 0.000000000000000000 ) ) ;
#20513=CARTESIAN_POINT ( 'NONE',  ( 10.92648345035337343, -2.706483450353490916, 455.0000000000000568 ) ) ;
#20517=DIRECTION ( 'NONE',  ( -1.000000000000000000, 1.047444401652940007E-14, -1.836970198721010706E-16 ) ) ;
#20519=ORIENTED_EDGE ( 'NONE', *, *, #18158, .T. ) ;
#20522=ORIENTED_EDGE ( 'NONE', *, *, #66910, .T. ) ;
#20538=AXIS2_PLACEMENT_3D ( 'NONE', #9557, #62951, #35711 ) ;
#20541=DIRECTION ( 'NONE',  ( 8.673617379884051249E-15, 1.000000000000000000, 0.000000000000000000 ) ) ;
#20551=CARTESIAN_POINT ( 'NONE',  ( -4.188533722949335569, 7.259684009079808931, 455.0000000000000568 ) ) ;
#20552=CARTESIAN_POINT ( 'NONE',  ( -1.677516549646825839, -10.74648345035347141, 455.0000000000000568 ) ) ;
#20558=DIRECTION ( 'NONE',  ( 1.901462112903059913E-14, 1.000000000000000000, 1.836970198721045958E-16 ) ) ;
#20560=FILL_AREA_STYLE_COLOUR ( '', #22084 ) ;
#20562=CARTESIAN_POINT ( 'NONE',  ( -8.452095193409439489, -7.757955312929496472, 195.0000000000000284 ) ) ;
#20566=VERTEX_POINT ( 'NONE', #24025 ) ;
#20569=AXIS2_PLACEMENT_3D ( 'NONE', #38783, #49056, #21487 ) ;
#20574=CYLINDRICAL_SURFACE ( 'NONE', #45461, 0.1999999999999996503 ) ;
#20575=ORIENTED_EDGE ( 'NONE', *, *, #56460, .F. ) ;
#20586=EDGE_LOOP ( 'NONE', ( #62871, #28036, #60932, #13956 ) ) ;
#20589=VERTEX_POINT ( 'NONE', #18725 ) ;
#20597=DIRECTION ( 'NONE',  ( -1.000000000000000000, 0.000000000000000000, 0.000000000000000000 ) ) ;
#20605=CYLINDRICAL_SURFACE ( 'NONE', #53476, 0.4000000000000010214 ) ;
#20607=ORIENTED_EDGE ( 'NONE', *, *, #16728, .F. ) ;
#20610=VERTEX_POINT ( 'NONE', #41341 ) ;
#20616=CARTESIAN_POINT ( 'NONE',  ( 11.12648345035337982, -7.806483450353395526, 195.0000000000000284 ) ) ;
#20618=CARTESIAN_POINT ( 'NONE',  ( -11.33351654964671162, 1.077516549646603483, 455.0000000000000568 ) ) ;
#20619=ORIENTED_EDGE ( 'NONE', *, *, #40847, .F. ) ;
#20630=ADVANCED_FACE ( 'NONE', ( #4578 ), #69270, .T. ) ;
#20635=ORIENTED_EDGE ( 'NONE', *, *, #57084, .T. ) ;
#20636=CARTESIAN_POINT ( 'NONE',  ( -11.47551654964667733, 11.07551654964660237, 455.0000000000000568 ) ) ;
#20641=FACE_OUTER_BOUND ( 'NONE', #48802, .T. ) ;
#20658=ORIENTED_EDGE ( 'NONE', *, *, #62083, .T. ) ;
#20659=CARTESIAN_POINT ( 'NONE',  ( -9.093516549646826874, -10.92648345035338941, 455.0000000000000568 ) ) ;
#20667=VERTEX_POINT ( 'NONE', #13770 ) ;
#20670=EDGE_CURVE ( 'NONE', #27698, #24754, #64051, .T. ) ;
#20672=CARTESIAN_POINT ( 'NONE',  ( -11.33351654964671162, 1.077516549646603483, 195.0000000000000284 ) ) ;
#20675=EDGE_CURVE ( 'NONE', #19534, #33331, #58326, .T. ) ;
#20683=FACE_OUTER_BOUND ( 'NONE', #51183, .T. ) ;
#20685=DIRECTION ( 'NONE',  ( 0.000000000000000000, 3.673940397442059868E-16, -1.000000000000000000 ) ) ;
#20686=VECTOR ( 'NONE', #69748, 1000.000000000000000 ) ;
#20689=VERTEX_POINT ( 'NONE', #63627 ) ;
#20708=LINE ( 'NONE', #15419, #11423 ) ;
#20716=ADVANCED_FACE ( 'NONE', ( #37792 ), #33170, .F. ) ;
#20721=DIRECTION ( 'NONE',  ( -1.000000000000000000, 0.000000000000000000, 0.000000000000000000 ) ) ;
#20723=CIRCLE ( 'NONE', #53504, 0.3999999999999993006 ) ;
#20746=DIRECTION ( 'NONE',  ( 0.7671651518153029814, 0.6414496315691537998, -2.309356642088817231E-17 ) ) ;
#20749=CIRCLE ( 'NONE', #35421, 0.1999999999999992339 ) ;
#20755=ORIENTED_EDGE ( 'NONE', *, *, #39662, .F. ) ;
#20760=DIRECTION ( 'NONE',  ( 1.000000000000000000, -3.491481338843132961E-15, 0.000000000000000000 ) ) ;
#20762=EDGE_CURVE ( 'NONE', #40491, #67569, #54061, .T. ) ;
#20763=ORIENTED_EDGE ( 'NONE', *, *, #28049, .F. ) ;
#20767=ORIENTED_EDGE ( 'NONE', *, *, #34807, .F. ) ;
#20768=LINE ( 'NONE', #42337, #43045 ) ;
#20770=DIRECTION ( 'NONE',  ( -0.7071067811865446862, 0.7071067811865503483, -0.000000000000000000 ) ) ;
#20772=DIRECTION ( 'NONE',  ( -0.000000000000000000, 3.673940397442059868E-16, -1.000000000000000000 ) ) ;
#20782=SHAPE_DEFINITION_REPRESENTATION ( #23373, #35 ) ;
#20796=EDGE_LOOP ( 'NONE', ( #48940, #61565, #39592, #7404 ) ) ;
#20798=LINE ( 'NONE', #48723, #52780 ) ;
#20800=CARTESIAN_POINT ( 'NONE',  ( 6.619341603356799553, 4.734785091273873370, 195.0000000000000284 ) ) ;
#20809=EDGE_LOOP ( 'NONE', ( #7891, #5056, #18170, #15468 ) ) ;
#20811=LINE ( 'NONE', #42377, #17355 ) ;
#20820=CARTESIAN_POINT ( 'NONE',  ( -11.99351654964674729, -7.826483450353316051, 195.0000000000000284 ) ) ;
#20824=CARTESIAN_POINT ( 'NONE',  ( -6.331612867284196255, -8.406483450353375630, 195.0000000000000284 ) ) ;
#20838=AXIS2_PLACEMENT_3D ( 'NONE', #17522, #28137, #66321 ) ;
#20840=VERTEX_POINT ( 'NONE', #45772 ) ;
#20843=ORIENTED_EDGE ( 'NONE', *, *, #65185, .T. ) ;
#20846=CARTESIAN_POINT ( 'NONE',  ( -7.798499376344067535, 7.259684009079840017, 455.0000000000000568 ) ) ;
#20849=EDGE_CURVE ( 'NONE', #4435, #20840, #62027, .T. ) ;
#20857=EDGE_CURVE ( 'NONE', #3246, #39788, #40822, .T. ) ;
#20859=VERTEX_POINT ( 'NONE', #8646 ) ;
#20882=ORIENTED_EDGE ( 'NONE', *, *, #26445, .F. ) ;
#20884=PLANE ( 'NONE',  #35318 ) ;
#20888=EDGE_CURVE ( 'NONE', #54143, #8176, #53542, .T. ) ;
#20894=ORIENTED_EDGE ( 'NONE', *, *, #24591, .T. ) ;
#20902=DIRECTION ( 'NONE',  ( -0.7671651518152895477, 0.6414496315691698980, -2.309356642088442522E-17 ) ) ;
#20909=PRESENTATION_STYLE_ASSIGNMENT (( #4658 ) ) ;
#20919=CARTESIAN_POINT ( 'NONE',  ( -7.259684009079963474, -4.201500623656036382, 455.0000000000000568 ) ) ;
#20936=ORIENTED_EDGE ( 'NONE', *, *, #20413, .F. ) ;
#20941=LINE ( 'NONE', #42159, #69314 ) ;
#20944=DIRECTION ( 'NONE',  ( -1.011922027653137735E-14, -1.000000000000000000, 0.000000000000000000 ) ) ;
#20945=CARTESIAN_POINT ( 'NONE',  ( -4.383466043307969962, -8.606483450353444198, 455.0000000000000568 ) ) ;
#20948=DIRECTION ( 'NONE',  ( -1.000000000000000000, 0.000000000000000000, 0.000000000000000000 ) ) ;
#20950=ORIENTED_EDGE ( 'NONE', *, *, #67366, .F. ) ;
#20952=VERTEX_POINT ( 'NONE', #36564 ) ;
#20954=CIRCLE ( 'NONE', #60460, 0.3999999999999993006 ) ;
#20961=ORIENTED_EDGE ( 'NONE', *, *, #39906, .T. ) ;
#20963=VECTOR ( 'NONE', #14203, 1000.000000000000000 ) ;
#20976=CARTESIAN_POINT ( 'NONE',  ( 11.08848345035342042, 11.47551654964652812, 455.0000000000000568 ) ) ;
#20980=LINE ( 'NONE', #26994, #14087 ) ;
#20986=DIRECTION ( 'NONE',  ( -0.5000000000000019984, -0.8660254037844375974, -0.000000000000000000 ) ) ;
#20989=FACE_BOUND ( 'NONE', #5053, .T. ) ;
#20991=CIRCLE ( 'NONE', #6299, 2.204799999999997873 ) ;
#20998=CIRCLE ( 'NONE', #60506, 0.5999999999999998668 ) ;
#21000=VERTEX_POINT ( 'NONE', #58506 ) ;
#21019=EDGE_LOOP ( 'NONE', ( #24694, #30169, #36225, #42439 ) ) ;
#21045=VECTOR ( 'NONE', #38303, 1000.000000000000000 ) ;
#21046=VECTOR ( 'NONE', #66642, 1000.000000000000000 ) ;
#21051=VECTOR ( 'NONE', #474, 1000.000000000000114 ) ;
#21054=ORIENTED_EDGE ( 'NONE', *, *, #43069, .T. ) ;
#21063=LINE ( 'NONE', #10449, #11942 ) ;
#21064=CIRCLE ( 'NONE', #67344, 0.1999999999999987899 ) ;
#21066=EDGE_CURVE ( 'NONE', #47485, #68671, #1511, .T. ) ;
#21071=DIRECTION ( 'NONE',  ( -0.000000000000000000, -0.000000000000000000, -1.000000000000000000 ) ) ;
#21078=CARTESIAN_POINT ( 'NONE',  ( -7.415254214038336400, 2.993516549646603853, 455.0000000000000568 ) ) ;
#21080=CARTESIAN_POINT ( 'NONE',  ( -5.993516549646711766, 5.993516549646603409, 195.0000000000000284 ) ) ;
#21084=AXIS2_PLACEMENT_3D ( 'NONE', #25861, #31171, #20541 ) ;
#21085=ADVANCED_FACE ( 'NONE', ( #48931 ), #32662, .F. ) ;
#21088=DIRECTION ( 'NONE',  ( 1.836970198721029934E-16, 1.836970198721010706E-16, -1.000000000000000000 ) ) ;
#21093=CIRCLE ( 'NONE', #18809, 0.1999999999999987899 ) ;
#21094=AXIS2_PLACEMENT_3D ( 'NONE', #51469, #1983, #3043 ) ;
#21107=EDGE_CURVE ( 'NONE', #37207, #32424, #27362, .T. ) ;
#21110=LINE ( 'NONE', #58595, #19698 ) ;
#21115=ORIENTED_EDGE ( 'NONE', *, *, #4683, .T. ) ;
#21120=DIRECTION ( 'NONE',  ( -0.7071067811865550112, -0.7071067811865401342, -2.597868168706466299E-16 ) ) ;
#21123=CARTESIAN_POINT ( 'NONE',  ( -11.77351654964670935, 7.813516549646603693, 455.0000000000000568 ) ) ;
#21131=DIRECTION ( 'NONE',  ( -1.836970198721029934E-16, 1.836970198721036344E-16, -1.000000000000000000 ) ) ;
#21133=CARTESIAN_POINT ( 'NONE',  ( 11.78648345035337819, -7.826483450353491023, 455.0000000000000568 ) ) ;
#21147=VECTOR ( 'NONE', #17571, 999.9999999999998863 ) ;
#21150=ORIENTED_EDGE ( 'NONE', *, *, #69559, .F. ) ;
#21158=CIRCLE ( 'NONE', #48264, 0.5999999999999989786 ) ;
#21160=CARTESIAN_POINT ( 'NONE',  ( -8.393516549646712122, 4.383466043307770121, 455.0000000000000568 ) ) ;
#21169=DIRECTION ( 'NONE',  ( -1.000000000000000000, 0.000000000000000000, 0.000000000000000000 ) ) ;
#21185=CARTESIAN_POINT ( 'NONE',  ( 4.201500623656003519, -7.272650909786698037, 455.0000000000000568 ) ) ;
#21186=ORIENTED_EDGE ( 'NONE', *, *, #42488, .T. ) ;
#21189=LINE ( 'NONE', #31461, #69860 ) ;
#21192=ADVANCED_FACE ( 'NONE', ( #40741 ), #67967, .F. ) ;
#21197=ORIENTED_EDGE ( 'NONE', *, *, #49754, .T. ) ;
#21205=CARTESIAN_POINT ( 'NONE',  ( 12.00648345035338238, 4.173516549646515195, 455.0000000000000568 ) ) ;
#21208=VECTOR ( 'NONE', #36492, 1000.000000000000000 ) ;
#21209=VECTOR ( 'NONE', #64475, 1000.000000000000000 ) ;
#21210=DIRECTION ( 'NONE',  ( -1.836970198721029934E-16, -1.836970198721010706E-16, 1.000000000000000000 ) ) ;
#21212=ORIENTED_EDGE ( 'NONE', *, *, #17927, .F. ) ;
#21216=CARTESIAN_POINT ( 'NONE',  ( -3.593516549646701197, 7.415254214038210279, 455.0000000000000568 ) ) ;
#21217=AXIS2_PLACEMENT_3D ( 'NONE', #63440, #5455, #30912 ) ;
#21220=CARTESIAN_POINT ( 'NONE',  ( 10.09643294401454661, -2.706483450353396325, 195.0000000000000284 ) ) ;
#21228=AXIS2_PLACEMENT_3D ( 'NONE', #29579, #67067, #18622 ) ;
#21236=ORIENTED_EDGE ( 'NONE', *, *, #35527, .T. ) ;
#21247=ORIENTED_EDGE ( 'NONE', *, *, #21833, .T. ) ;
#21248=DIRECTION ( 'NONE',  ( -0.000000000000000000, -0.000000000000000000, -1.000000000000000000 ) ) ;
#21254=FACE_OUTER_BOUND ( 'NONE', #44003, .T. ) ;
#21260=EDGE_CURVE ( 'NONE', #14532, #7744, #45329, .T. ) ;
#21261=DIRECTION ( 'NONE',  ( -0.000000000000000000, -0.000000000000000000, -1.000000000000000000 ) ) ;
#21266=DIRECTION ( 'NONE',  ( -1.836970198721029934E-16, 1.836970198721036344E-16, -1.000000000000000000 ) ) ;
#21276=ORIENTED_EDGE ( 'NONE', *, *, #8202, .T. ) ;
#21278=DIRECTION ( 'NONE',  ( 0.000000000000000000, 0.000000000000000000, 1.000000000000000000 ) ) ;
#21281=DIRECTION ( 'NONE',  ( 0.000000000000000000, 0.000000000000000000, 1.000000000000000000 ) ) ;
#21293=PLANE ( 'NONE',  #17100 ) ;
#21294=ORIENTED_EDGE ( 'NONE', *, *, #12049, .T. ) ;
#21296=DIRECTION ( 'NONE',  ( -0.7071067811865474617, -0.7071067811865474617, -2.597868168706479611E-16 ) ) ;
#21301=DIRECTION ( 'NONE',  ( 0.000000000000000000, 3.673940397442059868E-16, -1.000000000000000000 ) ) ;
#21308=LINE ( 'NONE', #1128, #43369 ) ;
#21312=ORIENTED_EDGE ( 'NONE', *, *, #53464, .T. ) ;
#21318=LINE ( 'NONE', #42871, #34247 ) ;
#21327=ORIENTED_EDGE ( 'NONE', *, *, #19789, .T. ) ;
#21333=CARTESIAN_POINT ( 'NONE',  ( 4.740315990920131561, -7.811466277050742590, 195.0000000000000284 ) ) ;
#21337=CARTESIAN_POINT ( 'NONE',  ( 7.826483450353380000, -11.78648345035339418, 195.0000000000000284 ) ) ;
#21340=EDGE_CURVE ( 'NONE', #68617, #6256, #58763, .T. ) ;
#21347=ORIENTED_EDGE ( 'NONE', *, *, #67768, .F. ) ;
#21348=LINE ( 'NONE', #10389, #46165 ) ;
#21349=VECTOR ( 'NONE', #27992, 1000.000000000000000 ) ;
#21354=CARTESIAN_POINT ( 'NONE',  ( -7.603567055985634759, -8.406483450353409381, 455.0000000000000568 ) ) ;
#21355=DIRECTION ( 'NONE',  ( 1.356437060717834182E-15, 1.000000000000000000, 1.836970198721033878E-16 ) ) ;
#21369=ORIENTED_EDGE ( 'NONE', *, *, #47204, .T. ) ;
#21373=DIRECTION ( 'NONE',  ( 0.000000000000000000, -1.000000000000000000, 0.000000000000000000 ) ) ;
#21380=VERTEX_POINT ( 'NONE', #33615 ) ;
#21391=CARTESIAN_POINT ( 'NONE',  ( -2.693516549646820746, -10.09643294401462832, 455.0000000000000568 ) ) ;
#21398=DIRECTION ( 'NONE',  ( -1.000000000000000000, 3.491481338843133355E-15, 1.836970198721036344E-16 ) ) ;
#21401=EDGE_LOOP ( 'NONE', ( #24971, #31534, #18122, #53855 ) ) ;
#21403=ORIENTED_EDGE ( 'NONE', *, *, #29728, .T. ) ;
#21404=CARTESIAN_POINT ( 'NONE',  ( -5.993516549646776603, -6.006483450353426790, 455.0000000000000568 ) ) ;
#21405=DIRECTION ( 'NONE',  ( -0.000000000000000000, 3.673940397442059868E-16, -1.000000000000000000 ) ) ;
#21413=CIRCLE ( 'NONE', #12343, 0.8128000000000145109 ) ;
#21418=EDGE_CURVE ( 'NONE', #37177, #51945, #765, .T. ) ;
#21423=EDGE_CURVE ( 'NONE', #60071, #33734, #49875, .T. ) ;
#21458=ORIENTED_EDGE ( 'NONE', *, *, #12768, .T. ) ;
#21470=CARTESIAN_POINT ( 'NONE',  ( 11.34648345035334671, 1.077516549646521327, 455.0000000000000568 ) ) ;
#21472=LINE ( 'NONE', #54016, #49424 ) ;
#21487=DIRECTION ( 'NONE',  ( 0.000000000000000000, 1.000000000000000000, 0.000000000000000000 ) ) ;
#21489=DIRECTION ( 'NONE',  ( -1.836970198721029934E-16, 1.836970198721036344E-16, -1.000000000000000000 ) ) ;
#21490=CIRCLE ( 'NONE', #64411, 0.5999999999999998668 ) ;
#21491=LINE ( 'NONE', #4543, #61063 ) ;
#21498=AXIS2_PLACEMENT_3D ( 'NONE', #67087, #18643, #13695 ) ;
#21500=DIRECTION ( 'NONE',  ( -1.000000000000000000, 0.000000000000000000, 0.000000000000000000 ) ) ;
#21502=ORIENTED_EDGE ( 'NONE', *, *, #36058, .F. ) ;
#21503=DIRECTION ( 'NONE',  ( 0.000000000000000000, 3.673940397442059868E-16, -1.000000000000000000 ) ) ;
#21505=EDGE_CURVE ( 'NONE', #29254, #37032, #51621, .T. ) ;
#21513=CARTESIAN_POINT ( 'NONE',  ( 4.201500623656003519, -4.740315990920286104, 455.0000000000000568 ) ) ;
#21514=DIRECTION ( 'NONE',  ( -1.836970198721029934E-16, 1.836970198721036344E-16, -1.000000000000000000 ) ) ;
#21517=VERTEX_POINT ( 'NONE', #44916 ) ;
#21528=CARTESIAN_POINT ( 'NONE',  ( -11.99351654964671354, 4.173516549646604901, 455.0000000000000568 ) ) ;
#21533=ORIENTED_EDGE ( 'NONE', *, *, #60371, .T. ) ;
#21534=DIRECTION ( 'NONE',  ( 0.6414496315691367023, -0.7671651518153173033, -2.309356642089295169E-17 ) ) ;
#21536=DIRECTION ( 'NONE',  ( 1.047444401652940007E-14, 1.000000000000000000, 1.836970198721029934E-16 ) ) ;
#21553=EDGE_LOOP ( 'NONE', ( #1508, #9994, #45883, #11361 ) ) ;
#21555=CARTESIAN_POINT ( 'NONE',  ( 11.19368345035340973, 11.99351654964656433, 455.0000000000000568 ) ) ;
#21568=LINE ( 'NONE', #37145, #29914 ) ;
#21569=ORIENTED_EDGE ( 'NONE', *, *, #44083, .T. ) ;
#21572=DIRECTION ( 'NONE',  ( -0.000000000000000000, -0.000000000000000000, -1.000000000000000000 ) ) ;
#21578=VECTOR ( 'NONE', #11555, 1000.000000000000000 ) ;
#21581=VERTEX_POINT ( 'NONE', #42408 ) ;
#21594=ORIENTED_EDGE ( 'NONE', *, *, #2023, .F. ) ;
#21597=DIRECTION ( 'NONE',  ( -1.047444401652939849E-14, -1.000000000000000000, -1.836970198721029934E-16 ) ) ;
#21602=CARTESIAN_POINT ( 'NONE',  ( -7.813516549646839948, -12.00648345035340903, 455.0000000000000568 ) ) ;
#21604=ADVANCED_FACE ( 'NONE', ( #30755 ), #31470, .F. ) ;
#21608=DIRECTION ( 'NONE',  ( 0.000000000000000000, -3.673940397442059868E-16, 1.000000000000000000 ) ) ;
#21609=VECTOR ( 'NONE', #50661, 1000.000000000000000 ) ;
#21611=DIRECTION ( 'NONE',  ( -1.000000000000000000, 0.000000000000000000, 0.000000000000000000 ) ) ;
#21617=PLANE ( 'NONE',  #15318 ) ;
#21629=VERTEX_POINT ( 'NONE', #37119 ) ;
#21631=DIRECTION ( 'NONE',  ( -0.6414496315691473605, -0.7671651518153083105, -2.309356642089130002E-17 ) ) ;
#21634=EDGE_LOOP ( 'NONE', ( #9751, #399, #48864, #14768 ) ) ;
#21643=CARTESIAN_POINT ( 'NONE',  ( 4.622483450353380263, -3.606483450353491271, 455.0000000000000568 ) ) ;
#21650=CARTESIAN_POINT ( 'NONE',  ( -10.08346604330788665, -2.906483450353353426, 455.0000000000000568 ) ) ;
#21652=ADVANCED_FACE ( 'NONE', ( #42755 ), #32505, .F. ) ;
#21654=DIRECTION ( 'NONE',  ( -0.000000000000000000, -0.000000000000000000, -1.000000000000000000 ) ) ;
#21655=DIRECTION ( 'NONE',  ( -0.000000000000000000, 3.673940397442059868E-16, -1.000000000000000000 ) ) ;
#21670=ORIENTED_EDGE ( 'NONE', *, *, #22133, .T. ) ;
#21674=DIRECTION ( 'NONE',  ( 4.336808689942006692E-15, 1.000000000000000000, 0.000000000000000000 ) ) ;
#21676=VERTEX_POINT ( 'NONE', #65710 ) ;
#21677=ADVANCED_FACE ( 'NONE', ( #11262 ), #5631, .F. ) ;
#21679=DIRECTION ( 'NONE',  ( 1.836970198721029934E-16, 1.836970198721010706E-16, -1.000000000000000000 ) ) ;
#21682=ADVANCED_BREP_SHAPE_REPRESENTATION ( '', ( #43625, #45918 ), #47199 ) ;
#21683=PLANE ( 'NONE',  #29104 ) ;
#21693=VECTOR ( 'NONE', #53438, 1000.000000000000000 ) ;
#21695=ORIENTED_EDGE ( 'NONE', *, *, #57844, .T. ) ;
#21697=EDGE_CURVE ( 'NONE', #61197, #48072, #48761, .T. ) ;
#21711=VERTEX_POINT ( 'NONE', #4933 ) ;
#21719=DIRECTION ( 'NONE',  ( 4.121462285523434951E-16, 1.000000000000000000, 3.673940397442059868E-16 ) ) ;
#21724=EDGE_LOOP ( 'NONE', ( #17491, #53574, #11184, #40286 ) ) ;
#21727=DIRECTION ( 'NONE',  ( -0.000000000000000000, -0.000000000000000000, -1.000000000000000000 ) ) ;
#21746=VERTEX_POINT ( 'NONE', #56142 ) ;
#21748=DIRECTION ( 'NONE',  ( 1.000000000000000000, -1.813998472013049506E-14, 0.000000000000000000 ) ) ;
#21751=AXIS2_PLACEMENT_3D ( 'NONE', #50673, #7178, #66590 ) ;
#21756=CARTESIAN_POINT ( 'NONE',  ( 7.606483450353380249, -11.78648345035349010, 455.0000000000000568 ) ) ;
#21759=VECTOR ( 'NONE', #40842, 1000.000000000000000 ) ;
#21762=ORIENTED_EDGE ( 'NONE', *, *, #26637, .F. ) ;
#21765=CARTESIAN_POINT ( 'NONE',  ( -3.593516549646712299, 4.609516549646604844, 455.0000000000000568 ) ) ;
#21766=AXIS2_PLACEMENT_3D ( 'NONE', #51604, #44534, #12699 ) ;
#21770=ADVANCED_FACE ( 'NONE', ( #6989 ), #28221, .F. ) ;
#21772=DIRECTION ( 'NONE',  ( 1.000000000000000000, 0.000000000000000000, 0.000000000000000000 ) ) ;
#21775=EDGE_CURVE ( 'NONE', #42524, #24992, #37751, .T. ) ;
#21778=DIRECTION ( 'NONE',  ( -4.121462285523434951E-16, -1.000000000000000000, -0.000000000000000000 ) ) ;
#21783=LINE ( 'NONE', #31710, #3111 ) ;
#21785=AXIS2_PLACEMENT_3D ( 'NONE', #26389, #217, #54308 ) ;
#21807=CARTESIAN_POINT ( 'NONE',  ( 7.428221114745000797, 3.593516549646565750, 455.0000000000000568 ) ) ;
#21812=ORIENTED_EDGE ( 'NONE', *, *, #67041, .F. ) ;
#21814=ORIENTED_EDGE ( 'NONE', *, *, #33705, .T. ) ;
#21815=LINE ( 'NONE', #31743, #164 ) ;
#21816=EDGE_CURVE ( 'NONE', #31048, #5249, #36627, .T. ) ;
#21819=LINE ( 'NONE', #6249, #63224 ) ;
#21822=ORIENTED_EDGE ( 'NONE', *, *, #6637, .T. ) ;
#21825=DIRECTION ( 'NONE',  ( -1.836970198721029934E-16, -1.836970198721010706E-16, 1.000000000000000000 ) ) ;
#21833=EDGE_CURVE ( 'NONE', #27500, #27698, #18290, .T. ) ;
#21843=DIRECTION ( 'NONE',  ( -0.000000000000000000, -0.000000000000000000, -1.000000000000000000 ) ) ;
#21844=CARTESIAN_POINT ( 'NONE',  ( -2.993516549646701108, 7.415254214038204061, 455.0000000000000568 ) ) ;
#21854=VECTOR ( 'NONE', #11517, 1000.000000000000000 ) ;
#21864=DIRECTION ( 'NONE',  ( 2.135044278125299371E-15, 1.000000000000000000, 0.000000000000000000 ) ) ;
#21881=EDGE_CURVE ( 'NONE', #7012, #4376, #44469, .T. ) ;
#21883=DIRECTION ( 'NONE',  ( -1.000000000000000000, 0.000000000000000000, 0.000000000000000000 ) ) ;
#21886=DIRECTION ( 'NONE',  ( 0.7671651518153106419, 0.6414496315691445849, 0.000000000000000000 ) ) ;
#21890=CIRCLE ( 'NONE', #44423, 0.1999999999999996503 ) ;
#21904=FACE_OUTER_BOUND ( 'NONE', #17204, .T. ) ;
#21910=DIRECTION ( 'NONE',  ( -1.000000000000000000, 0.000000000000000000, 0.000000000000000000 ) ) ;
#21914=VERTEX_POINT ( 'NONE', #24661 ) ;
#21916=ADVANCED_FACE ( 'NONE', ( #20055 ), #63187, .F. ) ;
#21926=EDGE_LOOP ( 'NONE', ( #50635, #64852, #38694, #2315 ) ) ;
#21932=DIRECTION ( 'NONE',  ( 3.491481338843133355E-15, 1.000000000000000000, 1.836970198721029934E-16 ) ) ;
#21936=CARTESIAN_POINT ( 'NONE',  ( 9.955011587777223170, 2.752095193409229257, 455.0000000000000568 ) ) ;
#21938=EDGE_LOOP ( 'NONE', ( #44122, #34810, #4121, #38843 ) ) ;
#21959=VECTOR ( 'NONE', #29076, 1000.000000000000000 ) ;
#21961=CARTESIAN_POINT ( 'NONE',  ( -4.173516549646666185, 11.99351654964658920, 455.0000000000000568 ) ) ;
#21963=ORIENTED_EDGE ( 'NONE', *, *, #36177, .T. ) ;
#21978=CARTESIAN_POINT ( 'NONE',  ( -7.813516549646836395, -11.78648345035340661, 455.0000000000000568 ) ) ;
#21992=EDGE_CURVE ( 'NONE', #7898, #68617, #41970, .T. ) ;
#21995=LINE ( 'NONE', #11377, #24373 ) ;
#21996=CARTESIAN_POINT ( 'NONE',  ( -9.093516549646711411, 11.11351654964659730, 455.0000000000000568 ) ) ;
#22004=CARTESIAN_POINT ( 'NONE',  ( -11.11351654964675539, -9.106483450353326958, 195.0000000000000284 ) ) ;
#22021=ORIENTED_EDGE ( 'NONE', *, *, #55564, .F. ) ;
#22033=DIRECTION ( 'NONE',  ( -0.000000000000000000, 3.673940397442059868E-16, -1.000000000000000000 ) ) ;
#22034=CARTESIAN_POINT ( 'NONE',  ( -9.828310488886000229, -2.290483450353309358, 195.0000000000000284 ) ) ;
#22040=FACE_BOUND ( 'NONE', #49911, .T. ) ;
#22041=EDGE_CURVE ( 'NONE', #51945, #20060, #21110, .T. ) ;
#22043=DIRECTION ( 'NONE',  ( 1.000000000000000000, 0.000000000000000000, 0.000000000000000000 ) ) ;
#22044=DIRECTION ( 'NONE',  ( 0.7071067811865537900, 0.7071067811865412445, -1.896300252935124802E-30 ) ) ;
#22050=VECTOR ( 'NONE', #40402, 1000.000000000000000 ) ;
#22053=DIRECTION ( 'NONE',  ( 0.8660254037844510311, 0.4999999999999785727, 1.836970198720951294E-16 ) ) ;
#22055=VECTOR ( 'NONE', #47929, 1000.000000000000000 ) ;
#22057=AXIS2_PLACEMENT_3D ( 'NONE', #41656, #30705, #56859 ) ;
#22065=VECTOR ( 'NONE', #46592, 1000.000000000000000 ) ;
#22084=COLOUR_RGB ( '', 0.66274510, 0.83137255, 0.94901961) ;
#22085=PLANE ( 'NONE',  #26607 ) ;
#22099=VECTOR ( 'NONE', #6659, 1000.000000000000000 ) ;
#22122=CARTESIAN_POINT ( 'NONE',  ( 1.090483450353338268, -11.34648345035345329, 455.0000000000000568 ) ) ;
#22125=VERTEX_POINT ( 'NONE', #16145 ) ;
#22133=EDGE_CURVE ( 'NONE', #44422, #40712, #26293, .T. ) ;
#22136=CARTESIAN_POINT ( 'NONE',  ( -11.11351654964668789, 8.333516549646644123, 195.0000000000000284 ) ) ;
#22138=CARTESIAN_POINT ( 'NONE',  ( -4.188533722949335569, 4.727349090213398775, 455.0000000000000568 ) ) ;
#22164=VECTOR ( 'NONE', #27647, 1000.000000000000114 ) ;
#22170=ORIENTED_EDGE ( 'NONE', *, *, #50611, .T. ) ;
#22171=ORIENTED_EDGE ( 'NONE', *, *, #44959, .T. ) ;
#22175=DIRECTION ( 'NONE',  ( -0.000000000000000000, 0.000000000000000000, -1.000000000000000000 ) ) ;
#22187=EDGE_CURVE ( 'NONE', #63906, #30476, #8971, .T. ) ;
#22188=VERTEX_POINT ( 'NONE', #68378 ) ;
#22194=ORIENTED_EDGE ( 'NONE', *, *, #59905, .T. ) ;
#22220=VERTEX_POINT ( 'NONE', #31273 ) ;
#22241=LINE ( 'NONE', #65375, #52296 ) ;
#22257=CARTESIAN_POINT ( 'NONE',  ( 10.20488345035340494, 9.791916549646614953, 195.0000000000000284 ) ) ;
#22260=AXIS2_PLACEMENT_3D ( 'NONE', #33362, #23445, #65540 ) ;
#22267=ADVANCED_FACE ( 'NONE', ( #19938 ), #3328, .F. ) ;
#22280=EDGE_CURVE ( 'NONE', #1298, #26074, #20284, .T. ) ;
#22288=DIRECTION ( 'NONE',  ( 1.836970198721029934E-16, -1.836970198721036344E-16, 1.000000000000000000 ) ) ;
#22294=DIRECTION ( 'NONE',  ( -0.000000000000000000, -0.000000000000000000, -1.000000000000000000 ) ) ;
#22297=CARTESIAN_POINT ( 'NONE',  ( 9.955011587777235604, -2.765062094116182312, 455.0000000000000568 ) ) ;
#22308=DIRECTION ( 'NONE',  ( -1.000000000000000000, -5.013651664672856055E-16, -1.841985738954423698E-31 ) ) ;
#22312=DIRECTION ( 'NONE',  ( 1.000000000000000000, 0.000000000000000000, 0.000000000000000000 ) ) ;
#22314=VECTOR ( 'NONE', #27628, 1000.000000000000000 ) ;
#22315=AXIS2_PLACEMENT_3D ( 'NONE', #15331, #30894, #57408 ) ;
#22317=VERTEX_POINT ( 'NONE', #22388 ) ;
#22319=EDGE_CURVE ( 'NONE', #8790, #57591, #43246, .T. ) ;
#22320=EDGE_CURVE ( 'NONE', #28515, #27839, #36858, .T. ) ;
#22332=CARTESIAN_POINT ( 'NONE',  ( 7.265214908726155052, 6.606374702650035680, 455.0000000000000568 ) ) ;
#22333=EDGE_CURVE ( 'NONE', #61486, #36045, #49257, .T. ) ;
#22335=EDGE_CURVE ( 'NONE', #40341, #9194, #35715, .T. ) ;
#22343=CARTESIAN_POINT ( 'NONE',  ( 8.406483450353348985, 5.655420232009159776, 195.0000000000000284 ) ) ;
#22346=ORIENTED_EDGE ( 'NONE', *, *, #10003, .F. ) ;
#22351=FACE_OUTER_BOUND ( 'NONE', #25914, .T. ) ;
#22360=ORIENTED_EDGE ( 'NONE', *, *, #16379, .T. ) ;
#22374=VERTEX_POINT ( 'NONE', #69789 ) ;
#22375=ORIENTED_EDGE ( 'NONE', *, *, #56446, .F. ) ;
#22376=DIRECTION ( 'NONE',  ( -0.8660254037844347108, 0.5000000000000069944, 2.509347957447884214E-16 ) ) ;
#22377=ADVANCED_FACE ( 'NONE', ( #64481 ), #5445, .F. ) ;
#22382=DIRECTION ( 'NONE',  ( 1.836970198721029934E-16, -1.836970198721036344E-16, 1.000000000000000000 ) ) ;
#22388=CARTESIAN_POINT ( 'NONE',  ( -11.99351654964671354, 7.813516549646603693, 455.0000000000000568 ) ) ;
#22391=LINE ( 'NONE', #33337, #21051 ) ;
#22396=VERTEX_POINT ( 'NONE', #33335 ) ;
#22399=EDGE_CURVE ( 'NONE', #53770, #18339, #48911, .T. ) ;
#22407=ADVANCED_FACE ( 'NONE', ( #16039 ), #60192, .F. ) ;
#22430=CARTESIAN_POINT ( 'NONE',  ( 4.396432944014576627, 8.393516549646587777, 455.0000000000000568 ) ) ;
#22446=EDGE_CURVE ( 'NONE', #69428, #28943, #46024, .T. ) ;
#22447=DIRECTION ( 'NONE',  ( 1.000000000000000000, -1.047444401652939849E-14, 1.836970198721010706E-16 ) ) ;
#22452=VECTOR ( 'NONE', #26348, 1000.000000000000000 ) ;
#22453=ORIENTED_EDGE ( 'NONE', *, *, #42707, .T. ) ;
#22475=ADVANCED_FACE ( 'NONE', ( #29060 ), #6789, .F. ) ;
#22476=VECTOR ( 'NONE', #32495, 1000.000000000000000 ) ;
#22477=VECTOR ( 'NONE', #43245, 1000.000000000000000 ) ;
#22487=DIRECTION ( 'NONE',  ( -1.000000000000000000, 3.491481338843133355E-15, 1.836970198721036344E-16 ) ) ;
#22489=DIRECTION ( 'NONE',  ( -1.836970198721029934E-16, 1.836970198721036344E-16, -1.000000000000000000 ) ) ;
#22492=ORIENTED_EDGE ( 'NONE', *, *, #24942, .T. ) ;
#22499=CARTESIAN_POINT ( 'NONE',  ( 4.201500623656003519, -7.272650909786602114, 195.0000000000000284 ) ) ;
#22501=AXIS2_PLACEMENT_3D ( 'NONE', #64420, #1099, #27287 ) ;
#22505=AXIS2_PLACEMENT_3D ( 'NONE', #23712, #39959, #51996 ) ;
#22513=CIRCLE ( 'NONE', #30437, 0.5999999999999998668 ) ;
#22514=DIRECTION ( 'NONE',  ( 1.000000000000000000, 1.671920889371702657E-15, 0.000000000000000000 ) ) ;
#22520=CIRCLE ( 'NONE', #65474, 1.399999999999999245 ) ;
#22522=DIRECTION ( 'NONE',  ( 1.000000000000000000, -1.088659024508174415E-14, 1.836970198721009966E-16 ) ) ;
#22523=DIRECTION ( 'NONE',  ( 7.457533623526253657E-15, 1.000000000000000000, 0.000000000000000000 ) ) ;
#22525=VERTEX_POINT ( 'NONE', #34706 ) ;
#22530=ORIENTED_EDGE ( 'NONE', *, *, #41299, .F. ) ;
#22533=ORIENTED_EDGE ( 'NONE', *, *, #21066, .T. ) ;
#22537=ORIENTED_EDGE ( 'NONE', *, *, #23998, .T. ) ;
#22552=ORIENTED_EDGE ( 'NONE', *, *, #9055, .T. ) ;
#22554=VECTOR ( 'NONE', #60806, 1000.000000000000000 ) ;
#22562=FACE_OUTER_BOUND ( 'NONE', #60705, .T. ) ;
#22570=CYLINDRICAL_SURFACE ( 'NONE', #18301, 0.1999999999999996503 ) ;
#22581=CYLINDRICAL_SURFACE ( 'NONE', #12434, 0.6000000000000005329 ) ;
#22589=CARTESIAN_POINT ( 'NONE',  ( -11.99351654964671354, 4.173516549646604901, 455.0000000000000568 ) ) ;
#22591=ORIENTED_EDGE ( 'NONE', *, *, #62083, .F. ) ;
#22595=VECTOR ( 'NONE', #44841, 1000.000000000000000 ) ;
#22600=VECTOR ( 'NONE', #16494, 1000.000000000000000 ) ;
#22601=PLANE ( 'NONE',  #23062 ) ;
#22609=ORIENTED_EDGE ( 'NONE', *, *, #42532, .F. ) ;
#22610=EDGE_CURVE ( 'NONE', #11813, #66424, #55870, .T. ) ;
#22611=ORIENTED_EDGE ( 'NONE', *, *, #33177, .F. ) ;
#22614=ADVANCED_FACE ( 'NONE', ( #7074 ), #28641, .F. ) ;
#22617=CIRCLE ( 'NONE', #50804, 0.5999999999999998668 ) ;
#22624=DIRECTION ( 'NONE',  ( 0.000000000000000000, 3.673940397442059868E-16, -1.000000000000000000 ) ) ;
#22642=VECTOR ( 'NONE', #42813, 1000.000000000000000 ) ;
#22647=( NAMED_UNIT ( * ) SI_UNIT ( $, .STERADIAN. ) SOLID_ANGLE_UNIT ( ) );
#22650=ORIENTED_EDGE ( 'NONE', *, *, #6572, .F. ) ;
#22655=AXIS2_PLACEMENT_3D ( 'NONE', #58921, #26057, #15087 ) ;
#22658=CARTESIAN_POINT ( 'NONE',  ( 7.616533956692213003, -8.406483450353491094, 455.0000000000000568 ) ) ;
#22666=CARTESIAN_POINT ( 'NONE',  ( 3.606483450353380249, -4.622483450353491286, 455.0000000000000568 ) ) ;
#22668=FACE_OUTER_BOUND ( 'NONE', #45376, .T. ) ;
#22673=CARTESIAN_POINT ( 'NONE',  ( -4.242044687070659847, -8.465062094116134972, 455.0000000000000568 ) ) ;
#22676=ORIENTED_EDGE ( 'NONE', *, *, #25989, .F. ) ;
#22680=ORIENTED_EDGE ( 'NONE', *, *, #33886, .F. ) ;
#22681=PLANE ( 'NONE',  #23586 ) ;
#22686=LINE ( 'NONE', #12064, #52417 ) ;
#22694=ADVANCED_FACE ( 'NONE', ( #7770 ), #68132, .F. ) ;
#22695=LINE ( 'NONE', #39971, #47946 ) ;
#22701=CARTESIAN_POINT ( 'NONE',  ( 4.740315990920129785, -4.201500623656146516, 455.0000000000000568 ) ) ;
#22710=ORIENTED_EDGE ( 'NONE', *, *, #67549, .F. ) ;
#22727=CARTESIAN_POINT ( 'NONE',  ( -11.99351654964679526, -7.826483450353362237, 455.0000000000000568 ) ) ;
#22729=CARTESIAN_POINT ( 'NONE',  ( 10.74648345035337904, -1.690483450353491124, 455.0000000000000568 ) ) ;
#22736=EDGE_CURVE ( 'NONE', #32917, #17706, #16614, .T. ) ;
#22738=CARTESIAN_POINT ( 'NONE',  ( -10.08346604330788132, -2.706483450353354581, 455.0000000000000568 ) ) ;
#22740=CARTESIAN_POINT ( 'NONE',  ( 2.765062094116107705, 9.942044687070449527, 455.0000000000000568 ) ) ;
#22742=ORIENTED_EDGE ( 'NONE', *, *, #14636, .T. ) ;
#22747=CARTESIAN_POINT ( 'NONE',  ( 3.430747519065335815, 7.839518282750141509, 455.0000000000000568 ) ) ;
#22750=LINE ( 'NONE', #50659, #11872 ) ;
#22756=CARTESIAN_POINT ( 'NONE',  ( 11.08848345035334404, -10.20488345035352928, 455.0000000000000568 ) ) ;
#22761=DIRECTION ( 'NONE',  ( 4.336808689942043768E-15, 1.000000000000000000, 0.000000000000000000 ) ) ;
#22771=CARTESIAN_POINT ( 'NONE',  ( -11.11351654964670743, 2.893516549646604208, 455.0000000000000568 ) ) ;
#22775=CARTESIAN_POINT ( 'NONE',  ( 0.000000000000000000, 0.000000000000000000, 0.000000000000000000 ) ) ;
#22783=ORIENTED_EDGE ( 'NONE', *, *, #69352, .F. ) ;
#22785=EDGE_LOOP ( 'NONE', ( #14958, #46418, #33895, #41151 ) ) ;
#22792=ORIENTED_EDGE ( 'NONE', *, *, #69155, .F. ) ;
#22797=LINE ( 'NONE', #5508, #18260 ) ;
#22816=ADVANCED_FACE ( 'NONE', ( #47271 ), #63885, .F. ) ;
#22841=ORIENTED_EDGE ( 'NONE', *, *, #41518, .F. ) ;
#22843=EDGE_CURVE ( 'NONE', #44680, #62302, #18210, .T. ) ;
#22857=FACE_OUTER_BOUND ( 'NONE', #36974, .T. ) ;
#22861=ORIENTED_EDGE ( 'NONE', *, *, #16410, .T. ) ;
#22862=CARTESIAN_POINT ( 'NONE',  ( 11.19368345035336709, -12.00648345035349251, 455.0000000000000568 ) ) ;
#22865=DIRECTION ( 'NONE',  ( 7.665540703601096574E-15, 1.000000000000000000, -0.000000000000000000 ) ) ;
#22868=VERTEX_POINT ( 'NONE', #39426 ) ;
#22871=EDGE_CURVE ( 'NONE', #47459, #38948, #62879, .T. ) ;
#22872=FACE_OUTER_BOUND ( 'NONE', #65726, .T. ) ;
#22883=AXIS2_PLACEMENT_3D ( 'NONE', #25882, #68667, #51428 ) ;
#22885=DIRECTION ( 'NONE',  ( 0.000000000000000000, 1.000000000000000000, 0.000000000000000000 ) ) ;
#22886=CARTESIAN_POINT ( 'NONE',  ( 6.619341603356827974, 7.252248008019368974, 195.0000000000000284 ) ) ;
#22902=CIRCLE ( 'NONE', #56810, 0.6000000000000006439 ) ;
#22916=DIRECTION ( 'NONE',  ( -1.000000000000000000, 0.000000000000000000, 0.000000000000000000 ) ) ;
#22923=VERTEX_POINT ( 'NONE', #44724 ) ;
#22926=DIRECTION ( 'NONE',  ( 0.7071067811865348052, -0.7071067811865602293, -3.278703137324831017E-30 ) ) ;
#22935=ORIENTED_EDGE ( 'NONE', *, *, #69227, .T. ) ;
#22946=VERTEX_POINT ( 'NONE', #50733 ) ;
#22957=AXIS2_PLACEMENT_3D ( 'NONE', #12213, #60997, #6586 ) ;
#22961=ORIENTED_EDGE ( 'NONE', *, *, #9025, .F. ) ;
#22966=PLANE ( 'NONE',  #55401 ) ;
#22973=DIRECTION ( 'NONE',  ( 0.6414496315691494699, -0.7671651518153064231, 0.000000000000000000 ) ) ;
#22974=DIRECTION ( 'NONE',  ( 0.000000000000000000, -3.673940397442059868E-16, 1.000000000000000000 ) ) ;
#22976=DIRECTION ( 'NONE',  ( 3.717264591378875951E-15, 1.000000000000000000, 0.000000000000000000 ) ) ;
#22983=CARTESIAN_POINT ( 'NONE',  ( -4.188533722949417282, -4.740315990920195510, 455.0000000000000568 ) ) ;
#23000=EDGE_CURVE ( 'NONE', #19035, #59906, #52143, .T. ) ;
#23006=ORIENTED_EDGE ( 'NONE', *, *, #18988, .F. ) ;
#23007=CARTESIAN_POINT ( 'NONE',  ( 3.606483450353397568, 4.609516549646590633, 455.0000000000000568 ) ) ;
#23010=CARTESIAN_POINT ( 'NONE',  ( 11.12648345035337982, -7.806483450353395526, 195.0000000000000284 ) ) ;
#23011=CARTESIAN_POINT ( 'NONE',  ( -11.11351654964679270, -7.806483450353373321, 455.0000000000000568 ) ) ;
#23017=ORIENTED_EDGE ( 'NONE', *, *, #19345, .T. ) ;
#23022=DIRECTION ( 'NONE',  ( -1.836970198721029934E-16, 1.836970198721036344E-16, -1.000000000000000000 ) ) ;
#23030=ORIENTED_EDGE ( 'NONE', *, *, #32377, .F. ) ;
#23031=LINE ( 'NONE', #28334, #25328 ) ;
#23033=FACE_OUTER_BOUND ( 'NONE', #20796, .T. ) ;
#23036=ORIENTED_EDGE ( 'NONE', *, *, #48075, .T. ) ;
#23043=ORIENTED_EDGE ( 'NONE', *, *, #37299, .T. ) ;
#23052=ORIENTED_EDGE ( 'NONE', *, *, #8302, .F. ) ;
#23062=AXIS2_PLACEMENT_3D ( 'NONE', #17969, #66064, #7011 ) ;
#23066=ORIENTED_EDGE ( 'NONE', *, *, #38966, .T. ) ;
#23068=CYLINDRICAL_SURFACE ( 'NONE', #60347, 1.399999999999999245 ) ;
#23072=CIRCLE ( 'NONE', #36610, 0.1999999999999987899 ) ;
#23075=ORIENTED_EDGE ( 'NONE', *, *, #20857, .F. ) ;
#23078=EDGE_CURVE ( 'NONE', #35467, #51761, #57093, .T. ) ;
#23081=ORIENTED_EDGE ( 'NONE', *, *, #43961, .F. ) ;
#23085=EDGE_LOOP ( 'NONE', ( #14355, #14447, #14759, #22792, #23795, #4222, #9534, #3102, #67666, #60357, #14758, #23441, #52011, #51414, #13243, #27208, #31781 ) ) ;
#23089=DIRECTION ( 'NONE',  ( 1.000000000000000000, -6.308085367188447236E-15, -2.317552966102676720E-30 ) ) ;
#23094=DIRECTION ( 'NONE',  ( -1.000000000000000000, 1.079558018506126467E-14, 1.836970198721049656E-16 ) ) ;
#23096=VECTOR ( 'NONE', #10487, 1000.000000000000114 ) ;
#23104=VECTOR ( 'NONE', #48774, 1000.000000000000000 ) ;
#23108=VECTOR ( 'NONE', #38689, 1000.000000000000000 ) ;
#23119=EDGE_CURVE ( 'NONE', #31070, #22317, #5106, .T. ) ;
#23137=PLANE ( 'NONE',  #48639 ) ;
#23153=DIRECTION ( 'NONE',  ( 1.836970198721029934E-16, 1.836970198721010706E-16, -1.000000000000000000 ) ) ;
#23157=CARTESIAN_POINT ( 'NONE',  ( 7.811466277050697293, 4.727349090213374794, 195.0000000000000284 ) ) ;
#23165=CARTESIAN_POINT ( 'NONE',  ( 10.09643294401454661, -9.106483450353492159, 455.0000000000000568 ) ) ;
#23175=DIRECTION ( 'NONE',  ( -2.135044278125299371E-15, 1.000000000000000000, 0.000000000000000000 ) ) ;
#23176=EDGE_CURVE ( 'NONE', #42678, #49724, #36572, .T. ) ;
#23180=DIRECTION ( 'NONE',  ( 0.000000000000000000, 1.000000000000000000, 0.000000000000000000 ) ) ;
#23181=ORIENTED_EDGE ( 'NONE', *, *, #42634, .F. ) ;
#23196=DIRECTION ( 'NONE',  ( 0.6414496315691420314, -0.7671651518153128624, 0.000000000000000000 ) ) ;
#23205=VECTOR ( 'NONE', #36329, 1000.000000000000114 ) ;
#23206=ORIENTED_EDGE ( 'NONE', *, *, #15059, .T. ) ;
#23208=VERTEX_POINT ( 'NONE', #42225 ) ;
#23216=ORIENTED_EDGE ( 'NONE', *, *, #56768, .F. ) ;
#23231=CARTESIAN_POINT ( 'NONE',  ( 9.247904806590725002, 9.942044687070426434, 455.0000000000000568 ) ) ;
#23232=CARTESIAN_POINT ( 'NONE',  ( 10.92648345035336099, 9.093516549646611935, 195.0000000000000284 ) ) ;
#23235=EDGE_CURVE ( 'NONE', #18501, #15780, #23408, .T. ) ;
#23239=ORIENTED_EDGE ( 'NONE', *, *, #67053, .T. ) ;
#23247=EDGE_CURVE ( 'NONE', #26502, #53142, #823, .T. ) ;
#23269=ORIENTED_EDGE ( 'NONE', *, *, #9099, .F. ) ;
#23274=CARTESIAN_POINT ( 'NONE',  ( 7.272650909786598561, -7.811466277050860718, 455.0000000000000568 ) ) ;
#23278=DIRECTION ( 'NONE',  ( -0.000000000000000000, -0.000000000000000000, -1.000000000000000000 ) ) ;
#23306=AXIS2_PLACEMENT_3D ( 'NONE', #38980, #55248, #11752 ) ;
#23316=VERTEX_POINT ( 'NONE', #49294 ) ;
#23323=DIRECTION ( 'NONE',  ( -0.6414496315691445849, 0.7671651518153106419, 2.818519042764040096E-16 ) ) ;
#23342=CARTESIAN_POINT ( 'NONE',  ( -11.77351654964670935, 4.393516549646602876, 455.0000000000000568 ) ) ;
#23352=CARTESIAN_POINT ( 'NONE',  ( -11.29351654964668583, 8.513516549646642062, 194.9999952000000292 ) ) ;
#23355=EDGE_CURVE ( 'NONE', #34313, #46798, #24138, .T. ) ;
#23358=ORIENTED_EDGE ( 'NONE', *, *, #16335, .T. ) ;
#23360=CARTESIAN_POINT ( 'NONE',  ( 7.811466277050736373, -7.272650909786728235, 455.0000000000000568 ) ) ;
#23373=PRODUCT_DEFINITION_SHAPE ( 'NONE', 'NONE',  #63345 ) ;
#23376=FACE_OUTER_BOUND ( 'NONE', #13572, .T. ) ;
#23387=ADVANCED_FACE ( 'NONE', ( #12810 ), #62307, .F. ) ;
#23388=CARTESIAN_POINT ( 'NONE',  ( -11.18071654964681372, -11.19368345035335821, 455.0000000000000568 ) ) ;
#23391=AXIS2_PLACEMENT_3D ( 'NONE', #20132, #57258, #63268 ) ;
#23392=ORIENTED_EDGE ( 'NONE', *, *, #56515, .F. ) ;
#23395=ADVANCED_FACE ( 'NONE', ( #51718 ), #14230, .F. ) ;
#23401=VECTOR ( 'NONE', #4229, 1000.000000000000000 ) ;
#23408=CIRCLE ( 'NONE', #45966, 0.1999999999999987899 ) ;
#23409=VECTOR ( 'NONE', #27415, 1000.000000000000000 ) ;
#23416=DIRECTION ( 'NONE',  ( 0.000000000000000000, 1.000000000000000000, 0.000000000000000000 ) ) ;
#23417=VECTOR ( 'NONE', #59737, 1000.000000000000000 ) ;
#23418=FACE_OUTER_BOUND ( 'NONE', #25752, .T. ) ;
#23423=ORIENTED_EDGE ( 'NONE', *, *, #42532, .T. ) ;
#23441=ORIENTED_EDGE ( 'NONE', *, *, #879, .F. ) ;
#23445=DIRECTION ( 'NONE',  ( 0.000000000000000000, 0.000000000000000000, 1.000000000000000000 ) ) ;
#23465=DIRECTION ( 'NONE',  ( 1.836970198721029934E-16, 1.836970198721010706E-16, -1.000000000000000000 ) ) ;
#23470=CARTESIAN_POINT ( 'NONE',  ( 4.740315990920191958, 4.188533722949208560, 455.0000000000000568 ) ) ;
#23471=DIRECTION ( 'NONE',  ( 1.000000000000000000, -1.088659024508174415E-14, 1.836970198721009966E-16 ) ) ;
#23478=EDGE_LOOP ( 'NONE', ( #36718, #56184, #65500, #52691 ) ) ;
#23488=ORIENTED_EDGE ( 'NONE', *, *, #16896, .T. ) ;
#23497=DIRECTION ( 'NONE',  ( 1.000000000000000000, 0.000000000000000000, 0.000000000000000000 ) ) ;
#23501=LINE ( 'NONE', #51066, #15655 ) ;
#23512=FACE_OUTER_BOUND ( 'NONE', #37057, .T. ) ;
#23515=ORIENTED_EDGE ( 'NONE', *, *, #28482, .T. ) ;
#23523=LINE ( 'NONE', #12550, #46542 ) ;
#23526=DIRECTION ( 'NONE',  ( -1.000000000000000000, 0.000000000000000000, 0.000000000000000000 ) ) ;
#23531=ORIENTED_EDGE ( 'NONE', *, *, #27274, .T. ) ;
#23541=ORIENTED_EDGE ( 'NONE', *, *, #26296, .F. ) ;
#23544=VECTOR ( 'NONE', #66584, 1000.000000000000000 ) ;
#23546=CARTESIAN_POINT ( 'NONE',  ( -5.993516549646711766, 5.993516549646603409, 195.0000000000000284 ) ) ;
#23548=ORIENTED_EDGE ( 'NONE', *, *, #5693, .T. ) ;
#23551=AXIS2_PLACEMENT_3D ( 'NONE', #45755, #51415, #19242 ) ;
#23552=LINE ( 'NONE', #12926, #27119 ) ;
#23559=EDGE_CURVE ( 'NONE', #28681, #31048, #37210, .T. ) ;
#23560=CIRCLE ( 'NONE', #20144, 0.3999999999999993006 ) ;
#23566=EDGE_LOOP ( 'NONE', ( #3482, #12691, #46249, #17575 ) ) ;
#23569=CARTESIAN_POINT ( 'NONE',  ( -7.259684009079963474, -4.201500623656036382, 455.0000000000000568 ) ) ;
#23570=EDGE_CURVE ( 'NONE', #44289, #58177, #53824, .T. ) ;
#23576=ORIENTED_EDGE ( 'NONE', *, *, #69592, .F. ) ;
#23582=ORIENTED_EDGE ( 'NONE', *, *, #38895, .T. ) ;
#23586=AXIS2_PLACEMENT_3D ( 'NONE', #38264, #54870, #48869 ) ;
#23589=DIRECTION ( 'NONE',  ( 1.836970198721029934E-16, 1.836970198721010706E-16, -1.000000000000000000 ) ) ;
#23595=DIRECTION ( 'NONE',  ( 0.000000000000000000, -1.000000000000000000, 0.000000000000000000 ) ) ;
#23600=DIRECTION ( 'NONE',  ( -0.6414496315691617934, -0.7671651518152962090, -2.818519042763987834E-16 ) ) ;
#23601=CARTESIAN_POINT ( 'NONE',  ( -11.77351654964679106, -7.606483450353366038, 455.0000000000000568 ) ) ;
#23615=ORIENTED_EDGE ( 'NONE', *, *, #9436, .T. ) ;
#23624=ORIENTED_EDGE ( 'NONE', *, *, #57962, .T. ) ;
#23630=VERTEX_POINT ( 'NONE', #15642 ) ;
#23636=AXIS2_PLACEMENT_3D ( 'NONE', #34830, #34469, #40128 ) ;
#23658=CARTESIAN_POINT ( 'NONE',  ( -7.252248008019455128, 6.606374702650072983, 455.0000000000000568 ) ) ;
#23665=EDGE_CURVE ( 'NONE', #8340, #6513, #37902, .T. ) ;
#23669=VERTEX_POINT ( 'NONE', #43190 ) ;
#23672=DIRECTION ( 'NONE',  ( 1.000000000000000000, -4.121462285523434458E-16, 0.000000000000000000 ) ) ;
#23675=AXIS2_PLACEMENT_3D ( 'NONE', #21404, #4799, #4460 ) ;
#23679=FACE_OUTER_BOUND ( 'NONE', #47822, .T. ) ;
#23687=CYLINDRICAL_SURFACE ( 'NONE', #27104, 1.399999999999999245 ) ;
#23697=ORIENTED_EDGE ( 'NONE', *, *, #18550, .T. ) ;
#23703=EDGE_CURVE ( 'NONE', #9194, #6389, #6069, .T. ) ;
#23706=ORIENTED_EDGE ( 'NONE', *, *, #16421, .T. ) ;
#23712=CARTESIAN_POINT ( 'NONE',  ( -11.31351654964674047, -4.206483450353332820, 455.0000000000000568 ) ) ;
#23714=CARTESIAN_POINT ( 'NONE',  ( -4.173516549646837603, -11.78648345035344214, 455.0000000000000568 ) ) ;
#23715=EDGE_CURVE ( 'NONE', #56475, #803, #26947, .T. ) ;
#23717=CARTESIAN_POINT ( 'NONE',  ( 3.606483450353369147, -7.428221114745003462, 195.0000000000000284 ) ) ;
#23719=VECTOR ( 'NONE', #12578, 1000.000000000000000 ) ;
#23723=CARTESIAN_POINT ( 'NONE',  ( -4.193516549646833624, -11.32648345035344128, 455.0000000000000568 ) ) ;
#23726=ORIENTED_EDGE ( 'NONE', *, *, #24528, .T. ) ;
#23727=VERTEX_POINT ( 'NONE', #32598 ) ;
#23732=LINE ( 'NONE', #67920, #55535 ) ;
#23736=VERTEX_POINT ( 'NONE', #44221 ) ;
#23737=ADVANCED_FACE ( 'NONE', ( #1439 ), #65801, .F. ) ;
#23742=CARTESIAN_POINT ( 'NONE',  ( -10.73351654964671020, 1.677516549646603794, 455.0000000000000568 ) ) ;
#23749=CARTESIAN_POINT ( 'NONE',  ( -7.793516549646712477, 11.31351654964660014, 195.0000000000000284 ) ) ;
#23751=DIRECTION ( 'NONE',  ( -0.000000000000000000, -0.000000000000000000, -1.000000000000000000 ) ) ;
#23765=DIRECTION ( 'NONE',  ( 0.8660254037844383745, 0.5000000000000005551, -0.000000000000000000 ) ) ;
#23768=CARTESIAN_POINT ( 'NONE',  ( -1.077516549646670541, 11.33351654964656596, 195.0000000000000284 ) ) ;
#23769=CARTESIAN_POINT ( 'NONE',  ( 9.106483450353419329, 11.11351654964656710, 455.0000000000000568 ) ) ;
#23771=LINE ( 'NONE', #1504, #49867 ) ;
#23785=EDGE_CURVE ( 'NONE', #5610, #40926, #2136, .T. ) ;
#23789=ORIENTED_EDGE ( 'NONE', *, *, #16510, .T. ) ;
#23790=DIRECTION ( 'NONE',  ( 0.7071067811865550112, 0.7071067811865401342, 2.597868168706466792E-16 ) ) ;
#23791=EDGE_CURVE ( 'NONE', #31344, #58112, #13788, .T. ) ;
#23795=ORIENTED_EDGE ( 'NONE', *, *, #52881, .F. ) ;
#23797=PLANE ( 'NONE',  #38519 ) ;
#23800=VECTOR ( 'NONE', #66097, 1000.000000000000000 ) ;
#23802=DIRECTION ( 'NONE',  ( 1.000000000000000000, -3.491481338843133355E-15, -1.836970198721036344E-16 ) ) ;
#23809=ORIENTED_EDGE ( 'NONE', *, *, #23785, .T. ) ;
#23815=LINE ( 'NONE', #45718, #51262 ) ;
#23816=VECTOR ( 'NONE', #7869, 1000.000000000000000 ) ;
#23817=CARTESIAN_POINT ( 'NONE',  ( 4.396432944014526889, -8.606483450353477949, 455.0000000000000568 ) ) ;
#23824=ORIENTED_EDGE ( 'NONE', *, *, #48662, .F. ) ;
#23831=VERTEX_POINT ( 'NONE', #7084 ) ;
#23837=PLANE ( 'NONE',  #63980 ) ;
#23842=CARTESIAN_POINT ( 'NONE',  ( 9.106483450353369591, 10.08346604330778362, 195.0000000000000284 ) ) ;
#23852=CARTESIAN_POINT ( 'NONE',  ( -2.693516549646675529, 10.91351654964657314, 195.0000000000000284 ) ) ;
#23864=CARTESIAN_POINT ( 'NONE',  ( -11.31351654964671027, 4.393516549646604652, 195.0000000000000284 ) ) ;
#23873=EDGE_CURVE ( 'NONE', #35140, #66944, #7435, .T. ) ;
#23888=CARTESIAN_POINT ( 'NONE',  ( -3.593516549646701197, 7.415254214038210279, 455.0000000000000568 ) ) ;
#23891=ORIENTED_EDGE ( 'NONE', *, *, #15726, .T. ) ;
#23907=ORIENTED_EDGE ( 'NONE', *, *, #8200, .T. ) ;
#23914=DIRECTION ( 'NONE',  ( 1.836970198721029934E-16, 1.836970198721010706E-16, -1.000000000000000000 ) ) ;
#23917=ORIENTED_EDGE ( 'NONE', *, *, #58646, .T. ) ;
#23921=CARTESIAN_POINT ( 'NONE',  ( -10.19191654964686578, -11.08848345035334759, 455.0000000000000568 ) ) ;
#23936=DIRECTION ( 'NONE',  ( 1.053224967557347660E-14, 1.000000000000000000, 0.000000000000000000 ) ) ;
#23939=CARTESIAN_POINT ( 'NONE',  ( 8.211283450353400681, 5.993516549646574099, 455.0000000000000568 ) ) ;
#23941=CARTESIAN_POINT ( 'NONE',  ( -8.452095193409402185, 4.242044687070461784, 455.0000000000000568 ) ) ;
#23948=ORIENTED_EDGE ( 'NONE', *, *, #4849, .F. ) ;
#23952=DIRECTION ( 'NONE',  ( -0.000000000000000000, 3.673940397442059868E-16, -1.000000000000000000 ) ) ;
#23955=VECTOR ( 'NONE', #31833, 1000.000000000000114 ) ;
#23956=VERTEX_POINT ( 'NONE', #21216 ) ;
#23958=CIRCLE ( 'NONE', #2661, 0.3999999999999993006 ) ;
#23967=DIRECTION ( 'NONE',  ( -0.000000000000000000, 3.673940397442059868E-16, -1.000000000000000000 ) ) ;
#23971=EDGE_LOOP ( 'NONE', ( #9933, #40645, #28083, #28089 ) ) ;
#23984=CIRCLE ( 'NONE', #36413, 1.399999999999999245 ) ;
#23987=LINE ( 'NONE', #55825, #51366 ) ;
#23989=LINE ( 'NONE', #56862, #32571 ) ;
#23998=EDGE_CURVE ( 'NONE', #15622, #30530, #42766, .T. ) ;
#24017=AXIS2_PLACEMENT_3D ( 'NONE', #62540, #41683, #9166 ) ;
#24025=CARTESIAN_POINT ( 'NONE',  ( -11.77351654964670935, 7.593516549646604830, 455.0000000000000568 ) ) ;
#24027=CARTESIAN_POINT ( 'NONE',  ( 11.78648345035337819, -4.186483450353396307, 195.0000000000000284 ) ) ;
#24029=CARTESIAN_POINT ( 'NONE',  ( 2.765062094116041980, -9.955011587777324422, 455.0000000000000568 ) ) ;
#24032=VERTEX_POINT ( 'NONE', #19787 ) ;
#24034=CARTESIAN_POINT ( 'NONE',  ( -4.173516549646839380, -12.00648345035344811, 455.0000000000000568 ) ) ;
#24038=DIRECTION ( 'NONE',  ( 0.000000000000000000, 0.000000000000000000, 1.000000000000000000 ) ) ;
#24039=ORIENTED_EDGE ( 'NONE', *, *, #1664, .T. ) ;
#24044=ORIENTED_EDGE ( 'NONE', *, *, #11056, .F. ) ;
#24045=AXIS2_PLACEMENT_3D ( 'NONE', #25047, #46250, #41294 ) ;
#24048=EDGE_CURVE ( 'NONE', #39173, #2080, #69290, .T. ) ;
#24051=LINE ( 'NONE', #51640, #55841 ) ;
#24064=VECTOR ( 'NONE', #50223, 1000.000000000000000 ) ;
#24080=VERTEX_POINT ( 'NONE', #32519 ) ;
#24089=LINE ( 'NONE', #56269, #46977 ) ;
#24093=CARTESIAN_POINT ( 'NONE',  ( -9.293516549646710700, 10.91351654964659801, 455.0000000000000568 ) ) ;
#24096=DIRECTION ( 'NONE',  ( -1.000000000000000000, -2.135044278125299371E-15, 0.000000000000000000 ) ) ;
#24102=EDGE_CURVE ( 'NONE', #47832, #65081, #27212, .T. ) ;
#24109=CIRCLE ( 'NONE', #11689, 1.399999999999998579 ) ;
#24110=AXIS2_PLACEMENT_3D ( 'NONE', #58957, #35013, #67564 ) ;
#24120=EDGE_CURVE ( 'NONE', #31671, #18501, #43452, .T. ) ;
#24122=LINE ( 'NONE', #3257, #40352 ) ;
#24123=EDGE_CURVE ( 'NONE', #56148, #20589, #49799, .T. ) ;
#24129=LINE ( 'NONE', #41702, #67290 ) ;
#24138=LINE ( 'NONE', #40027, #11003 ) ;
#24140=ORIENTED_EDGE ( 'NONE', *, *, #59288, .T. ) ;
#24146=ORIENTED_EDGE ( 'NONE', *, *, #48720, .T. ) ;
#24154=DIRECTION ( 'NONE',  ( 0.000000000000000000, 0.000000000000000000, 1.000000000000000000 ) ) ;
#24158=EDGE_CURVE ( 'NONE', #50749, #19531, #6327, .T. ) ;
#24159=ORIENTED_EDGE ( 'NONE', *, *, #28026, .T. ) ;
#24163=DIRECTION ( 'NONE',  ( 1.214636490590110272E-14, 1.000000000000000000, 1.836970198721032892E-16 ) ) ;
#24165=AXIS2_PLACEMENT_3D ( 'NONE', #18284, #6982, #29239 ) ;
#24166=AXIS2_PLACEMENT_3D ( 'NONE', #8240, #44669, #2248 ) ;
#24170=ORIENTED_EDGE ( 'NONE', *, *, #60529, .F. ) ;
#24181=VERTEX_POINT ( 'NONE', #55118 ) ;
#24184=DIRECTION ( 'NONE',  ( 1.000000000000000000, 0.000000000000000000, 0.000000000000000000 ) ) ;
#24195=DIRECTION ( 'NONE',  ( -0.000000000000000000, -0.000000000000000000, -1.000000000000000000 ) ) ;
#24199=CARTESIAN_POINT ( 'NONE',  ( 4.186483450353335023, -12.00648345035347830, 455.0000000000000568 ) ) ;
#24202=ORIENTED_EDGE ( 'NONE', *, *, #59726, .F. ) ;
#24205=EDGE_CURVE ( 'NONE', #24424, #46212, #40223, .T. ) ;
#24208=EDGE_CURVE ( 'NONE', #15685, #67578, #12641, .T. ) ;
#24222=CIRCLE ( 'NONE', #37764, 0.1999999999999987899 ) ;
#24230=DIRECTION ( 'NONE',  ( 1.836970198721029934E-16, 1.836970198721010706E-16, -1.000000000000000000 ) ) ;
#24242=CARTESIAN_POINT ( 'NONE',  ( -10.91351654964670637, 9.293516549646604119, 195.0000000000000284 ) ) ;
#24246=DIRECTION ( 'NONE',  ( 1.836970198721029934E-16, -1.836970198721036344E-16, 1.000000000000000000 ) ) ;
#24250=VECTOR ( 'NONE', #51276, 1000.000000000000000 ) ;
#24258=FACE_OUTER_BOUND ( 'NONE', #34203, .T. ) ;
#24263=AXIS2_PLACEMENT_3D ( 'NONE', #4660, #26221, #64745 ) ;
#24267=EDGE_CURVE ( 'NONE', #22188, #31070, #25796, .T. ) ;
#24271=ADVANCED_FACE ( 'NONE', ( #56488 ), #29967, .T. ) ;
#24280=CARTESIAN_POINT ( 'NONE',  ( -9.791916549646856538, -10.20488345035338718, 455.0000000000000568 ) ) ;
#24301=VECTOR ( 'NONE', #55621, 1000.000000000000114 ) ;
#24323=ORIENTED_EDGE ( 'NONE', *, *, #60602, .F. ) ;
#24326=ORIENTED_EDGE ( 'NONE', *, *, #25915, .T. ) ;
#24344=CARTESIAN_POINT ( 'NONE',  ( -4.609516549646713202, 3.593516549646603941, 195.0000000000000284 ) ) ;
#24346=EDGE_CURVE ( 'NONE', #4281, #12232, #47290, .T. ) ;
#24347=CYLINDRICAL_SURFACE ( 'NONE', #52918, 2.204799999999997429 ) ;
#24352=CARTESIAN_POINT ( 'NONE',  ( 9.841277389592647751, 1.677516549646587363, 195.0000000000000284 ) ) ;
#24354=ORIENTED_EDGE ( 'NONE', *, *, #9502, .F. ) ;
#24359=ADVANCED_FACE ( 'NONE', ( #25371 ), #52604, .F. ) ;
#24367=ORIENTED_EDGE ( 'NONE', *, *, #4287, .F. ) ;
#24372=VECTOR ( 'NONE', #35257, 1000.000000000000114 ) ;
#24373=VECTOR ( 'NONE', #65144, 1000.000000000000000 ) ;
#24381=FACE_OUTER_BOUND ( 'NONE', #51900, .T. ) ;
#24388=DIRECTION ( 'NONE',  ( -1.836970198721029934E-16, 1.836970198721036344E-16, -1.000000000000000000 ) ) ;
#24402=EDGE_LOOP ( 'NONE', ( #21403, #59579, #14669, #21327 ) ) ;
#24403=EDGE_CURVE ( 'NONE', #53423, #51193, #14523, .T. ) ;
#24407=VECTOR ( 'NONE', #47983, 1000.000000000000000 ) ;
#24409=CARTESIAN_POINT ( 'NONE',  ( 7.811466277050736373, -7.272650909786728235, 455.0000000000000568 ) ) ;
#24412=VERTEX_POINT ( 'NONE', #15118 ) ;
#24415=VERTEX_POINT ( 'NONE', #14050 ) ;
#24417=VECTOR ( 'NONE', #60876, 1000.000000000000000 ) ;
#24422=DIRECTION ( 'NONE',  ( 0.7071067811865510144, 0.7071067811865441310, -8.343721112914546325E-31 ) ) ;
#24423=DIRECTION ( 'NONE',  ( -1.836970198721029934E-16, 1.836970198721036344E-16, -1.000000000000000000 ) ) ;
#24424=VERTEX_POINT ( 'NONE', #68153 ) ;
#24433=VERTEX_POINT ( 'NONE', #36681 ) ;
#24434=ORIENTED_EDGE ( 'NONE', *, *, #15533, .F. ) ;
#24437=CYLINDRICAL_SURFACE ( 'NONE', #5099, 0.1999999999999987899 ) ;
#24444=ORIENTED_EDGE ( 'NONE', *, *, #55321, .T. ) ;
#24450=ADVANCED_FACE ( 'NONE', ( #3802 ), #9822, .F. ) ;
#24451=DIRECTION ( 'NONE',  ( 0.000000000000000000, 0.000000000000000000, 1.000000000000000000 ) ) ;
#24454=VECTOR ( 'NONE', #58043, 1000.000000000000000 ) ;
#24455=CARTESIAN_POINT ( 'NONE',  ( -9.093516549646711411, 10.91351654964659978, 195.0000000000000284 ) ) ;
#24466=AXIS2_PLACEMENT_3D ( 'NONE', #36, #21597, #43150 ) ;
#24469=ORIENTED_EDGE ( 'NONE', *, *, #38896, .F. ) ;
#24485=CARTESIAN_POINT ( 'NONE',  ( 10.74648345035337904, -1.690483450353395645, 195.0000000000000284 ) ) ;
#24486=ORIENTED_EDGE ( 'NONE', *, *, #25749, .T. ) ;
#24490=DIRECTION ( 'NONE',  ( 9.973078850062115052E-15, 1.000000000000000000, 1.836970198721028948E-16 ) ) ;
#24493=ORIENTED_EDGE ( 'NONE', *, *, #60050, .T. ) ;
#24496=LINE ( 'NONE', #66913, #51137 ) ;
#24497=DIRECTION ( 'NONE',  ( 1.000000000000000000, -1.671920889371702657E-15, 0.000000000000000000 ) ) ;
#24520=LINE ( 'NONE', #46078, #67226 ) ;
#24521=CARTESIAN_POINT ( 'NONE',  ( 8.406483450353379183, -7.616533956692325802, 455.0000000000000568 ) ) ;
#24528=EDGE_CURVE ( 'NONE', #41197, #59963, #26776, .T. ) ;
#24532=VECTOR ( 'NONE', #50151, 1000.000000000000000 ) ;
#24534=ORIENTED_EDGE ( 'NONE', *, *, #50212, .F. ) ;
#24541=VERTEX_POINT ( 'NONE', #21807 ) ;
#24543=DIRECTION ( 'NONE',  ( 0.000000000000000000, 0.000000000000000000, -1.000000000000000000 ) ) ;
#24545=EDGE_CURVE ( 'NONE', #56003, #69389, #6830, .T. ) ;
#24549=ORIENTED_EDGE ( 'NONE', *, *, #64059, .T. ) ;
#24552=DIRECTION ( 'NONE',  ( -9.050731179009442381E-15, -1.000000000000000000, 0.000000000000000000 ) ) ;
#24556=ADVANCED_FACE ( 'NONE', ( #5552 ), #17803, .F. ) ;
#24558=LINE ( 'NONE', #13939, #26640 ) ;
#24571=VECTOR ( 'NONE', #49201, 1000.000000000000000 ) ;
#24572=VECTOR ( 'NONE', #54908, 1000.000000000000000 ) ;
#24589=DIRECTION ( 'NONE',  ( 0.000000000000000000, 1.000000000000000000, 0.000000000000000000 ) ) ;
#24591=EDGE_CURVE ( 'NONE', #10643, #33426, #17447, .T. ) ;
#24594=DIRECTION ( 'NONE',  ( -0.000000000000000000, 3.673940397442059868E-16, -1.000000000000000000 ) ) ;
#24596=ORIENTED_EDGE ( 'NONE', *, *, #30793, .T. ) ;
#24599=EDGE_CURVE ( 'NONE', #4106, #29489, #15651, .T. ) ;
#24613=EDGE_CURVE ( 'NONE', #12341, #28734, #64258, .T. ) ;
#24614=CARTESIAN_POINT ( 'NONE',  ( -7.793516549646829716, -11.32648345035340576, 455.0000000000000568 ) ) ;
#24615=VERTEX_POINT ( 'NONE', #15809 ) ;
#24633=EDGE_CURVE ( 'NONE', #55193, #66404, #12229, .T. ) ;
#24635=ADVANCED_FACE ( 'NONE', ( #67638 ), #57019, .F. ) ;
#24636=AXIS2_PLACEMENT_3D ( 'NONE', #24907, #52130, #19596 ) ;
#24639=DIRECTION ( 'NONE',  ( 1.836970198721029934E-16, 1.836970198721010706E-16, -1.000000000000000000 ) ) ;
#24646=CARTESIAN_POINT ( 'NONE',  ( 11.78648345035337996, 4.393516549646516722, 455.0000000000000568 ) ) ;
#24653=CARTESIAN_POINT ( 'NONE',  ( -8.333516549646715177, 11.11351654964659907, 455.0000000000000568 ) ) ;
#24657=DIRECTION ( 'NONE',  ( -1.084202172485511060E-14, -1.000000000000000000, 0.000000000000000000 ) ) ;
#24658=EDGE_LOOP ( 'NONE', ( #19772, #20097, #34117, #33953 ) ) ;
#24659=DIRECTION ( 'NONE',  ( -1.000000000000000000, 1.349135440953254805E-14, -1.836970198721005529E-16 ) ) ;
#24661=CARTESIAN_POINT ( 'NONE',  ( -8.198316549646726514, -6.006483450353354847, 195.0000000000000284 ) ) ;
#24665=VECTOR ( 'NONE', #21120, 1000.000000000000114 ) ;
#24669=DIRECTION ( 'NONE',  ( -1.000000000000000000, 8.339399738404099512E-15, -1.836970198721014650E-16 ) ) ;
#24673=DIRECTION ( 'NONE',  ( 1.000000000000000000, -3.491481338843133355E-15, -1.836970198721036344E-16 ) ) ;
#24678=EDGE_LOOP ( 'NONE', ( #43104, #64403, #24783, #40917 ) ) ;
#24680=VERTEX_POINT ( 'NONE', #51367 ) ;
#24681=LINE ( 'NONE', #68518, #7992 ) ;
#24685=CARTESIAN_POINT ( 'NONE',  ( 4.747751991980655895, 6.606374702650043673, 455.0000000000000568 ) ) ;
#24686=CARTESIAN_POINT ( 'NONE',  ( 11.12648345035337627, -2.906483450353491094, 455.0000000000000568 ) ) ;
#24687=PLANE ( 'NONE',  #35519 ) ;
#24694=ORIENTED_EDGE ( 'NONE', *, *, #4372, .T. ) ;
#24698=LINE ( 'NONE', #2771, #17494 ) ;
#24707=AXIS2_PLACEMENT_3D ( 'NONE', #34488, #56079, #28494 ) ;
#24713=AXIS2_PLACEMENT_3D ( 'NONE', #65141, #54524, #11034 ) ;
#24722=DIRECTION ( 'NONE',  ( 1.000000000000000000, -3.491481338843133355E-15, -1.836970198721036344E-16 ) ) ;
#24728=CARTESIAN_POINT ( 'NONE',  ( 9.841277389592654856, 2.277516549646586785, 195.0000000000000284 ) ) ;
#24732=CARTESIAN_POINT ( 'NONE',  ( -9.791916549646810353, -10.20488345035334099, 195.0000000000000284 ) ) ;
#24742=PLANE ( 'NONE',  #8306 ) ;
#24747=CARTESIAN_POINT ( 'NONE',  ( 8.406483450353356091, 6.331612867284063917, 195.0000000000000284 ) ) ;
#24754=VERTEX_POINT ( 'NONE', #56326 ) ;
#24756=EDGE_CURVE ( 'NONE', #18487, #32701, #51021, .T. ) ;
#24759=LINE ( 'NONE', #50920, #9550 ) ;
#24763=VERTEX_POINT ( 'NONE', #16337 ) ;
#24767=ORIENTED_EDGE ( 'NONE', *, *, #674, .F. ) ;
#24768=AXIS2_PLACEMENT_3D ( 'NONE', #60761, #7009, #65393 ) ;
#24771=CARTESIAN_POINT ( 'NONE',  ( 6.006483450353379716, -6.006483450353490738, 455.0000000000000568 ) ) ;
#24774=CARTESIAN_POINT ( 'NONE',  ( 4.406483450353420928, 11.31351654964658593, 455.0000000000000568 ) ) ;
#24777=LINE ( 'NONE', #46332, #66162 ) ;
#24783=ORIENTED_EDGE ( 'NONE', *, *, #61774, .F. ) ;
#24801=LINE ( 'NONE', #57674, #28292 ) ;
#24807=CARTESIAN_POINT ( 'NONE',  ( -10.73351654964668533, -1.090483450353341155, 455.0000000000000568 ) ) ;
#24811=LINE ( 'NONE', #46368, #61763 ) ;
#24822=DIRECTION ( 'NONE',  ( -1.047444401652939849E-14, -1.000000000000000000, 0.000000000000000000 ) ) ;
#24825=CARTESIAN_POINT ( 'NONE',  ( -3.417780618358674971, -7.852485183456956896, 195.0000000000000284 ) ) ;
#24828=DIRECTION ( 'NONE',  ( -0.6414496315691367023, 0.7671651518153173033, 0.000000000000000000 ) ) ;
#24832=CIRCLE ( 'NONE', #53123, 0.6000000000000006439 ) ;
#24838=ORIENTED_EDGE ( 'NONE', *, *, #61774, .T. ) ;
#24841=CARTESIAN_POINT ( 'NONE',  ( -9.293516549646817282, -10.09643294401455904, 455.0000000000000568 ) ) ;
#24848=CARTESIAN_POINT ( 'NONE',  ( 11.48848345035337104, 10.19191654964660820, 195.0000000000000284 ) ) ;
#24853=EDGE_CURVE ( 'NONE', #17390, #11892, #6639, .T. ) ;
#24856=FACE_OUTER_BOUND ( 'NONE', #14469, .T. ) ;
#24857=EDGE_CURVE ( 'NONE', #59597, #9482, #9647, .T. ) ;
#24863=CYLINDRICAL_SURFACE ( 'NONE', #25396, 0.1999999999999987899 ) ;
#24864=LINE ( 'NONE', #63048, #47894 ) ;
#24867=DIRECTION ( 'NONE',  ( -1.836970198721029934E-16, -1.836970198721010706E-16, 1.000000000000000000 ) ) ;
#24871=EDGE_LOOP ( 'NONE', ( #54451, #35925, #20755, #64450 ) ) ;
#24872=CIRCLE ( 'NONE', #44096, 1.399999999999998579 ) ;
#24875=ORIENTED_EDGE ( 'NONE', *, *, #57857, .T. ) ;
#24884=ORIENTED_EDGE ( 'NONE', *, *, #55797, .F. ) ;
#24888=DIRECTION ( 'NONE',  ( -3.491481338843132961E-15, -1.000000000000000000, -1.836970198721029934E-16 ) ) ;
#24902=AXIS2_PLACEMENT_3D ( 'NONE', #10703, #59497, #11396 ) ;
#24907=CARTESIAN_POINT ( 'NONE',  ( -2.893516549646681035, 10.08346604330774632, 455.0000000000000568 ) ) ;
#24911=CIRCLE ( 'NONE', #67814, 0.1999999999999987899 ) ;
#24912=PLANE ( 'NONE',  #61559 ) ;
#24914=DIRECTION ( 'NONE',  ( -1.000000000000000000, 0.000000000000000000, 0.000000000000000000 ) ) ;
#24915=ORIENTED_EDGE ( 'NONE', *, *, #59107, .F. ) ;
#24917=DIRECTION ( 'NONE',  ( 1.836970198721029934E-16, 1.836970198721010706E-16, -1.000000000000000000 ) ) ;
#24931=EDGE_CURVE ( 'NONE', #36045, #37589, #4691, .T. ) ;
#24937=ADVANCED_FACE ( 'NONE', ( #22351 ), #60153, .F. ) ;
#24938=CIRCLE ( 'NONE', #33958, 0.5999999999999989786 ) ;
#24942=EDGE_CURVE ( 'NONE', #5476, #65266, #15700, .T. ) ;
#24945=CARTESIAN_POINT ( 'NONE',  ( -7.839518282750280065, -3.430747519065322049, 455.0000000000000568 ) ) ;
#24947=CARTESIAN_POINT ( 'NONE',  ( 6.006483450353401921, 5.993516549646582092, 455.0000000000000568 ) ) ;
#24953=EDGE_LOOP ( 'NONE', ( #19301, #47776, #65738, #7703 ) ) ;
#24959=ORIENTED_EDGE ( 'NONE', *, *, #56854, .F. ) ;
#24966=VECTOR ( 'NONE', #51316, 1000.000000000000000 ) ;
#24968=EDGE_CURVE ( 'NONE', #43669, #28734, #32947, .T. ) ;
#24971=ORIENTED_EDGE ( 'NONE', *, *, #69854, .F. ) ;
#24973=AXIS2_PLACEMENT_3D ( 'NONE', #12570, #44068, #43735 ) ;
#24974=EDGE_CURVE ( 'NONE', #62844, #63906, #17032, .T. ) ;
#24975=DIRECTION ( 'NONE',  ( 0.000000000000000000, 0.000000000000000000, 1.000000000000000000 ) ) ;
#24976=CYLINDRICAL_SURFACE ( 'NONE', #68395, 0.1999999999999987899 ) ;
#24978=EDGE_CURVE ( 'NONE', #60909, #24080, #11183, .T. ) ;
#24984=ORIENTED_EDGE ( 'NONE', *, *, #46564, .T. ) ;
#24985=DIRECTION ( 'NONE',  ( -0.000000000000000000, 3.673940397442059868E-16, -1.000000000000000000 ) ) ;
#24992=VERTEX_POINT ( 'NONE', #60502 ) ;
#24998=CARTESIAN_POINT ( 'NONE',  ( 10.09643294401454661, -2.906483450353491094, 455.0000000000000568 ) ) ;
#24999=ADVANCED_FACE ( 'NONE', ( #33294 ), #22681, .T. ) ;
#25001=EDGE_CURVE ( 'NONE', #35248, #16863, #49218, .T. ) ;
#25002=LINE ( 'NONE', #29946, #45381 ) ;
#25003=ORIENTED_EDGE ( 'NONE', *, *, #34899, .T. ) ;
#25018=CARTESIAN_POINT ( 'NONE',  ( 11.08848345035341865, 11.07551654964652776, 455.0000000000000568 ) ) ;
#25022=ADVANCED_FACE ( 'NONE', ( #8851 ), #18759, .F. ) ;
#25024=ORIENTED_EDGE ( 'NONE', *, *, #34479, .F. ) ;
#25032=ORIENTED_EDGE ( 'NONE', *, *, #36677, .F. ) ;
#25037=EDGE_CURVE ( 'NONE', #44153, #35248, #53002, .T. ) ;
#25041=ORIENTED_EDGE ( 'NONE', *, *, #1664, .F. ) ;
#25043=AXIS2_PLACEMENT_3D ( 'NONE', #2812, #24388, #36391 ) ;
#25045=DIRECTION ( 'NONE',  ( -1.261617073437657577E-14, -1.000000000000000000, 0.000000000000000000 ) ) ;
#25046=VERTEX_POINT ( 'NONE', #50928 ) ;
#25047=CARTESIAN_POINT ( 'NONE',  ( -1.853252480934882929, -9.417013320880883498, 455.0000000000000568 ) ) ;
#25048=VERTEX_POINT ( 'NONE', #56245 ) ;
#25056=VECTOR ( 'NONE', #29136, 1000.000000000000000 ) ;
#25064=CARTESIAN_POINT ( 'NONE',  ( -10.91351654964670814, 2.893516549646604208, 455.0000000000000568 ) ) ;
#25070=LINE ( 'NONE', #46982, #39851 ) ;
#25072=DIRECTION ( 'NONE',  ( 1.836970198721029934E-16, 1.836970198721010706E-16, -1.000000000000000000 ) ) ;
#25079=AXIS2_PLACEMENT_3D ( 'NONE', #11528, #17884, #50057 ) ;
#25084=ORIENTED_EDGE ( 'NONE', *, *, #55321, .F. ) ;
#25087=PLANE ( 'NONE',  #1821 ) ;
#25089=ORIENTED_EDGE ( 'NONE', *, *, #54335, .F. ) ;
#25094=CARTESIAN_POINT ( 'NONE',  ( -4.242044687070550602, 8.452095193409279617, 455.0000000000000568 ) ) ;
#25100=CARTESIAN_POINT ( 'NONE',  ( 10.92648345035337343, -2.706483450353490916, 455.0000000000000568 ) ) ;
#25111=EDGE_LOOP ( 'NONE', ( #13710, #12564, #67997, #68582 ) ) ;
#25118=EDGE_CURVE ( 'NONE', #3209, #11172, #30423, .T. ) ;
#25120=DIRECTION ( 'NONE',  ( 0.000000000000000000, 1.000000000000000000, 0.000000000000000000 ) ) ;
#25126=DIRECTION ( 'NONE',  ( -3.016910393003147986E-15, -1.000000000000000000, -3.673940397442060361E-16 ) ) ;
#25131=VERTEX_POINT ( 'NONE', #34306 ) ;
#25142=LINE ( 'NONE', #12460, #36443 ) ;
#25176=ADVANCED_FACE ( 'NONE', ( #36070 ), #9211, .F. ) ;
#25178=ORIENTED_EDGE ( 'NONE', *, *, #19011, .T. ) ;
#25186=DIRECTION ( 'NONE',  ( -1.836970198721029934E-16, -1.836970198721010706E-16, 1.000000000000000000 ) ) ;
#25197=ORIENTED_EDGE ( 'NONE', *, *, #60602, .T. ) ;
#25202=EDGE_CURVE ( 'NONE', #54282, #6582, #57641, .T. ) ;
#25205=CARTESIAN_POINT ( 'NONE',  ( 8.406483450353379183, -4.396432944014657451, 455.0000000000000568 ) ) ;
#25207=PLANE ( 'NONE',  #57934 ) ;
#25209=EDGE_CURVE ( 'NONE', #27223, #30559, #29281, .T. ) ;
#25214=ORIENTED_EDGE ( 'NONE', *, *, #22133, .F. ) ;
#25215=EDGE_CURVE ( 'NONE', #19912, #51662, #53746, .T. ) ;
#25217=ORIENTED_EDGE ( 'NONE', *, *, #6637, .F. ) ;
#25218=DIRECTION ( 'NONE',  ( -1.000000000000000000, 1.610765207321970913E-14, 1.836970198721059516E-16 ) ) ;
#25220=DIRECTION ( 'NONE',  ( 0.000000000000000000, 1.000000000000000000, 3.673940397442059868E-16 ) ) ;
#25222=DIRECTION ( 'NONE',  ( -1.053224967557348291E-14, -1.000000000000000000, 0.000000000000000000 ) ) ;
#25224=ORIENTED_EDGE ( 'NONE', *, *, #18526, .T. ) ;
#25226=CARTESIAN_POINT ( 'NONE',  ( -2.893516549646820035, -10.09643294401462654, 455.0000000000000568 ) ) ;
#25234=EDGE_LOOP ( 'NONE', ( #42331, #21212, #39306, #40328 ) ) ;
#25238=AXIS2_PLACEMENT_3D ( 'NONE', #62551, #55526, #56900 ) ;
#25244=AXIS2_PLACEMENT_3D ( 'NONE', #31119, #49103, #21883 ) ;
#25247=VECTOR ( 'NONE', #48889, 1000.000000000000000 ) ;
#25248=DIRECTION ( 'NONE',  ( 0.8660254037844435926, 0.4999999999999913958, 2.509347957447859069E-16 ) ) ;
#25261=LINE ( 'NONE', #46812, #67894 ) ;
#25262=CYLINDRICAL_SURFACE ( 'NONE', #24636, 0.1999999999999992339 ) ;
#25269=CYLINDRICAL_SURFACE ( 'NONE', #37743, 0.1999999999999987899 ) ;
#25278=DIRECTION ( 'NONE',  ( 1.836970198721029934E-16, 1.836970198721010706E-16, -1.000000000000000000 ) ) ;
#25293=CARTESIAN_POINT ( 'NONE',  ( -11.11351654964670743, 9.093516549646603053, 455.0000000000000568 ) ) ;
#25302=LINE ( 'NONE', #62771, #6892 ) ;
#25305=ORIENTED_EDGE ( 'NONE', *, *, #57567, .F. ) ;
#25312=ORIENTED_EDGE ( 'NONE', *, *, #3126, .T. ) ;
#25324=FACE_OUTER_BOUND ( 'NONE', #54967, .T. ) ;
#25328=VECTOR ( 'NONE', #12752, 1000.000000000000000 ) ;
#25331=EDGE_CURVE ( 'NONE', #30714, #64997, #43820, .T. ) ;
#25335=CYLINDRICAL_SURFACE ( 'NONE', #26509, 0.1999999999999987899 ) ;
#25336=CARTESIAN_POINT ( 'NONE',  ( -5.993516549646711766, 8.198316549646602169, 195.0000000000000284 ) ) ;
#25343=VECTOR ( 'NONE', #47734, 1000.000000000000000 ) ;
#25349=EDGE_CURVE ( 'NONE', #47230, #37838, #11231, .T. ) ;
#25351=DIRECTION ( 'NONE',  ( 1.000000000000000000, 0.000000000000000000, 0.000000000000000000 ) ) ;
#25352=DIRECTION ( 'NONE',  ( -1.000000000000000000, 0.000000000000000000, 0.000000000000000000 ) ) ;
#25358=DIRECTION ( 'NONE',  ( 1.836970198721029934E-16, 1.836970198721010706E-16, -1.000000000000000000 ) ) ;
#25371=FACE_OUTER_BOUND ( 'NONE', #50210, .T. ) ;
#25385=CARTESIAN_POINT ( 'NONE',  ( 7.265214908726107090, 6.606374702650081865, 195.0000000000000284 ) ) ;
#25389=LINE ( 'NONE', #47306, #62677 ) ;
#25392=ORIENTED_EDGE ( 'NONE', *, *, #50933, .F. ) ;
#25396=AXIS2_PLACEMENT_3D ( 'NONE', #30170, #51743, #18492 ) ;
#25407=VECTOR ( 'NONE', #25698, 999.9999999999998863 ) ;
#25417=EDGE_CURVE ( 'NONE', #58452, #17797, #38187, .T. ) ;
#25424=LINE ( 'NONE', #14105, #56704 ) ;
#25427=DIRECTION ( 'NONE',  ( 1.000000000000000000, -1.203165845134433242E-14, -1.836970198721052121E-16 ) ) ;
#25450=CARTESIAN_POINT ( 'NONE',  ( -8.393516549646712122, 7.603567055985436696, 455.0000000000000568 ) ) ;
#25451=LINE ( 'NONE', #53728, #60949 ) ;
#25463=CARTESIAN_POINT ( 'NONE',  ( -2.893516549646675706, 10.91351654964657669, 195.0000000000000284 ) ) ;
#25466=ORIENTED_EDGE ( 'NONE', *, *, #63931, .T. ) ;
#25476=EDGE_CURVE ( 'NONE', #51761, #30714, #48501, .T. ) ;
#25485=ORIENTED_EDGE ( 'NONE', *, *, #33037, .T. ) ;
#25493=VERTEX_POINT ( 'NONE', #45180 ) ;
#25503=EDGE_CURVE ( 'NONE', #39516, #61131, #18309, .T. ) ;
#25504=EDGE_CURVE ( 'NONE', #39228, #16506, #61436, .T. ) ;
#25505=ORIENTED_EDGE ( 'NONE', *, *, #56442, .T. ) ;
#25522=LINE ( 'NONE', #34711, #29419 ) ;
#25523=LINE ( 'NONE', #58746, #43917 ) ;
#25528=EDGE_CURVE ( 'NONE', #13479, #14815, #62147, .T. ) ;
#25529=ORIENTED_EDGE ( 'NONE', *, *, #39344, .F. ) ;
#25547=ORIENTED_EDGE ( 'NONE', *, *, #17279, .F. ) ;
#25571=CARTESIAN_POINT ( 'NONE',  ( -9.093516549646711411, 10.08346604330776941, 455.0000000000000568 ) ) ;
#25574=VERTEX_POINT ( 'NONE', #24685 ) ;
#25577=ORIENTED_EDGE ( 'NONE', *, *, #55043, .F. ) ;
#25580=EDGE_CURVE ( 'NONE', #62370, #14977, #60938, .T. ) ;
#25584=ORIENTED_EDGE ( 'NONE', *, *, #57970, .F. ) ;
#25590=CARTESIAN_POINT ( 'NONE',  ( 7.811466277050727491, 7.259684009079840905, 195.0000000000000284 ) ) ;
#25592=VERTEX_POINT ( 'NONE', #8398 ) ;
#25593=CIRCLE ( 'NONE', #34589, 0.2000000000000005107 ) ;
#25595=DIRECTION ( 'NONE',  ( -2.891205793294675467E-15, -1.000000000000000000, 0.000000000000000000 ) ) ;
#25603=CARTESIAN_POINT ( 'NONE',  ( 7.826483450353421745, 11.99351654964657499, 455.0000000000000568 ) ) ;
#25604=CARTESIAN_POINT ( 'NONE',  ( -7.393516549646776070, -6.006483450353426790, 455.0000000000000568 ) ) ;
#25605=ORIENTED_EDGE ( 'NONE', *, *, #6772, .F. ) ;
#25607=CIRCLE ( 'NONE', #13104, 0.5999999999999989786 ) ;
#25612=FACE_OUTER_BOUND ( 'NONE', #63061, .T. ) ;
#25618=DIRECTION ( 'NONE',  ( -1.000000000000000000, 1.883404846338789915E-14, 0.000000000000000000 ) ) ;
#25619=CARTESIAN_POINT ( 'NONE',  ( -7.393516549646710345, 5.993516549646603409, 195.0000000000000284 ) ) ;
#25621=EDGE_CURVE ( 'NONE', #12677, #40597, #69214, .T. ) ;
#25623=DIRECTION ( 'NONE',  ( -0.000000000000000000, 3.673940397442059868E-16, -1.000000000000000000 ) ) ;
#25645=ORIENTED_EDGE ( 'NONE', *, *, #30353, .T. ) ;
#25651=DIRECTION ( 'NONE',  ( -1.000000000000000000, 0.000000000000000000, 0.000000000000000000 ) ) ;
#25659=CARTESIAN_POINT ( 'NONE',  ( 9.955011587777235604, -9.247904806590801385, 455.0000000000000568 ) ) ;
#25660=ADVANCED_FACE ( 'NONE', ( #47646 ), #35987, .F. ) ;
#25666=DIRECTION ( 'NONE',  ( -0.000000000000000000, 3.673940397442059868E-16, -1.000000000000000000 ) ) ;
#25668=EDGE_CURVE ( 'NONE', #15146, #42524, #62861, .T. ) ;
#25669=DIRECTION ( 'NONE',  ( 0.7071067811865503483, 0.7071067811865446862, 0.000000000000000000 ) ) ;
#25670=CARTESIAN_POINT ( 'NONE',  ( -7.593516549646711411, 11.77351654964660277, 195.0000000000000284 ) ) ;
#25671=LINE ( 'NONE', #26701, #64172 ) ;
#25672=VECTOR ( 'NONE', #13411, 1000.000000000000000 ) ;
#25682=LINE ( 'NONE', #47237, #56435 ) ;
#25698=DIRECTION ( 'NONE',  ( -0.8660254037844363761, 0.5000000000000038858, -0.000000000000000000 ) ) ;
#25699=ORIENTED_EDGE ( 'NONE', *, *, #26353, .T. ) ;
#25700=ADVANCED_FACE ( 'NONE', ( #63208 ), #37054, .F. ) ;
#25702=DIRECTION ( 'NONE',  ( -0.000000000000000000, -0.000000000000000000, -1.000000000000000000 ) ) ;
#25704=VECTOR ( 'NONE', #46811, 1000.000000000000000 ) ;
#25711=CARTESIAN_POINT ( 'NONE',  ( -3.593516549646762481, -4.622483450353452206, 455.0000000000000568 ) ) ;
#25728=ORIENTED_EDGE ( 'NONE', *, *, #57008, .F. ) ;
#25737=LINE ( 'NONE', #52248, #23205 ) ;
#25741=EDGE_CURVE ( 'NONE', #19531, #49979, #41992, .T. ) ;
#25748=DIRECTION ( 'NONE',  ( -3.540573132209558464E-15, -1.000000000000000000, 0.000000000000000000 ) ) ;
#25749=EDGE_CURVE ( 'NONE', #55385, #56867, #14775, .T. ) ;
#25752=EDGE_LOOP ( 'NONE', ( #5506, #28444, #44895, #60572 ) ) ;
#25761=ORIENTED_EDGE ( 'NONE', *, *, #37355, .T. ) ;
#25769=ORIENTED_EDGE ( 'NONE', *, *, #52239, .T. ) ;
#25770=VECTOR ( 'NONE', #28799, 1000.000000000000000 ) ;
#25771=DIRECTION ( 'NONE',  ( -0.000000000000000000, 3.673940397442059868E-16, -1.000000000000000000 ) ) ;
#25779=LINE ( 'NONE', #12181, #12526 ) ;
#25786=CARTESIAN_POINT ( 'NONE',  ( 10.20488345035338185, -10.20488345035352928, 455.0000000000000568 ) ) ;
#25790=ADVANCED_FACE ( 'NONE', ( #966 ), #38771, .F. ) ;
#25793=CARTESIAN_POINT ( 'NONE',  ( -10.91351654964675610, -9.306483450353326248, 195.0000000000000284 ) ) ;
#25795=FACE_OUTER_BOUND ( 'NONE', #37446, .T. ) ;
#25796=CIRCLE ( 'NONE', #65314, 0.8128000000000145109 ) ;
#25824=ORIENTED_EDGE ( 'NONE', *, *, #10466, .F. ) ;
#25828=ORIENTED_EDGE ( 'NONE', *, *, #31938, .T. ) ;
#25830=LINE ( 'NONE', #48437, #3080 ) ;
#25833=EDGE_CURVE ( 'NONE', #14148, #45353, #21819, .T. ) ;
#25835=DIRECTION ( 'NONE',  ( 1.000000000000000000, 0.000000000000000000, 0.000000000000000000 ) ) ;
#25837=DIRECTION ( 'NONE',  ( 1.836970198721029934E-16, 1.836970198721010706E-16, -1.000000000000000000 ) ) ;
#25838=EDGE_LOOP ( 'NONE', ( #40599, #46482, #18148, #41735 ) ) ;
#25850=ORIENTED_EDGE ( 'NONE', *, *, #15726, .F. ) ;
#25855=ORIENTED_EDGE ( 'NONE', *, *, #5169, .F. ) ;
#25861=CARTESIAN_POINT ( 'NONE',  ( -8.593516549646745162, -7.616533956692185470, 195.0000000000000284 ) ) ;
#25862=EDGE_CURVE ( 'NONE', #68801, #61197, #65648, .T. ) ;
#25872=EDGE_CURVE ( 'NONE', #44963, #68597, #17200, .T. ) ;
#25880=DIRECTION ( 'NONE',  ( -0.000000000000000000, -0.000000000000000000, -1.000000000000000000 ) ) ;
#25882=CARTESIAN_POINT ( 'NONE',  ( 8.406483450353382736, 4.383466043307721272, 455.0000000000000568 ) ) ;
#25883=EDGE_CURVE ( 'NONE', #5458, #58797, #65977, .T. ) ;
#25886=CARTESIAN_POINT ( 'NONE',  ( -4.727349090213504468, -4.201500623656015065, 195.0000000000000284 ) ) ;
#25895=VERTEX_POINT ( 'NONE', #51468 ) ;
#25905=ADVANCED_FACE ( 'NONE', ( #8323 ), #12572, .T. ) ;
#25907=EDGE_CURVE ( 'NONE', #26074, #57794, #30468, .T. ) ;
#25914=EDGE_LOOP ( 'NONE', ( #58303, #10961, #49057, #32568 ) ) ;
#25915=EDGE_CURVE ( 'NONE', #41272, #30271, #68783, .T. ) ;
#25916=ORIENTED_EDGE ( 'NONE', *, *, #31297, .T. ) ;
#25926=CARTESIAN_POINT ( 'NONE',  ( 6.006483450353379716, -6.006483450353394815, 195.0000000000000284 ) ) ;
#25927=ORIENTED_EDGE ( 'NONE', *, *, #35319, .T. ) ;
#25932=CARTESIAN_POINT ( 'NONE',  ( -11.33351654964671162, 1.077516549646603483, 455.0000000000000568 ) ) ;
#25934=FACE_OUTER_BOUND ( 'NONE', #54346, .T. ) ;
#25935=VERTEX_POINT ( 'NONE', #34139 ) ;
#25946=DIRECTION ( 'NONE',  ( -0.000000000000000000, -0.000000000000000000, -1.000000000000000000 ) ) ;
#25949=ORIENTED_EDGE ( 'NONE', *, *, #37875, .T. ) ;
#25952=CARTESIAN_POINT ( 'NONE',  ( 11.19368345035336176, 11.99351654964661051, 195.0000000000000284 ) ) ;
#25953=DIRECTION ( 'NONE',  ( -1.836970198721029934E-16, 1.836970198721036344E-16, -1.000000000000000000 ) ) ;
#25954=CARTESIAN_POINT ( 'NONE',  ( -7.793516549646827940, -11.12648345035340647, 455.0000000000000568 ) ) ;
#25955=ORIENTED_EDGE ( 'NONE', *, *, #24978, .T. ) ;
#25969=ADVANCED_FACE ( 'NONE', ( #60683 ), #1982, .T. ) ;
#25970=DIRECTION ( 'NONE',  ( 1.000000000000000000, 0.000000000000000000, 0.000000000000000000 ) ) ;
#25989=EDGE_CURVE ( 'NONE', #39974, #49724, #9388, .T. ) ;
#26003=AXIS2_PLACEMENT_3D ( 'NONE', #36384, #57951, #9520 ) ;
#26006=VERTEX_POINT ( 'NONE', #31669 ) ;
#26016=ORIENTED_EDGE ( 'NONE', *, *, #25833, .T. ) ;
#26024=FACE_OUTER_BOUND ( 'NONE', #36840, .T. ) ;
#26025=UNCERTAINTY_MEASURE_WITH_UNIT (LENGTH_MEASURE( 1.000000000000000082E-05 ), #19999, 'distance_accuracy_value', 'NONE');
#26026=CARTESIAN_POINT ( 'NONE',  ( 7.806483450353379538, -11.12648345035348996, 455.0000000000000568 ) ) ;
#26027=ORIENTED_EDGE ( 'NONE', *, *, #11856, .T. ) ;
#26031=DIRECTION ( 'NONE',  ( 8.673617379884051249E-15, 1.000000000000000000, 0.000000000000000000 ) ) ;
#26032=EDGE_LOOP ( 'NONE', ( #56019, #23052, #35536, #41222 ) ) ;
#26042=CARTESIAN_POINT ( 'NONE',  ( 9.804883450353379715, -10.20488345035352928, 455.0000000000000568 ) ) ;
#26044=FACE_OUTER_BOUND ( 'NONE', #23971, .T. ) ;
#26046=CARTESIAN_POINT ( 'NONE',  ( 11.08848345035334404, -11.08848345035349148, 455.0000000000000568 ) ) ;
#26051=EDGE_CURVE ( 'NONE', #62970, #19180, #14350, .T. ) ;
#26057=DIRECTION ( 'NONE',  ( -0.6414496315691415873, 0.7671651518153131954, 2.309356642089130310E-17 ) ) ;
#26074=VERTEX_POINT ( 'NONE', #35910 ) ;
#26075=EDGE_LOOP ( 'NONE', ( #56769, #35867, #25305, #30717 ) ) ;
#26085=EDGE_LOOP ( 'NONE', ( #43318, #55822, #67373, #33578 ) ) ;
#26093=CARTESIAN_POINT ( 'NONE',  ( 6.006483450353401921, 5.993516549646582092, 455.0000000000000568 ) ) ;
#26104=ADVANCED_FACE ( 'NONE', ( #36252 ), #57818, .T. ) ;
#26125=CARTESIAN_POINT ( 'NONE',  ( 9.955011587777223170, 2.752095193409229701, 455.0000000000000568 ) ) ;
#26128=CARTESIAN_POINT ( 'NONE',  ( 1.866219381641485375, 9.404046420174006826, 455.0000000000000568 ) ) ;
#26134=DIRECTION ( 'NONE',  ( 1.836970198721029934E-16, 1.836970198721010706E-16, -1.000000000000000000 ) ) ;
#26142=CARTESIAN_POINT ( 'NONE',  ( 7.826483450353380000, -12.00648345035349251, 455.0000000000000568 ) ) ;
#26143=DIRECTION ( 'NONE',  ( -0.7671651518153006499, 0.6414496315691565753, 0.000000000000000000 ) ) ;
#26144=ORIENTED_EDGE ( 'NONE', *, *, #27982, .T. ) ;
#26151=DIRECTION ( 'NONE',  ( -1.836970198721029934E-16, 1.836970198721036344E-16, -1.000000000000000000 ) ) ;
#26162=VERTEX_POINT ( 'NONE', #69834 ) ;
#26168=AXIS2_PLACEMENT_3D ( 'NONE', #37276, #43949, #10052 ) ;
#26170=LINE ( 'NONE', #4947, #36680 ) ;
#26175=EDGE_LOOP ( 'NONE', ( #29797, #17537, #21247, #57734 ) ) ;
#26180=ORIENTED_EDGE ( 'NONE', *, *, #61992, .T. ) ;
#26181=EDGE_CURVE ( 'NONE', #6839, #59936, #53933, .T. ) ;
#26182=LINE ( 'NONE', #3562, #57177 ) ;
#26193=ORIENTED_EDGE ( 'NONE', *, *, #28125, .T. ) ;
#26221=DIRECTION ( 'NONE',  ( -1.836970198721029934E-16, -1.836970198721010706E-16, 1.000000000000000000 ) ) ;
#26224=EDGE_CURVE ( 'NONE', #44826, #14045, #26700, .T. ) ;
#26228=CARTESIAN_POINT ( 'NONE',  ( -7.252248008019462233, -5.393625297349887049, 195.0000000000000284 ) ) ;
#26229=LINE ( 'NONE', #64417, #13607 ) ;
#26231=ORIENTED_EDGE ( 'NONE', *, *, #60013, .T. ) ;
#26251=ORIENTED_EDGE ( 'NONE', *, *, #5654, .F. ) ;
#26263=PLANE ( 'NONE',  #58309 ) ;
#26293=LINE ( 'NONE', #68027, #54752 ) ;
#26294=ADVANCED_FACE ( 'NONE', ( #34765 ), #49646, .F. ) ;
#26296=EDGE_CURVE ( 'NONE', #13319, #68801, #7547, .T. ) ;
#26297=DIRECTION ( 'NONE',  ( -0.7671651518153106419, 0.6414496315691445849, 0.000000000000000000 ) ) ;
#26298=CARTESIAN_POINT ( 'NONE',  ( 3.430747519065294071, -7.852485183456927587, 195.0000000000000284 ) ) ;
#26301=ORIENTED_EDGE ( 'NONE', *, *, #61274, .F. ) ;
#26309=LINE ( 'NONE', #64162, #42708 ) ;
#26313=EDGE_CURVE ( 'NONE', #13060, #69389, #7184, .T. ) ;
#26316=CIRCLE ( 'NONE', #55679, 0.8128000000000145109 ) ;
#26321=DIRECTION ( 'NONE',  ( -0.7071067811865474617, -0.7071067811865474617, -2.597868168706479611E-16 ) ) ;
#26324=ORIENTED_EDGE ( 'NONE', *, *, #56242, .F. ) ;
#26325=DIRECTION ( 'NONE',  ( 0.7671651518152962090, -0.6414496315691619044, -2.356647714346269254E-16 ) ) ;
#26340=DIRECTION ( 'NONE',  ( 0.7071067811865474617, -0.7071067811865474617, 0.000000000000000000 ) ) ;
#26348=DIRECTION ( 'NONE',  ( -1.203165845134433242E-14, -1.000000000000000000, -1.836970198721014403E-16 ) ) ;
#26352=EDGE_LOOP ( 'NONE', ( #51379, #66670, #25041, #27841 ) ) ;
#26353=EDGE_CURVE ( 'NONE', #41078, #41134, #34399, .T. ) ;
#26356=ORIENTED_EDGE ( 'NONE', *, *, #4892, .T. ) ;
#26359=EDGE_CURVE ( 'NONE', #13319, #8498, #55996, .T. ) ;
#26384=DIRECTION ( 'NONE',  ( -0.000000000000000000, 3.673940397442059868E-16, -1.000000000000000000 ) ) ;
#26385=CARTESIAN_POINT ( 'NONE',  ( 9.955011587777271131, 9.234937905883876752, 455.0000000000000568 ) ) ;
#26386=ORIENTED_EDGE ( 'NONE', *, *, #12415, .T. ) ;
#26389=CARTESIAN_POINT ( 'NONE',  ( -10.19191654964685156, -9.804883450353383267, 455.0000000000000568 ) ) ;
#26392=ORIENTED_EDGE ( 'NONE', *, *, #50225, .T. ) ;
#26395=EDGE_CURVE ( 'NONE', #43734, #13690, #37200, .T. ) ;
#26406=ORIENTED_EDGE ( 'NONE', *, *, #5539, .F. ) ;
#26408=CARTESIAN_POINT ( 'NONE',  ( -7.793516549646712477, 11.11351654964660085, 195.0000000000000284 ) ) ;
#26415=CARTESIAN_POINT ( 'NONE',  ( 7.826483450353421745, 11.99351654964657499, 455.0000000000000568 ) ) ;
#26421=CARTESIAN_POINT ( 'NONE',  ( -3.593516549646714520, -4.622483450353405132, 195.0000000000000284 ) ) ;
#26424=ORIENTED_EDGE ( 'NONE', *, *, #31898, .F. ) ;
#26427=VERTEX_POINT ( 'NONE', #37893 ) ;
#26428=DIRECTION ( 'NONE',  ( -1.000000000000000000, 0.000000000000000000, 0.000000000000000000 ) ) ;
#26431=EDGE_CURVE ( 'NONE', #65042, #58346, #59102, .T. ) ;
#26433=CARTESIAN_POINT ( 'NONE',  ( -7.603567055985545942, 8.393516549646601987, 455.0000000000000568 ) ) ;
#26438=LINE ( 'NONE', #46590, #31274 ) ;
#26445=EDGE_CURVE ( 'NONE', #15780, #45972, #48498, .T. ) ;
#26451=CARTESIAN_POINT ( 'NONE',  ( -2.893516549646673930, 11.11351654964657598, 455.0000000000000568 ) ) ;
#26471=ORIENTED_EDGE ( 'NONE', *, *, #67229, .F. ) ;
#26472=ORIENTED_EDGE ( 'NONE', *, *, #12125, .F. ) ;
#26478=DIRECTION ( 'NONE',  ( 0.000000000000000000, -1.000000000000000000, 0.000000000000000000 ) ) ;
#26479=VERTEX_POINT ( 'NONE', #43526 ) ;
#26483=DIRECTION ( 'NONE',  ( 0.000000000000000000, 0.000000000000000000, 1.000000000000000000 ) ) ;
#26484=VERTEX_POINT ( 'NONE', #16679 ) ;
#26494=ORIENTED_EDGE ( 'NONE', *, *, #24403, .T. ) ;
#26499=CARTESIAN_POINT ( 'NONE',  ( -10.19191654964681781, -11.08848345035329963, 195.0000000000000284 ) ) ;
#26502=VERTEX_POINT ( 'NONE', #38582 ) ;
#26504=DIRECTION ( 'NONE',  ( -1.836970198721029934E-16, 1.836970198721036344E-16, -1.000000000000000000 ) ) ;
#26506=ORIENTED_EDGE ( 'NONE', *, *, #4674, .T. ) ;
#26509=AXIS2_PLACEMENT_3D ( 'NONE', #31702, #47601, #53272 ) ;
#26511=AXIS2_PLACEMENT_3D ( 'NONE', #26093, #10168, #69216 ) ;
#26529=VERTEX_POINT ( 'NONE', #60479 ) ;
#26533=EDGE_CURVE ( 'NONE', #32262, #65403, #35199, .T. ) ;
#26542=VECTOR ( 'NONE', #56316, 1000.000000000000000 ) ;
#26545=DIRECTION ( 'NONE',  ( 1.047444401652939849E-14, 1.000000000000000000, 0.000000000000000000 ) ) ;
#26553=DIRECTION ( 'NONE',  ( -0.000000000000000000, -0.000000000000000000, -1.000000000000000000 ) ) ;
#26560=DIRECTION ( 'NONE',  ( -1.000000000000000000, 0.000000000000000000, 0.000000000000000000 ) ) ;
#26561=PLANE ( 'NONE',  #44807 ) ;
#26579=DIRECTION ( 'NONE',  ( -0.000000000000000000, -0.000000000000000000, -1.000000000000000000 ) ) ;
#26587=ORIENTED_EDGE ( 'NONE', *, *, #62944, .T. ) ;
#26592=AXIS2_PLACEMENT_3D ( 'NONE', #48062, #32503, #53725 ) ;
#26597=VERTEX_POINT ( 'NONE', #55402 ) ;
#26604=DIRECTION ( 'NONE',  ( -1.000000000000000000, 0.000000000000000000, 0.000000000000000000 ) ) ;
#26607=AXIS2_PLACEMENT_3D ( 'NONE', #5826, #49311, #889 ) ;
#26612=ORIENTED_EDGE ( 'NONE', *, *, #59099, .T. ) ;
#26621=EDGE_CURVE ( 'NONE', #21581, #44389, #6945, .T. ) ;
#26622=ORIENTED_EDGE ( 'NONE', *, *, #7425, .T. ) ;
#26629=CARTESIAN_POINT ( 'NONE',  ( 4.747751991980663000, 5.380658396643107189, 455.0000000000000568 ) ) ;
#26630=ADVANCED_FACE ( 'NONE', ( #62076 ), #46173, .T. ) ;
#26633=ORIENTED_EDGE ( 'NONE', *, *, #25037, .F. ) ;
#26637=EDGE_CURVE ( 'NONE', #28943, #37001, #56780, .T. ) ;
#26638=EDGE_LOOP ( 'NONE', ( #7730, #8133, #33415, #35261 ) ) ;
#26639=CARTESIAN_POINT ( 'NONE',  ( -7.744988412222854279, 8.452095193409293827, 455.0000000000000568 ) ) ;
#26640=VECTOR ( 'NONE', #57072, 1000.000000000000000 ) ;
#26644=LINE ( 'NONE', #27345, #49127 ) ;
#26645=CARTESIAN_POINT ( 'NONE',  ( -8.393516549646712122, 4.383466043307770121, 455.0000000000000568 ) ) ;
#26652=LINE ( 'NONE', #20636, #30377 ) ;
#26664=DIRECTION ( 'NONE',  ( 1.000000000000000000, 2.135044278125301343E-15, -0.000000000000000000 ) ) ;
#26670=CARTESIAN_POINT ( 'NONE',  ( 4.740315990920172418, 7.798499376343941414, 455.0000000000000568 ) ) ;
#26678=DIRECTION ( 'NONE',  ( 0.6414496315691619044, 0.7671651518152962090, 0.000000000000000000 ) ) ;
#26682=DIRECTION ( 'NONE',  ( 1.836970198721029934E-16, -1.836970198721036344E-16, 1.000000000000000000 ) ) ;
#26687=CARTESIAN_POINT ( 'NONE',  ( 5.668387132715918320, -8.406483450353487541, 455.0000000000000568 ) ) ;
#26698=VERTEX_POINT ( 'NONE', #67409 ) ;
#26700=LINE ( 'NONE', #33393, #34835 ) ;
#26701=CARTESIAN_POINT ( 'NONE',  ( 11.08848345035337424, 11.47551654964657608, 195.0000000000000284 ) ) ;
#26708=CARTESIAN_POINT ( 'NONE',  ( -10.91351654964670637, 2.693516549646604030, 455.0000000000000568 ) ) ;
#26718=EDGE_CURVE ( 'NONE', #32701, #60888, #18646, .T. ) ;
#26722=DIRECTION ( 'NONE',  ( -1.000000000000000000, 1.047444401652940007E-14, -1.836970198721010952E-16 ) ) ;
#26727=ORIENTED_EDGE ( 'NONE', *, *, #15116, .T. ) ;
#26729=DIRECTION ( 'NONE',  ( 1.836970198721029934E-16, -1.836970198721036344E-16, 1.000000000000000000 ) ) ;
#26730=CARTESIAN_POINT ( 'NONE',  ( 11.08848345035337069, 10.19191654964660998, 195.0000000000000284 ) ) ;
#26732=CARTESIAN_POINT ( 'NONE',  ( -7.415254214038356828, -3.606483450353401121, 455.0000000000000568 ) ) ;
#26734=LINE ( 'NONE', #37346, #40353 ) ;
#26739=CIRCLE ( 'NONE', #36952, 0.1999999999999992339 ) ;
#26741=EDGE_CURVE ( 'NONE', #1362, #27098, #30969, .T. ) ;
#26746=LINE ( 'NONE', #69528, #57036 ) ;
#26752=CARTESIAN_POINT ( 'NONE',  ( -4.188533722949335569, 4.727349090213398775, 195.0000000000000284 ) ) ;
#26755=VECTOR ( 'NONE', #33590, 1000.000000000000000 ) ;
#26776=LINE ( 'NONE', #26421, #1009 ) ;
#26779=EDGE_CURVE ( 'NONE', #44522, #17797, #35552, .T. ) ;
#26781=EDGE_CURVE ( 'NONE', #16233, #40339, #57834, .T. ) ;
#26787=EDGE_LOOP ( 'NONE', ( #61420, #57383, #55648, #38249 ) ) ;
#26806=ADVANCED_FACE ( 'NONE', ( #4461 ), #3398, .F. ) ;
#26812=CARTESIAN_POINT ( 'NONE',  ( 8.465062094116099445, 7.744988412222715723, 455.0000000000000568 ) ) ;
#26815=EDGE_LOOP ( 'NONE', ( #57043, #65800, #61025, #21294 ) ) ;
#26820=ORIENTED_EDGE ( 'NONE', *, *, #59040, .T. ) ;
#26827=FACE_OUTER_BOUND ( 'NONE', #19682, .T. ) ;
#26829=ORIENTED_EDGE ( 'NONE', *, *, #64014, .F. ) ;
#26848=ORIENTED_EDGE ( 'NONE', *, *, #59136, .T. ) ;
#26854=DIRECTION ( 'NONE',  ( -0.000000000000000000, -0.000000000000000000, -1.000000000000000000 ) ) ;
#26858=EDGE_CURVE ( 'NONE', #50893, #6839, #31097, .T. ) ;
#26865=CARTESIAN_POINT ( 'NONE',  ( -7.259684009079930611, 4.188533722949235205, 455.0000000000000568 ) ) ;
#26879=CIRCLE ( 'NONE', #17824, 0.1999999999999987899 ) ;
#26886=CARTESIAN_POINT ( 'NONE',  ( 4.406483450353420928, 11.77351654964658501, 455.0000000000000568 ) ) ;
#26897=VERTEX_POINT ( 'NONE', #21756 ) ;
#26898=EDGE_CURVE ( 'NONE', #7775, #40339, #9644, .T. ) ;
#26901=VERTEX_POINT ( 'NONE', #27410 ) ;
#26906=VERTEX_POINT ( 'NONE', #49337 ) ;
#26908=CARTESIAN_POINT ( 'NONE',  ( 7.811466277050736373, -4.740315990920255906, 455.0000000000000568 ) ) ;
#26914=DIRECTION ( 'NONE',  ( 0.000000000000000000, -3.673940397442059868E-16, 1.000000000000000000 ) ) ;
#26915=AXIS2_PLACEMENT_3D ( 'NONE', #49492, #1058, #1727 ) ;
#26917=CYLINDRICAL_SURFACE ( 'NONE', #69684, 2.204799999999997429 ) ;
#26922=PLANE ( 'NONE',  #69948 ) ;
#26933=FACE_OUTER_BOUND ( 'NONE', #54554, .T. ) ;
#26934=EDGE_CURVE ( 'NONE', #37901, #22868, #65254, .T. ) ;
#26943=ORIENTED_EDGE ( 'NONE', *, *, #23873, .T. ) ;
#26947=LINE ( 'NONE', #17710, #17800 ) ;
#26953=DIRECTION ( 'NONE',  ( 0.000000000000000000, 0.000000000000000000, -1.000000000000000000 ) ) ;
#26958=DIRECTION ( 'NONE',  ( -1.678252938371784572E-14, -1.000000000000000000, -1.836970198721041520E-16 ) ) ;
#26963=DIRECTION ( 'NONE',  ( 1.000000000000000000, 0.000000000000000000, 0.000000000000000000 ) ) ;
#26967=ORIENTED_EDGE ( 'NONE', *, *, #67796, .F. ) ;
#26973=AXIS2_PLACEMENT_3D ( 'NONE', #54220, #64145, #10722 ) ;
#26974=EDGE_CURVE ( 'NONE', #28387, #32424, #48287, .T. ) ;
#26987=LINE ( 'NONE', #53176, #50856 ) ;
#26994=CARTESIAN_POINT ( 'NONE',  ( 4.255011587777218551, -8.465062094116168723, 455.0000000000000568 ) ) ;
#27000=VERTEX_POINT ( 'NONE', #28776 ) ;
#27005=DIRECTION ( 'NONE',  ( 8.673617379884013384E-15, 1.000000000000000000, 0.000000000000000000 ) ) ;
#27011=AXIS2_PLACEMENT_3D ( 'NONE', #29005, #66139, #1106 ) ;
#27018=ORIENTED_EDGE ( 'NONE', *, *, #56455, .F. ) ;
#27023=VECTOR ( 'NONE', #59437, 1000.000000000000114 ) ;
#27026=FACE_OUTER_BOUND ( 'NONE', #40486, .T. ) ;
#27034=LINE ( 'NONE', #882, #20325 ) ;
#27039=CARTESIAN_POINT ( 'NONE',  ( -11.07551654964667520, 10.19191654964664018, 195.0000000000000284 ) ) ;
#27042=ORIENTED_EDGE ( 'NONE', *, *, #48703, .T. ) ;
#27051=CIRCLE ( 'NONE', #16903, 0.1999999999999996503 ) ;
#27052=CARTESIAN_POINT ( 'NONE',  ( -10.08346604330787777, 2.893516549646604208, 195.0000000000000284 ) ) ;
#27055=EDGE_CURVE ( 'NONE', #3474, #56963, #56354, .T. ) ;
#27057=CIRCLE ( 'NONE', #53015, 0.3999999999999993006 ) ;
#27066=ORIENTED_EDGE ( 'NONE', *, *, #4847, .T. ) ;
#27071=DIRECTION ( 'NONE',  ( -1.000000000000000000, 3.491481338843132961E-15, 0.000000000000000000 ) ) ;
#27076=AXIS2_PLACEMENT_3D ( 'NONE', #3573, #62601, #2167 ) ;
#27078=DIRECTION ( 'NONE',  ( -0.000000000000000000, 3.673940397442059868E-16, -1.000000000000000000 ) ) ;
#27084=VECTOR ( 'NONE', #10761, 1000.000000000000000 ) ;
#27093=EDGE_CURVE ( 'NONE', #30530, #67203, #17479, .T. ) ;
#27095=AXIS2_PLACEMENT_3D ( 'NONE', #43422, #55434, #33514 ) ;
#27098=VERTEX_POINT ( 'NONE', #39049 ) ;
#27101=ADVANCED_FACE ( 'NONE', ( #66954 ), #61650, .F. ) ;
#27104=AXIS2_PLACEMENT_3D ( 'NONE', #11356, #29000, #6406 ) ;
#27105=DIRECTION ( 'NONE',  ( 1.836970198721029934E-16, 1.836970198721010706E-16, -1.000000000000000000 ) ) ;
#27108=LINE ( 'NONE', #44049, #2310 ) ;
#27117=CARTESIAN_POINT ( 'NONE',  ( -5.993516549646711766, 5.993516549646603409, 455.0000000000000568 ) ) ;
#27118=AXIS2_PLACEMENT_3D ( 'NONE', #35853, #9692, #19240 ) ;
#27119=VECTOR ( 'NONE', #56085, 1000.000000000000000 ) ;
#27123=ORIENTED_EDGE ( 'NONE', *, *, #14926, .F. ) ;
#27129=LINE ( 'NONE', #68523, #52824 ) ;
#27141=VERTEX_POINT ( 'NONE', #19226 ) ;
#27144=PLANE ( 'NONE',  #49930 ) ;
#27148=DIRECTION ( 'NONE',  ( 1.836970198721029934E-16, 1.836970198721010706E-16, -1.000000000000000000 ) ) ;
#27149=ORIENTED_EDGE ( 'NONE', *, *, #34777, .F. ) ;
#27158=VECTOR ( 'NONE', #21679, 1000.000000000000000 ) ;
#27164=DIRECTION ( 'NONE',  ( -1.836970198721029934E-16, 1.836970198721036344E-16, -1.000000000000000000 ) ) ;
#27167=ADVANCED_FACE ( 'NONE', ( #2963 ), #30538, .F. ) ;
#27174=EDGE_CURVE ( 'NONE', #4952, #19035, #59405, .T. ) ;
#27178=ORIENTED_EDGE ( 'NONE', *, *, #38805, .T. ) ;
#27180=DIRECTION ( 'NONE',  ( -1.000000000000000000, -5.013651664672856055E-16, 0.000000000000000000 ) ) ;
#27200=LINE ( 'NONE', #27885, #4553 ) ;
#27203=DIRECTION ( 'NONE',  ( 8.673617379884051249E-15, 1.000000000000000000, 0.000000000000000000 ) ) ;
#27208=ORIENTED_EDGE ( 'NONE', *, *, #50949, .F. ) ;
#27209=CARTESIAN_POINT ( 'NONE',  ( -3.593516549646701197, 7.415254214038210279, 455.0000000000000568 ) ) ;
#27212=LINE ( 'NONE', #38175, #9951 ) ;
#27217=DIRECTION ( 'NONE',  ( 0.7671651518152939886, -0.6414496315691645689, 2.309356642088621864E-17 ) ) ;
#27223=VERTEX_POINT ( 'NONE', #47161 ) ;
#27229=CIRCLE ( 'NONE', #58827, 0.3999999999999993006 ) ;
#27236=ORIENTED_EDGE ( 'NONE', *, *, #46229, .F. ) ;
#27237=ADVANCED_FACE ( 'NONE', ( #14982 ), #58110, .F. ) ;
#27241=ORIENTED_EDGE ( 'NONE', *, *, #9099, .T. ) ;
#27244=EDGE_CURVE ( 'NONE', #66711, #2958, #31599, .T. ) ;
#27246=ORIENTED_EDGE ( 'NONE', *, *, #23791, .T. ) ;
#27253=CIRCLE ( 'NONE', #67871, 0.1999999999999987899 ) ;
#27255=DIRECTION ( 'NONE',  ( 6.508391731846280553E-15, 1.000000000000000000, 0.000000000000000000 ) ) ;
#27263=CARTESIAN_POINT ( 'NONE',  ( 9.955011587777223170, 2.752095193409229701, 455.0000000000000568 ) ) ;
#27266=VECTOR ( 'NONE', #46059, 1000.000000000000000 ) ;
#27274=EDGE_CURVE ( 'NONE', #37049, #24763, #20991, .T. ) ;
#27276=ORIENTED_EDGE ( 'NONE', *, *, #65008, .F. ) ;
#27278=ORIENTED_EDGE ( 'NONE', *, *, #1222, .F. ) ;
#27282=ORIENTED_EDGE ( 'NONE', *, *, #4654, .T. ) ;
#27285=ORIENTED_EDGE ( 'NONE', *, *, #53465, .T. ) ;
#27287=DIRECTION ( 'NONE',  ( 1.000000000000000000, 0.000000000000000000, 0.000000000000000000 ) ) ;
#27294=VERTEX_POINT ( 'NONE', #42888 ) ;
#27297=CARTESIAN_POINT ( 'NONE',  ( -11.31351654964671027, 4.393516549646604652, 455.0000000000000568 ) ) ;
#27299=ORIENTED_EDGE ( 'NONE', *, *, #43925, .T. ) ;
#27303=ORIENTED_EDGE ( 'NONE', *, *, #54718, .T. ) ;
#27308=CARTESIAN_POINT ( 'NONE',  ( 9.955011587777235604, -9.247904806590801385, 455.0000000000000568 ) ) ;
#27309=DIRECTION ( 'NONE',  ( 0.000000000000000000, -0.000000000000000000, -1.000000000000000000 ) ) ;
#27316=AXIS2_PLACEMENT_3D ( 'NONE', #28317, #56237, #7438 ) ;
#27321=CARTESIAN_POINT ( 'NONE',  ( -5.655420232009250370, 8.393516549646600211, 195.0000000000000284 ) ) ;
#27325=EDGE_CURVE ( 'NONE', #13233, #33822, #35655, .T. ) ;
#27330=LINE ( 'NONE', #49245, #58244 ) ;
#27334=PLANE ( 'NONE',  #2312 ) ;
#27345=CARTESIAN_POINT ( 'NONE',  ( 5.668387132715918320, -8.406483450353487541, 455.0000000000000568 ) ) ;
#27346=DIRECTION ( 'NONE',  ( -1.156482317317873342E-14, -1.000000000000000000, 0.000000000000000000 ) ) ;
#27347=CARTESIAN_POINT ( 'NONE',  ( 7.272650909786598561, -4.201500623656122535, 455.0000000000000568 ) ) ;
#27350=DIRECTION ( 'NONE',  ( -1.053224967557348291E-14, -1.000000000000000000, 0.000000000000000000 ) ) ;
#27355=CARTESIAN_POINT ( 'NONE',  ( 9.955011587777223170, 9.234937905883922937, 195.0000000000000284 ) ) ;
#27362=LINE ( 'NONE', #488, #4291 ) ;
#27366=ORIENTED_EDGE ( 'NONE', *, *, #65097, .F. ) ;
#27379=DIRECTION ( 'NONE',  ( -0.000000000000000000, 3.673940397442059868E-16, -1.000000000000000000 ) ) ;
#27387=PLANE ( 'NONE',  #53718 ) ;
#27388=DIRECTION ( 'NONE',  ( 1.836970198721029934E-16, 1.836970198721010706E-16, -1.000000000000000000 ) ) ;
#27389=CIRCLE ( 'NONE', #45430, 0.1999999999999987899 ) ;
#27394=DIRECTION ( 'NONE',  ( 0.8660254037844401509, 0.4999999999999973910, 0.000000000000000000 ) ) ;
#27396=( NAMED_UNIT ( * ) SI_UNIT ( $, .STERADIAN. ) SOLID_ANGLE_UNIT ( ) );
#27402=ORIENTED_EDGE ( 'NONE', *, *, #17279, .T. ) ;
#27403=ORIENTED_EDGE ( 'NONE', *, *, #5486, .T. ) ;
#27405=VERTEX_POINT ( 'NONE', #44262 ) ;
#27408=ADVANCED_FACE ( 'NONE', ( #34694 ), #7122, .F. ) ;
#27410=CARTESIAN_POINT ( 'NONE',  ( 5.393625297349901260, -4.747751991980754482, 455.0000000000000568 ) ) ;
#27414=EDGE_CURVE ( 'NONE', #27500, #33822, #24089, .T. ) ;
#27415=DIRECTION ( 'NONE',  ( -1.000000000000000000, 3.903627567395476653E-15, 1.836970198721037083E-16 ) ) ;
#27417=VECTOR ( 'NONE', #65947, 1000.000000000000000 ) ;
#27433=DIRECTION ( 'NONE',  ( -1.000000000000000000, 0.000000000000000000, 0.000000000000000000 ) ) ;
#27435=CIRCLE ( 'NONE', #235, 0.2000000000000000944 ) ;
#27448=DIRECTION ( 'NONE',  ( 1.000000000000000000, 2.135044278125301343E-15, -0.000000000000000000 ) ) ;
#27451=EDGE_CURVE ( 'NONE', #42528, #12808, #24911, .T. ) ;
#27458=FACE_OUTER_BOUND ( 'NONE', #12568, .T. ) ;
#27464=DIRECTION ( 'NONE',  ( 1.671920889371702657E-15, -1.000000000000000000, 0.000000000000000000 ) ) ;
#27473=CARTESIAN_POINT ( 'NONE',  ( -9.234937905884079257, -9.955011587777201854, 195.0000000000000284 ) ) ;
#27477=DIRECTION ( 'NONE',  ( 1.836970198721029934E-16, -1.836970198721036344E-16, 1.000000000000000000 ) ) ;
#27478=ORIENTED_EDGE ( 'NONE', *, *, #58241, .T. ) ;
#27489=EDGE_CURVE ( 'NONE', #67902, #31344, #44962, .T. ) ;
#27500=VERTEX_POINT ( 'NONE', #51310 ) ;
#27503=AXIS2_PLACEMENT_3D ( 'NONE', #45449, #24246, #12918 ) ;
#27511=CARTESIAN_POINT ( 'NONE',  ( -11.31351654964674047, -4.206483450353332820, 455.0000000000000568 ) ) ;
#27515=VECTOR ( 'NONE', #23022, 1000.000000000000000 ) ;
#27519=FACE_OUTER_BOUND ( 'NONE', #2598, .T. ) ;
#27523=DIRECTION ( 'NONE',  ( 1.047444401652940007E-14, 1.000000000000000000, 1.836970198721029934E-16 ) ) ;
#27527=ORIENTED_EDGE ( 'NONE', *, *, #21505, .F. ) ;
#27531=CARTESIAN_POINT ( 'NONE',  ( 7.606483450353380249, -11.32648345035348925, 455.0000000000000568 ) ) ;
#27537=EDGE_LOOP ( 'NONE', ( #452, #25024, #29973, #9342 ) ) ;
#27549=DIRECTION ( 'NONE',  ( -0.000000000000000000, 3.673940397442059868E-16, -1.000000000000000000 ) ) ;
#27553=FACE_OUTER_BOUND ( 'NONE', #21938, .T. ) ;
#27577=CARTESIAN_POINT ( 'NONE',  ( 2.765062094116107705, 9.942044687070449527, 455.0000000000000568 ) ) ;
#27587=PLANE ( 'NONE',  #59939 ) ;
#27589=ORIENTED_EDGE ( 'NONE', *, *, #52193, .F. ) ;
#27592=DIRECTION ( 'NONE',  ( -0.000000000000000000, -0.000000000000000000, -1.000000000000000000 ) ) ;
#27611=VECTOR ( 'NONE', #48920, 1000.000000000000114 ) ;
#27624=VERTEX_POINT ( 'NONE', #36095 ) ;
#27628=DIRECTION ( 'NONE',  ( -2.135044278125299371E-15, -1.000000000000000000, -3.673940397442060361E-16 ) ) ;
#27633=LINE ( 'NONE', #38596, #67927 ) ;
#27635=EDGE_LOOP ( 'NONE', ( #65390, #63594, #61958, #69021 ) ) ;
#27642=EDGE_CURVE ( 'NONE', #9826, #13193, #31862, .T. ) ;
#27647=DIRECTION ( 'NONE',  ( 0.7671651518153131954, 0.6414496315691415873, 2.587583378555109562E-16 ) ) ;
#27651=VECTOR ( 'NONE', #68504, 1000.000000000000227 ) ;
#27658=EDGE_CURVE ( 'NONE', #1406, #191, #16279, .T. ) ;
#27675=AXIS2_PLACEMENT_3D ( 'NONE', #53625, #37361, #38064 ) ;
#27678=CARTESIAN_POINT ( 'NONE',  ( -4.393516549646832914, -11.32648345035344128, 455.0000000000000568 ) ) ;
#27680=VECTOR ( 'NONE', #37347, 1000.000000000000114 ) ;
#27684=DIRECTION ( 'NONE',  ( 0.7671651518153006499, 0.6414496315691565753, 0.000000000000000000 ) ) ;
#27686=DIRECTION ( 'NONE',  ( -1.000000000000000000, 0.000000000000000000, 0.000000000000000000 ) ) ;
#27687=ORIENTED_EDGE ( 'NONE', *, *, #18257, .F. ) ;
#27693=DIRECTION ( 'NONE',  ( -0.000000000000000000, 3.673940397442059868E-16, -1.000000000000000000 ) ) ;
#27694=DIRECTION ( 'NONE',  ( 1.000000000000000000, 0.000000000000000000, 0.000000000000000000 ) ) ;
#27695=CARTESIAN_POINT ( 'NONE',  ( 2.706483450353419862, 10.91351654964658735, 455.0000000000000568 ) ) ;
#27698=VERTEX_POINT ( 'NONE', #31516 ) ;
#27704=VECTOR ( 'NONE', #52827, 1000.000000000000000 ) ;
#27705=VERTEX_POINT ( 'NONE', #15606 ) ;
#27706=DIRECTION ( 'NONE',  ( 1.053224967557347660E-14, 1.000000000000000000, 0.000000000000000000 ) ) ;
#27713=AXIS2_PLACEMENT_3D ( 'NONE', #29454, #55986, #61622 ) ;
#27716=ADVANCED_FACE ( 'NONE', ( #10624 ), #58730, .F. ) ;
#27721=CARTESIAN_POINT ( 'NONE',  ( -1.853252480934758584, 9.404046420173985510, 455.0000000000000568 ) ) ;
#27722=ORIENTED_EDGE ( 'NONE', *, *, #4654, .F. ) ;
#27731=FACE_OUTER_BOUND ( 'NONE', #48971, .T. ) ;
#27736=ORIENTED_EDGE ( 'NONE', *, *, #43282, .F. ) ;
#27747=ORIENTED_EDGE ( 'NONE', *, *, #51590, .F. ) ;
#27761=ADVANCED_FACE ( 'NONE', ( #11651 ), #22966, .F. ) ;
#27766=DIRECTION ( 'NONE',  ( 1.349135440953254805E-14, 1.000000000000000000, 1.836970198721035604E-16 ) ) ;
#27776=DIRECTION ( 'NONE',  ( -0.8660254037844358210, 0.5000000000000049960, 2.509347957447882735E-16 ) ) ;
#27786=LINE ( 'NONE', #28132, #38373 ) ;
#27788=CARTESIAN_POINT ( 'NONE',  ( -7.793516549646712477, 11.11351654964660085, 195.0000000000000284 ) ) ;
#27809=LINE ( 'NONE', #65302, #66549 ) ;
#27815=LINE ( 'NONE', #6919, #12628 ) ;
#27821=LINE ( 'NONE', #1619, #61086 ) ;
#27827=ORIENTED_EDGE ( 'NONE', *, *, #445, .T. ) ;
#27828=ORIENTED_EDGE ( 'NONE', *, *, #9919, .F. ) ;
#27831=ORIENTED_EDGE ( 'NONE', *, *, #39946, .T. ) ;
#27836=EDGE_LOOP ( 'NONE', ( #36235, #66653, #35855, #45018 ) ) ;
#27839=VERTEX_POINT ( 'NONE', #28269 ) ;
#27841=ORIENTED_EDGE ( 'NONE', *, *, #34777, .T. ) ;
#27844=VECTOR ( 'NONE', #9373, 1000.000000000000000 ) ;
#27868=LINE ( 'NONE', #65689, #9844 ) ;
#27869=PLANE ( 'NONE',  #49700 ) ;
#27876=CARTESIAN_POINT ( 'NONE',  ( 11.78648345035335865, 7.593516549646607494, 195.0000000000000284 ) ) ;
#27885=CARTESIAN_POINT ( 'NONE',  ( -10.73351654964671020, 1.677516549646603794, 455.0000000000000568 ) ) ;
#27901=ORIENTED_EDGE ( 'NONE', *, *, #34275, .F. ) ;
#27904=LINE ( 'NONE', #1041, #9135 ) ;
#27910=CARTESIAN_POINT ( 'NONE',  ( -10.08346604330787777, 2.693516549646604918, 455.0000000000000568 ) ) ;
#27917=CARTESIAN_POINT ( 'NONE',  ( 10.09643294401457858, 9.293516549646566816, 455.0000000000000568 ) ) ;
#27920=ORIENTED_EDGE ( 'NONE', *, *, #10163, .F. ) ;
#27926=ORIENTED_EDGE ( 'NONE', *, *, #55732, .T. ) ;
#27933=DIRECTION ( 'NONE',  ( 7.808916176531286882E-15, 1.000000000000000000, 0.000000000000000000 ) ) ;
#27941=EDGE_LOOP ( 'NONE', ( #19749, #32626, #7041, #18707 ) ) ;
#27944=DIRECTION ( 'NONE',  ( -1.000000000000000000, 0.000000000000000000, 0.000000000000000000 ) ) ;
#27948=VECTOR ( 'NONE', #40389, 1000.000000000000000 ) ;
#27952=ORIENTED_EDGE ( 'NONE', *, *, #33129, .F. ) ;
#27956=VECTOR ( 'NONE', #8966, 1000.000000000000000 ) ;
#27976=FACE_OUTER_BOUND ( 'NONE', #40576, .T. ) ;
#27979=ORIENTED_EDGE ( 'NONE', *, *, #28002, .T. ) ;
#27982=EDGE_CURVE ( 'NONE', #60071, #11614, #36363, .T. ) ;
#27985=VERTEX_POINT ( 'NONE', #52283 ) ;
#27986=ADVANCED_FACE ( 'NONE', ( #40962 ), #51936, .F. ) ;
#27991=ORIENTED_EDGE ( 'NONE', *, *, #32612, .F. ) ;
#27992=DIRECTION ( 'NONE',  ( 0.000000000000000000, -1.000000000000000000, -3.673940397442059868E-16 ) ) ;
#27996=LINE ( 'NONE', #27308, #60508 ) ;
#27999=ORIENTED_EDGE ( 'NONE', *, *, #27055, .F. ) ;
#28002=EDGE_CURVE ( 'NONE', #6350, #59597, #41314, .T. ) ;
#28008=CARTESIAN_POINT ( 'NONE',  ( -10.19191654964686933, -11.48848345035334795, 455.0000000000000568 ) ) ;
#28014=CIRCLE ( 'NONE', #3180, 0.1999999999999996503 ) ;
#28026=EDGE_CURVE ( 'NONE', #9595, #41334, #25779, .T. ) ;
#28029=VERTEX_POINT ( 'NONE', #20800 ) ;
#28031=CARTESIAN_POINT ( 'NONE',  ( 2.906483450353343656, -10.92648345035346402, 455.0000000000000568 ) ) ;
#28032=CARTESIAN_POINT ( 'NONE',  ( 6.006483450353401921, 5.993516549646582092, 455.0000000000000568 ) ) ;
#28033=CARTESIAN_POINT ( 'NONE',  ( -2.277516549646816379, -9.841277389592805847, 455.0000000000000568 ) ) ;
#28036=ORIENTED_EDGE ( 'NONE', *, *, #60407, .F. ) ;
#28046=CARTESIAN_POINT ( 'NONE',  ( 11.32648345035337734, -7.606483450353492159, 455.0000000000000568 ) ) ;
#28049=EDGE_CURVE ( 'NONE', #52876, #57882, #47676, .T. ) ;
#28050=ADVANCED_FACE ( 'NONE', ( #15161 ), #5253, .F. ) ;
#28054=EDGE_CURVE ( 'NONE', #34099, #64234, #60271, .T. ) ;
#28059=CARTESIAN_POINT ( 'NONE',  ( -4.383466043307858939, 8.593516549646588842, 455.0000000000000568 ) ) ;
#28068=FACE_OUTER_BOUND ( 'NONE', #53314, .T. ) ;
#28075=CARTESIAN_POINT ( 'NONE',  ( 4.206483450353422526, 11.31351654964658415, 455.0000000000000568 ) ) ;
#28079=DIRECTION ( 'NONE',  ( -0.4999999999999755196, 0.8660254037844526964, 2.509347957447861534E-16 ) ) ;
#28083=ORIENTED_EDGE ( 'NONE', *, *, #39777, .F. ) ;
#28089=ORIENTED_EDGE ( 'NONE', *, *, #3371, .T. ) ;
#28090=ORIENTED_EDGE ( 'NONE', *, *, #63334, .T. ) ;
#28100=ORIENTED_EDGE ( 'NONE', *, *, #5693, .F. ) ;
#28103=LINE ( 'NONE', #43319, #58317 ) ;
#28109=EDGE_CURVE ( 'NONE', #19877, #33774, #47531, .T. ) ;
#28113=EDGE_CURVE ( 'NONE', #49641, #63752, #51410, .T. ) ;
#28120=ORIENTED_EDGE ( 'NONE', *, *, #37631, .T. ) ;
#28125=EDGE_CURVE ( 'NONE', #55190, #28029, #45232, .T. ) ;
#28132=CARTESIAN_POINT ( 'NONE',  ( 11.78648345035337819, -4.186483450353492231, 455.0000000000000568 ) ) ;
#28133=DIRECTION ( 'NONE',  ( 1.000000000000000000, 2.135044278125301343E-15, -0.000000000000000000 ) ) ;
#28137=DIRECTION ( 'NONE',  ( -1.000000000000000000, 9.050731179009442381E-15, 3.325184690495119758E-30 ) ) ;
#28141=LINE ( 'NONE', #1965, #21854 ) ;
#28143=ADVANCED_FACE ( 'NONE', ( #61666 ), #51061, .F. ) ;
#28145=VECTOR ( 'NONE', #42428, 1000.000000000000000 ) ;
#28146=ADVANCED_FACE ( 'NONE', ( #1570 ), #23137, .F. ) ;
#28151=DIRECTION ( 'NONE',  ( 3.491481338843132961E-15, 1.000000000000000000, 1.836970198721029934E-16 ) ) ;
#28166=VECTOR ( 'NONE', #52119, 1000.000000000000000 ) ;
#28179=ORIENTED_EDGE ( 'NONE', *, *, #4849, .T. ) ;
#28183=EDGE_CURVE ( 'NONE', #27705, #43873, #45048, .T. ) ;
#28202=CARTESIAN_POINT ( 'NONE',  ( 6.006483450353377940, 7.393516549646579783, 455.0000000000000568 ) ) ;
#28204=DIRECTION ( 'NONE',  ( 0.000000000000000000, -1.000000000000000000, -3.673940397442059868E-16 ) ) ;
#28207=DIRECTION ( 'NONE',  ( 0.7071067811865550112, 0.7071067811865401342, 0.000000000000000000 ) ) ;
#28212=CARTESIAN_POINT ( 'NONE',  ( -2.693516549646827851, -10.92648345035345692, 455.0000000000000568 ) ) ;
#28214=DIRECTION ( 'NONE',  ( -0.000000000000000000, 3.673940397442059868E-16, -1.000000000000000000 ) ) ;
#28217=CARTESIAN_POINT ( 'NONE',  ( 11.19368345035336709, -12.00648345035349251, 455.0000000000000568 ) ) ;
#28221=CYLINDRICAL_SURFACE ( 'NONE', #49052, 1.399999999999998579 ) ;
#28225=EDGE_CURVE ( 'NONE', #55626, #5311, #2277, .T. ) ;
#28235=ORIENTED_EDGE ( 'NONE', *, *, #67556, .F. ) ;
#28238=ORIENTED_EDGE ( 'NONE', *, *, #3490, .F. ) ;
#28258=EDGE_CURVE ( 'NONE', #66768, #32863, #28382, .T. ) ;
#28262=AXIS2_PLACEMENT_3D ( 'NONE', #48, #42116, #21611 ) ;
#28264=DIRECTION ( 'NONE',  ( -1.836970198721029934E-16, 1.836970198721036344E-16, -1.000000000000000000 ) ) ;
#28269=CARTESIAN_POINT ( 'NONE',  ( 6.619341603356846626, 4.734785091273825408, 455.0000000000000568 ) ) ;
#28275=DIRECTION ( 'NONE',  ( -0.000000000000000000, -0.000000000000000000, -1.000000000000000000 ) ) ;
#28277=VERTEX_POINT ( 'NONE', #68380 ) ;
#28292=VECTOR ( 'NONE', #67233, 1000.000000000000000 ) ;
#28294=FACE_OUTER_BOUND ( 'NONE', #41757, .T. ) ;
#28300=AXIS2_PLACEMENT_3D ( 'NONE', #15379, #46838, #20322 ) ;
#28302=CARTESIAN_POINT ( 'NONE',  ( -8.393516549646745872, -4.396432944014549093, 455.0000000000000568 ) ) ;
#28304=CARTESIAN_POINT ( 'NONE',  ( -7.259684009080030975, -7.811466277050769236, 455.0000000000000568 ) ) ;
#28306=LINE ( 'NONE', #12035, #7145 ) ;
#28317=CARTESIAN_POINT ( 'NONE',  ( -10.08346604330792751, -9.106483450353335840, 195.0000000000000284 ) ) ;
#28321=ORIENTED_EDGE ( 'NONE', *, *, #58646, .F. ) ;
#28323=PLANE ( 'NONE',  #45610 ) ;
#28326=CYLINDRICAL_SURFACE ( 'NONE', #59181, 2.204799999999997429 ) ;
#28327=CARTESIAN_POINT ( 'NONE',  ( 7.428221114745003462, -3.606483450353394016, 195.0000000000000284 ) ) ;
#28328=ORIENTED_EDGE ( 'NONE', *, *, #56768, .T. ) ;
#28331=ORIENTED_EDGE ( 'NONE', *, *, #18420, .T. ) ;
#28334=CARTESIAN_POINT ( 'NONE',  ( -7.813516549646711162, 11.99351654964660341, 455.0000000000000568 ) ) ;
#28337=CYLINDRICAL_SURFACE ( 'NONE', #64769, 0.8128000000000145109 ) ;
#28359=ORIENTED_EDGE ( 'NONE', *, *, #65638, .F. ) ;
#28360=AXIS2_PLACEMENT_3D ( 'NONE', #69799, #21355, #6133 ) ;
#28374=LINE ( 'NONE', #23768, #21959 ) ;
#28382=CIRCLE ( 'NONE', #55500, 2.204799999999997429 ) ;
#28387=VERTEX_POINT ( 'NONE', #63784 ) ;
#28399=CARTESIAN_POINT ( 'NONE',  ( -7.593516549646838421, -11.78648345035340839, 455.0000000000000568 ) ) ;
#28406=EDGE_CURVE ( 'NONE', #47490, #3732, #47512, .T. ) ;
#28407=CARTESIAN_POINT ( 'NONE',  ( 4.406483450353420928, 11.77351654964658501, 455.0000000000000568 ) ) ;
#28412=CARTESIAN_POINT ( 'NONE',  ( -7.252248008019455128, 5.380658396643134722, 195.0000000000000284 ) ) ;
#28413=CARTESIAN_POINT ( 'NONE',  ( 8.406483450353334774, 4.383466043307768345, 195.0000000000000284 ) ) ;
#28425=ADVANCED_FACE ( 'NONE', ( #35486 ), #13930, .F. ) ;
#28432=DIRECTION ( 'NONE',  ( 1.000000000000000000, -3.491481338843132961E-15, -1.836970198721036344E-16 ) ) ;
#28439=DIRECTION ( 'NONE',  ( 0.000000000000000000, -1.000000000000000000, 0.000000000000000000 ) ) ;
#28444=ORIENTED_EDGE ( 'NONE', *, *, #46788, .F. ) ;
#28447=EDGE_CURVE ( 'NONE', #53340, #47124, #32985, .T. ) ;
#28463=CARTESIAN_POINT ( 'NONE',  ( -2.893516549646828473, -10.92648345035345514, 455.0000000000000568 ) ) ;
#28464=CARTESIAN_POINT ( 'NONE',  ( -7.415254214038336400, 3.593516549646602609, 455.0000000000000568 ) ) ;
#28465=DIRECTION ( 'NONE',  ( 1.836970198721029934E-16, 1.836970198721010706E-16, -1.000000000000000000 ) ) ;
#28466=CYLINDRICAL_SURFACE ( 'NONE', #13895, 0.1999999999999987899 ) ;
#28467=ORIENTED_EDGE ( 'NONE', *, *, #43925, .F. ) ;
#28474=FACE_OUTER_BOUND ( 'NONE', #18525, .T. ) ;
#28475=AXIS2_PLACEMENT_3D ( 'NONE', #1332, #39830, #6629 ) ;
#28476=EDGE_LOOP ( 'NONE', ( #34911, #3932, #68013, #16635 ) ) ;
#28481=EDGE_LOOP ( 'NONE', ( #67658, #15729, #52001, #52309 ) ) ;
#28482=EDGE_CURVE ( 'NONE', #45353, #39173, #45283, .T. ) ;
#28484=CARTESIAN_POINT ( 'NONE',  ( 12.00648345035340903, 7.813516549646560172, 455.0000000000000568 ) ) ;
#28490=ADVANCED_FACE ( 'NONE', ( #6471 ), #10383, .T. ) ;
#28494=DIRECTION ( 'NONE',  ( -1.000000000000000000, 0.000000000000000000, 0.000000000000000000 ) ) ;
#28499=ADVANCED_FACE ( 'NONE', ( #64148 ), #60193, .F. ) ;
#28500=ORIENTED_EDGE ( 'NONE', *, *, #25862, .F. ) ;
#28505=EDGE_LOOP ( 'NONE', ( #36356, #4174, #59005, #49668 ) ) ;
#28514=CARTESIAN_POINT ( 'NONE',  ( -11.31351654964670850, 4.193516549646605363, 455.0000000000000568 ) ) ;
#28515=VERTEX_POINT ( 'NONE', #1164 ) ;
#28522=DIRECTION ( 'NONE',  ( -8.673617379884087537E-15, -1.000000000000000000, 0.000000000000000000 ) ) ;
#28525=EDGE_CURVE ( 'NONE', #4544, #19912, #59167, .T. ) ;
#28537=DIRECTION ( 'NONE',  ( 1.000000000000000000, 0.000000000000000000, 0.000000000000000000 ) ) ;
#28546=AXIS2_PLACEMENT_3D ( 'NONE', #46553, #68131, #19675 ) ;
#28549=ADVANCED_FACE ( 'NONE', ( #23418 ), #66199, .F. ) ;
#28551=CARTESIAN_POINT ( 'NONE',  ( 2.906483450353417375, 10.08346604330775875, 455.0000000000000568 ) ) ;
#28555=LINE ( 'NONE', #50129, #40255 ) ;
#28568=DIRECTION ( 'NONE',  ( 1.836970198721029934E-16, 1.836970198721010706E-16, -1.000000000000000000 ) ) ;
#28580=ORIENTED_EDGE ( 'NONE', *, *, #19213, .F. ) ;
#28585=VERTEX_POINT ( 'NONE', #38978 ) ;
#28586=VECTOR ( 'NONE', #353, 1000.000000000000000 ) ;
#28600=DIRECTION ( 'NONE',  ( 0.8660254037844563602, 0.4999999999999695244, 2.509347957447842799E-16 ) ) ;
#28602=ORIENTED_EDGE ( 'NONE', *, *, #44237, .F. ) ;
#28604=AXIS2_PLACEMENT_3D ( 'NONE', #2651, #24230, #67369 ) ;
#28610=DIRECTION ( 'NONE',  ( 0.000000000000000000, -1.000000000000000000, 0.000000000000000000 ) ) ;
#28622=VERTEX_POINT ( 'NONE', #34708 ) ;
#28632=CARTESIAN_POINT ( 'NONE',  ( 7.272650909786598561, -4.201500623656027500, 195.0000000000000284 ) ) ;
#28636=ORIENTED_EDGE ( 'NONE', *, *, #12768, .F. ) ;
#28638=DIRECTION ( 'NONE',  ( 0.000000000000000000, -3.673940397442059868E-16, 1.000000000000000000 ) ) ;
#28641=PLANE ( 'NONE',  #45857 ) ;
#28643=APPLICATION_CONTEXT ( 'automotive_design' ) ;
#28646=DIRECTION ( 'NONE',  ( 0.000000000000000000, -3.673940397442059868E-16, 1.000000000000000000 ) ) ;
#28647=VECTOR ( 'NONE', #4240, 1000.000000000000000 ) ;
#28648=VERTEX_POINT ( 'NONE', #50630 ) ;
#28649=DIRECTION ( 'NONE',  ( -0.000000000000000000, -0.000000000000000000, -1.000000000000000000 ) ) ;
#28665=EDGE_CURVE ( 'NONE', #64711, #66347, #1490, .T. ) ;
#28666=ORIENTED_EDGE ( 'NONE', *, *, #12214, .F. ) ;
#28681=VERTEX_POINT ( 'NONE', #58400 ) ;
#28684=DIRECTION ( 'NONE',  ( -1.000000000000000000, 0.000000000000000000, 0.000000000000000000 ) ) ;
#28687=ORIENTED_EDGE ( 'NONE', *, *, #14387, .T. ) ;
#28695=EDGE_LOOP ( 'NONE', ( #22710, #48618, #63593, #37254 ) ) ;
#28701=ORIENTED_EDGE ( 'NONE', *, *, #1893, .T. ) ;
#28702=ORIENTED_EDGE ( 'NONE', *, *, #18591, .F. ) ;
#28715=ORIENTED_EDGE ( 'NONE', *, *, #7024, .F. ) ;
#28726=ORIENTED_EDGE ( 'NONE', *, *, #9436, .F. ) ;
#28727=DIRECTION ( 'NONE',  ( -1.000000000000000000, 0.000000000000000000, 0.000000000000000000 ) ) ;
#28734=VERTEX_POINT ( 'NONE', #3947 ) ;
#28740=DIRECTION ( 'NONE',  ( -0.000000000000000000, 3.673940397442059868E-16, -1.000000000000000000 ) ) ;
#28742=EDGE_LOOP ( 'NONE', ( #53306, #63571, #39451, #66418 ) ) ;
#28743=DIRECTION ( 'NONE',  ( -0.000000000000000000, 3.673940397442059868E-16, -1.000000000000000000 ) ) ;
#28748=CARTESIAN_POINT ( 'NONE',  ( 4.406483450353340103, -11.32648345035347681, 455.0000000000000568 ) ) ;
#28750=DIRECTION ( 'NONE',  ( -1.836970198721029934E-16, 1.836970198721036344E-16, -1.000000000000000000 ) ) ;
#28755=CARTESIAN_POINT ( 'NONE',  ( -3.593516549646762481, -4.622483450353452206, 455.0000000000000568 ) ) ;
#28757=VERTEX_POINT ( 'NONE', #30107 ) ;
#28764=ADVANCED_FACE ( 'NONE', ( #3241 ), #57332, .F. ) ;
#28765=DIRECTION ( 'NONE',  ( 0.7671651518153006499, 0.6414496315691565753, 0.000000000000000000 ) ) ;
#28769=ORIENTED_EDGE ( 'NONE', *, *, #36596, .F. ) ;
#28773=EDGE_LOOP ( 'NONE', ( #7375, #37507, #32528, #26727 ) ) ;
#28776=CARTESIAN_POINT ( 'NONE',  ( -4.383466043307859827, 8.393516549646591329, 455.0000000000000568 ) ) ;
#28778=CARTESIAN_POINT ( 'NONE',  ( 10.92648345035337343, -9.306483450353395526, 195.0000000000000284 ) ) ;
#28783=AXIS2_PLACEMENT_3D ( 'NONE', #1879, #23790, #61605 ) ;
#28787=DIRECTION ( 'NONE',  ( -1.836970198721029934E-16, 1.836970198721036344E-16, -1.000000000000000000 ) ) ;
#28791=AXIS2_PLACEMENT_3D ( 'NONE', #64977, #20440, #58969 ) ;
#28799=DIRECTION ( 'NONE',  ( 1.079558018506126625E-14, 1.000000000000000000, 1.836970198721016622E-16 ) ) ;
#28804=FACE_OUTER_BOUND ( 'NONE', #63818, .T. ) ;
#28808=FACE_OUTER_BOUND ( 'NONE', #63365, .T. ) ;
#28815=LINE ( 'NONE', #45080, #66644 ) ;
#28819=LINE ( 'NONE', #51450, #53174 ) ;
#28822=ORIENTED_EDGE ( 'NONE', *, *, #25209, .T. ) ;
#28826=ORIENTED_EDGE ( 'NONE', *, *, #62996, .T. ) ;
#28832=ORIENTED_EDGE ( 'NONE', *, *, #55719, .F. ) ;
#28840=AXIS2_PLACEMENT_3D ( 'NONE', #14708, #20011, #10107 ) ;
#28841=AXIS2_PLACEMENT_3D ( 'NONE', #31095, #47698, #26143 ) ;
#28856=ORIENTED_EDGE ( 'NONE', *, *, #29196, .F. ) ;
#28860=EDGE_CURVE ( 'NONE', #19296, #6839, #47769, .T. ) ;
#28867=CARTESIAN_POINT ( 'NONE',  ( -7.798499376344111056, -7.272650909786579909, 195.0000000000000284 ) ) ;
#28870=FACE_OUTER_BOUND ( 'NONE', #61675, .T. ) ;
#28877=EDGE_CURVE ( 'NONE', #59188, #26479, #38599, .T. ) ;
#28884=CARTESIAN_POINT ( 'NONE',  ( 6.006483450353379716, -6.006483450353490738, 455.0000000000000568 ) ) ;
#28894=AXIS2_PLACEMENT_3D ( 'NONE', #5854, #44350, #66288 ) ;
#28905=EDGE_CURVE ( 'NONE', #38001, #54143, #31874, .T. ) ;
#28909=DIRECTION ( 'NONE',  ( 0.7071067811865474617, -0.7071067811865474617, -2.597868168706479611E-16 ) ) ;
#28914=AXIS2_PLACEMENT_3D ( 'NONE', #63070, #15689, #53182 ) ;
#28920=EDGE_CURVE ( 'NONE', #50899, #22396, #32212, .T. ) ;
#28943=VERTEX_POINT ( 'NONE', #38891 ) ;
#28945=CIRCLE ( 'NONE', #61695, 0.5999999999999998668 ) ;
#28947=DIRECTION ( 'NONE',  ( 3.491481338843134144E-15, 1.000000000000000000, 1.836970198721030181E-16 ) ) ;
#28949=AXIS2_PLACEMENT_3D ( 'NONE', #16737, #32984, #10382 ) ;
#28965=EDGE_CURVE ( 'NONE', #15138, #53340, #197, .T. ) ;
#28989=VECTOR ( 'NONE', #14251, 1000.000000000000114 ) ;
#29000=DIRECTION ( 'NONE',  ( -0.000000000000000000, -0.000000000000000000, -1.000000000000000000 ) ) ;
#29005=CARTESIAN_POINT ( 'NONE',  ( 7.606483450353380249, -11.78648345035349010, 455.0000000000000568 ) ) ;
#29014=LINE ( 'NONE', #3550, #24250 ) ;
#29016=ORIENTED_EDGE ( 'NONE', *, *, #60901, .T. ) ;
#29019=ORIENTED_EDGE ( 'NONE', *, *, #37631, .F. ) ;
#29032=ORIENTED_EDGE ( 'NONE', *, *, #1190, .F. ) ;
#29047=DIRECTION ( 'NONE',  ( 0.7071067811865602293, 0.7071067811865348052, 2.597868168706466792E-16 ) ) ;
#29048=DIRECTION ( 'NONE',  ( 0.000000000000000000, -0.000000000000000000, 1.000000000000000000 ) ) ;
#29053=PLANE ( 'NONE',  #66357 ) ;
#29060=FACE_OUTER_BOUND ( 'NONE', #53523, .T. ) ;
#29074=EDGE_LOOP ( 'NONE', ( #8781, #32806, #56137, #12634 ) ) ;
#29076=DIRECTION ( 'NONE',  ( 1.000000000000000000, -5.120954910632640039E-15, 0.000000000000000000 ) ) ;
#29083=VERTEX_POINT ( 'NONE', #30729 ) ;
#29088=CARTESIAN_POINT ( 'NONE',  ( 4.740315990920143108, 4.188533722949256521, 195.0000000000000284 ) ) ;
#29102=VERTEX_POINT ( 'NONE', #46629 ) ;
#29104=AXIS2_PLACEMENT_3D ( 'NONE', #44264, #17397, #69784 ) ;
#29115=LINE ( 'NONE', #55637, #58997 ) ;
#29116=ORIENTED_EDGE ( 'NONE', *, *, #6814, .F. ) ;
#29121=LINE ( 'NONE', #55307, #15150 ) ;
#29124=ORIENTED_EDGE ( 'NONE', *, *, #14967, .T. ) ;
#29131=ORIENTED_EDGE ( 'NONE', *, *, #22399, .T. ) ;
#29136=DIRECTION ( 'NONE',  ( -8.359604446858500663E-15, -1.000000000000000000, 0.000000000000000000 ) ) ;
#29147=CARTESIAN_POINT ( 'NONE',  ( -4.173516549646666185, 11.99351654964658920, 455.0000000000000568 ) ) ;
#29152=ORIENTED_EDGE ( 'NONE', *, *, #17224, .T. ) ;
#29162=ORIENTED_EDGE ( 'NONE', *, *, #37157, .F. ) ;
#29179=PLANE ( 'NONE',  #31857 ) ;
#29180=ORIENTED_EDGE ( 'NONE', *, *, #33939, .F. ) ;
#29181=EDGE_CURVE ( 'NONE', #46347, #1592, #25424, .T. ) ;
#29190=CARTESIAN_POINT ( 'NONE',  ( -7.603567055985545942, 8.593516549646603053, 455.0000000000000568 ) ) ;
#29196=EDGE_CURVE ( 'NONE', #33331, #69428, #39729, .T. ) ;
#29202=CARTESIAN_POINT ( 'NONE',  ( -4.727349090213463612, 7.798499376343949407, 455.0000000000000568 ) ) ;
#29203=EDGE_LOOP ( 'NONE', ( #16202, #51128, #24367, #2678 ) ) ;
#29206=CARTESIAN_POINT ( 'NONE',  ( -2.752095193409373586, 9.942044687070435316, 455.0000000000000568 ) ) ;
#29210=CARTESIAN_POINT ( 'NONE',  ( 7.606483450353380249, -11.32648345035339155, 195.0000000000000284 ) ) ;
#29218=ORIENTED_EDGE ( 'NONE', *, *, #34405, .T. ) ;
#29239=DIRECTION ( 'NONE',  ( 1.011922027653137735E-14, 1.000000000000000000, 0.000000000000000000 ) ) ;
#29247=ORIENTED_EDGE ( 'NONE', *, *, #42317, .F. ) ;
#29254=VERTEX_POINT ( 'NONE', #54390 ) ;
#29257=ORIENTED_EDGE ( 'NONE', *, *, #26353, .F. ) ;
#29258=ADVANCED_FACE ( 'NONE', ( #5603 ), #5943, .T. ) ;
#29279=DIRECTION ( 'NONE',  ( 0.000000000000000000, 1.000000000000000000, 0.000000000000000000 ) ) ;
#29281=CIRCLE ( 'NONE', #63173, 0.3999999999999993006 ) ;
#29284=DIRECTION ( 'NONE',  ( -1.000000000000000000, 1.088659024508174257E-14, 0.000000000000000000 ) ) ;
#29285=ORIENTED_EDGE ( 'NONE', *, *, #15540, .T. ) ;
#29301=EDGE_CURVE ( 'NONE', #35322, #12465, #9875, .T. ) ;
#29321=EDGE_CURVE ( 'NONE', #35101, #22946, #2488, .T. ) ;
#29339=AXIS2_PLACEMENT_3D ( 'NONE', #52222, #25358, #63546 ) ;
#29344=AXIS2_PLACEMENT_3D ( 'NONE', #11926, #6638, #28207 ) ;
#29354=ORIENTED_EDGE ( 'NONE', *, *, #56331, .F. ) ;
#29358=DIRECTION ( 'NONE',  ( 1.000000000000000000, -0.000000000000000000, 0.000000000000000000 ) ) ;
#29362=EDGE_CURVE ( 'NONE', #26162, #9194, #38139, .T. ) ;
#29370=DIRECTION ( 'NONE',  ( -1.000000000000000000, 0.000000000000000000, 0.000000000000000000 ) ) ;
#29375=DIRECTION ( 'NONE',  ( 0.7071067811865500152, 0.7071067811865451302, 0.000000000000000000 ) ) ;
#29378=ORIENTED_EDGE ( 'NONE', *, *, #48773, .T. ) ;
#29387=DIRECTION ( 'NONE',  ( -0.000000000000000000, 3.673940397442059868E-16, -1.000000000000000000 ) ) ;
#29396=DIRECTION ( 'NONE',  ( -0.000000000000000000, -0.000000000000000000, -1.000000000000000000 ) ) ;
#29398=ORIENTED_EDGE ( 'NONE', *, *, #44980, .T. ) ;
#29402=CARTESIAN_POINT ( 'NONE',  ( 4.201500623656004407, 4.727349090213387228, 195.0000000000000284 ) ) ;
#29413=ADVANCED_FACE ( 'NONE', ( #33154 ), #34175, .T. ) ;
#29419=VECTOR ( 'NONE', #35401, 1000.000000000000000 ) ;
#29435=FACE_OUTER_BOUND ( 'NONE', #44165, .T. ) ;
#29439=ORIENTED_EDGE ( 'NONE', *, *, #47143, .F. ) ;
#29447=VECTOR ( 'NONE', #52027, 1000.000000000000000 ) ;
#29453=ADVANCED_FACE ( 'NONE', ( #55090 ), #11918, .F. ) ;
#29454=CARTESIAN_POINT ( 'NONE',  ( -9.828310488886053520, 2.277516549646603661, 455.0000000000000568 ) ) ;
#29457=VERTEX_POINT ( 'NONE', #33837 ) ;
#29458=ORIENTED_EDGE ( 'NONE', *, *, #46045, .F. ) ;
#29459=EDGE_CURVE ( 'NONE', #46212, #8276, #7027, .T. ) ;
#29463=ORIENTED_EDGE ( 'NONE', *, *, #23873, .F. ) ;
#29472=ORIENTED_EDGE ( 'NONE', *, *, #29301, .T. ) ;
#29484=FACE_OUTER_BOUND ( 'NONE', #13076, .T. ) ;
#29487=CARTESIAN_POINT ( 'NONE',  ( 9.804883450353456098, 11.07551654964653132, 455.0000000000000568 ) ) ;
#29489=VERTEX_POINT ( 'NONE', #65348 ) ;
#29491=DIRECTION ( 'NONE',  ( 0.000000000000000000, 0.000000000000000000, 1.000000000000000000 ) ) ;
#29492=CARTESIAN_POINT ( 'NONE',  ( -10.08346604330787777, 2.893516549646604208, 455.0000000000000568 ) ) ;
#29495=ORIENTED_EDGE ( 'NONE', *, *, #10433, .F. ) ;
#29504=CARTESIAN_POINT ( 'NONE',  ( 9.106483450353373144, 11.11351654964661329, 195.0000000000000284 ) ) ;
#29505=CARTESIAN_POINT ( 'NONE',  ( -10.73351654964663915, -1.090483450353293415, 195.0000000000000284 ) ) ;
#29512=LINE ( 'NONE', #19954, #19780 ) ;
#29517=CARTESIAN_POINT ( 'NONE',  ( 10.20488345035338185, -10.20488345035343336, 195.0000000000000284 ) ) ;
#29527=CARTESIAN_POINT ( 'NONE',  ( 3.606483450353369147, -7.428221114745098497, 455.0000000000000568 ) ) ;
#29530=ORIENTED_EDGE ( 'NONE', *, *, #16742, .T. ) ;
#29540=DIRECTION ( 'NONE',  ( 1.000000000000000000, 0.000000000000000000, 0.000000000000000000 ) ) ;
#29561=CARTESIAN_POINT ( 'NONE',  ( 2.706483450353343478, -10.92648345035346225, 455.0000000000000568 ) ) ;
#29574=DIRECTION ( 'NONE',  ( -1.836970198721029934E-16, 1.836970198721036344E-16, -1.000000000000000000 ) ) ;
#29579=CARTESIAN_POINT ( 'NONE',  ( -4.188533722949421723, -7.272650909786664286, 455.0000000000000568 ) ) ;
#29586=AXIS2_PLACEMENT_3D ( 'NONE', #54736, #39158, #12959 ) ;
#29588=CARTESIAN_POINT ( 'NONE',  ( -7.259684009079930611, 4.188533722949235205, 195.0000000000000284 ) ) ;
#29589=LINE ( 'NONE', #23941, #6656 ) ;
#29590=CARTESIAN_POINT ( 'NONE',  ( -2.993516549646791258, -7.428221114745081621, 455.0000000000000568 ) ) ;
#29598=VECTOR ( 'NONE', #46849, 1000.000000000000000 ) ;
#29602=FACE_OUTER_BOUND ( 'NONE', #69767, .T. ) ;
#29611=ORIENTED_EDGE ( 'NONE', *, *, #22736, .T. ) ;
#29612=PLANE ( 'NONE',  #67167 ) ;
#29613=DIRECTION ( 'NONE',  ( -1.836970198721029934E-16, 1.836970198721036344E-16, -1.000000000000000000 ) ) ;
#29614=ORIENTED_EDGE ( 'NONE', *, *, #29782, .F. ) ;
#29616=LINE ( 'NONE', #36333, #66703 ) ;
#29619=EDGE_CURVE ( 'NONE', #14148, #56608, #9423, .T. ) ;
#29622=CARTESIAN_POINT ( 'NONE',  ( -6.606374702650169795, 4.734785091273855606, 195.0000000000000284 ) ) ;
#29630=EDGE_LOOP ( 'NONE', ( #48185, #44945, #23948, #34927 ) ) ;
#29634=AXIS2_PLACEMENT_3D ( 'NONE', #44041, #5882, #33093 ) ;
#29635=ORIENTED_EDGE ( 'NONE', *, *, #39732, .T. ) ;
#29639=LINE ( 'NONE', #45548, #69447 ) ;
#29650=CARTESIAN_POINT ( 'NONE',  ( 6.006483450353379716, -6.006483450353394815, 195.0000000000000284 ) ) ;
#29674=VERTEX_POINT ( 'NONE', #31368 ) ;
#29687=ADVANCED_FACE ( 'NONE', ( #4481 ), #58576, .T. ) ;
#29692=DIRECTION ( 'NONE',  ( 1.000000000000000000, -1.671920889371702854E-15, 0.000000000000000000 ) ) ;
#29695=ORIENTED_EDGE ( 'NONE', *, *, #41483, .T. ) ;
#29698=EDGE_CURVE ( 'NONE', #65774, #26484, #48853, .T. ) ;
#29700=DIRECTION ( 'NONE',  ( -1.000000000000000000, 3.491481338843133355E-15, 1.836970198721036344E-16 ) ) ;
#29701=ORIENTED_EDGE ( 'NONE', *, *, #16406, .T. ) ;
#29709=CARTESIAN_POINT ( 'NONE',  ( 6.619341603356837744, -4.747751991980742936, 455.0000000000000568 ) ) ;
#29717=AXIS2_PLACEMENT_3D ( 'NONE', #32753, #33450, #65297 ) ;
#29724=CIRCLE ( 'NONE', #38764, 0.5999999999999998668 ) ;
#29728=EDGE_CURVE ( 'NONE', #21380, #67902, #47953, .T. ) ;
#29735=ADVANCED_FACE ( 'NONE', ( #37353 ), #36642, .F. ) ;
#29738=CARTESIAN_POINT ( 'NONE',  ( 7.806483450353379538, -11.12648345035348996, 455.0000000000000568 ) ) ;
#29743=CARTESIAN_POINT ( 'NONE',  ( 9.804883450353379715, -10.20488345035352928, 455.0000000000000568 ) ) ;
#29746=DIRECTION ( 'NONE',  ( 1.156482317317870187E-14, 1.000000000000000000, 0.000000000000000000 ) ) ;
#29760=AXIS2_PLACEMENT_3D ( 'NONE', #37888, #11680, #32587 ) ;
#29775=ADVANCED_FACE ( 'NONE', ( #69865 ), #53968, .F. ) ;
#29776=LINE ( 'NONE', #2913, #39801 ) ;
#29778=DIRECTION ( 'NONE',  ( 1.836970198721029934E-16, 1.836970198721010706E-16, -1.000000000000000000 ) ) ;
#29782=EDGE_CURVE ( 'NONE', #24541, #24415, #16129, .T. ) ;
#29784=CARTESIAN_POINT ( 'NONE',  ( -11.33351654964668676, -1.090483450353329165, 455.0000000000000568 ) ) ;
#29790=CARTESIAN_POINT ( 'NONE',  ( -4.242044687070659847, -8.465062094116134972, 455.0000000000000568 ) ) ;
#29791=LINE ( 'NONE', #17796, #56567 ) ;
#29795=VERTEX_POINT ( 'NONE', #66636 ) ;
#29797=ORIENTED_EDGE ( 'NONE', *, *, #51092, .F. ) ;
#29799=CARTESIAN_POINT ( 'NONE',  ( -11.07551654964681731, -9.804883450353372609, 455.0000000000000568 ) ) ;
#29805=ORIENTED_EDGE ( 'NONE', *, *, #879, .T. ) ;
#29816=CARTESIAN_POINT ( 'NONE',  ( 7.826483450353421745, 11.99351654964657499, 455.0000000000000568 ) ) ;
#29818=ORIENTED_EDGE ( 'NONE', *, *, #21992, .T. ) ;
#29831=ORIENTED_EDGE ( 'NONE', *, *, #987, .T. ) ;
#29833=DIRECTION ( 'NONE',  ( -1.836970198721029934E-16, 1.836970198721036344E-16, -1.000000000000000000 ) ) ;
#29836=CARTESIAN_POINT ( 'NONE',  ( -5.993516549646728642, -6.006483450353378828, 195.0000000000000284 ) ) ;
#29843=EDGE_LOOP ( 'NONE', ( #8447, #39323, #39667, #69223, #35440, #1516, #12313, #68855 ) ) ;
#29853=CARTESIAN_POINT ( 'NONE',  ( -7.603567055985545942, 8.393516549646601987, 455.0000000000000568 ) ) ;
#29854=DIRECTION ( 'NONE',  ( 1.836970198721029934E-16, 1.836970198721010706E-16, -1.000000000000000000 ) ) ;
#29866=CARTESIAN_POINT ( 'NONE',  ( 9.306483450353379538, -10.92648345035339119, 195.0000000000000284 ) ) ;
#29871=CIRCLE ( 'NONE', #5058, 0.2000000000000005107 ) ;
#29878=DIRECTION ( 'NONE',  ( -1.000000000000000000, 3.491481338843133355E-15, 1.836970198721036344E-16 ) ) ;
#29885=ORIENTED_EDGE ( 'NONE', *, *, #40798, .F. ) ;
#29895=CARTESIAN_POINT ( 'NONE',  ( -4.727349090213463612, 7.798499376343949407, 195.0000000000000284 ) ) ;
#29896=ADVANCED_FACE ( 'NONE', ( #36476 ), #4327, .F. ) ;
#29899=ORIENTED_EDGE ( 'NONE', *, *, #5356, .T. ) ;
#29914=VECTOR ( 'NONE', #20172, 999.9999999999998863 ) ;
#29919=DIRECTION ( 'NONE',  ( -1.836970198721029934E-16, 1.836970198721036344E-16, -1.000000000000000000 ) ) ;
#29920=VECTOR ( 'NONE', #33308, 1000.000000000000000 ) ;
#29921=DIRECTION ( 'NONE',  ( 1.000000000000000000, 0.000000000000000000, 0.000000000000000000 ) ) ;
#29928=VERTEX_POINT ( 'NONE', #29504 ) ;
#29941=FACE_OUTER_BOUND ( 'NONE', #46764, .T. ) ;
#29943=EDGE_CURVE ( 'NONE', #30449, #11172, #56729, .T. ) ;
#29946=CARTESIAN_POINT ( 'NONE',  ( 8.406483450353379183, -6.344579767990839336, 195.0000000000000284 ) ) ;
#29949=CARTESIAN_POINT ( 'NONE',  ( -10.19191654964682137, -11.48848345035329821, 195.0000000000000284 ) ) ;
#29951=ORIENTED_EDGE ( 'NONE', *, *, #54297, .F. ) ;
#29953=DIRECTION ( 'NONE',  ( -1.062171939662868407E-14, -1.000000000000000000, 0.000000000000000000 ) ) ;
#29954=CARTESIAN_POINT ( 'NONE',  ( -9.942044687070568543, 9.234937905883914055, 455.0000000000000568 ) ) ;
#29964=FACE_OUTER_BOUND ( 'NONE', #14525, .T. ) ;
#29967=CYLINDRICAL_SURFACE ( 'NONE', #48398, 0.1999999999999987899 ) ;
#29968=VECTOR ( 'NONE', #67826, 1000.000000000000000 ) ;
#29972=DIRECTION ( 'NONE',  ( -1.000000000000000000, 0.000000000000000000, 0.000000000000000000 ) ) ;
#29973=ORIENTED_EDGE ( 'NONE', *, *, #61442, .T. ) ;
#29980=VECTOR ( 'NONE', #2639, 999.9999999999998863 ) ;
#29982=VERTEX_POINT ( 'NONE', #67350 ) ;
#29989=VERTEX_POINT ( 'NONE', #29853 ) ;
#29990=CARTESIAN_POINT ( 'NONE',  ( 4.186483450353335023, -12.00648345035338238, 195.0000000000000284 ) ) ;
#29997=VERTEX_POINT ( 'NONE', #23852 ) ;
#30006=CARTESIAN_POINT ( 'NONE',  ( -9.828310488885993124, -1.690483450353310158, 195.0000000000000284 ) ) ;
#30027=ORIENTED_EDGE ( 'NONE', *, *, #31093, .F. ) ;
#30038=VECTOR ( 'NONE', #67867, 1000.000000000000000 ) ;
#30040=ORIENTED_EDGE ( 'NONE', *, *, #22333, .T. ) ;
#30045=DIRECTION ( 'NONE',  ( 3.491481338843133355E-15, 1.000000000000000000, 1.836970198721029934E-16 ) ) ;
#30047=CARTESIAN_POINT ( 'NONE',  ( 11.32648345035333470, 4.393516549646570901, 195.0000000000000284 ) ) ;
#30052=VERTEX_POINT ( 'NONE', #22701 ) ;
#30054=VECTOR ( 'NONE', #53891, 1000.000000000000000 ) ;
#30055=ORIENTED_EDGE ( 'NONE', *, *, #52157, .F. ) ;
#30060=DIRECTION ( 'NONE',  ( -0.8660254037844322683, 0.5000000000000111022, 0.000000000000000000 ) ) ;
#30065=ORIENTED_EDGE ( 'NONE', *, *, #23000, .T. ) ;
#30077=DIRECTION ( 'NONE',  ( 1.011922027653137735E-14, 1.000000000000000000, 0.000000000000000000 ) ) ;
#30104=ORIENTED_EDGE ( 'NONE', *, *, #29943, .F. ) ;
#30106=AXIS2_PLACEMENT_3D ( 'NONE', #26687, #48601, #37302 ) ;
#30107=CARTESIAN_POINT ( 'NONE',  ( 8.406483450353405829, 7.603567055985406498, 455.0000000000000568 ) ) ;
#30119=CARTESIAN_POINT ( 'NONE',  ( -1.077516549646778010, -10.74648345035343056, 195.0000000000000284 ) ) ;
#30121=EDGE_CURVE ( 'NONE', #26906, #47459, #6769, .T. ) ;
#30122=EDGE_CURVE ( 'NONE', #20149, #54700, #16182, .T. ) ;
#30160=CARTESIAN_POINT ( 'NONE',  ( 6.006483450353401921, 7.393516549646579783, 455.0000000000000568 ) ) ;
#30169=ORIENTED_EDGE ( 'NONE', *, *, #41936, .F. ) ;
#30170=CARTESIAN_POINT ( 'NONE',  ( -10.08346604330787777, 2.893516549646604208, 455.0000000000000568 ) ) ;
#30181=EDGE_LOOP ( 'NONE', ( #52626, #16019, #67916, #23206 ) ) ;
#30182=EDGE_LOOP ( 'NONE', ( #15967, #28726, #56323, #59215 ) ) ;
#30184=VERTEX_POINT ( 'NONE', #3141 ) ;
#30186=DIRECTION ( 'NONE',  ( 0.000000000000000000, 1.000000000000000000, 3.673940397442059868E-16 ) ) ;
#30191=CARTESIAN_POINT ( 'NONE',  ( -4.383466043307922000, -8.606483450353396236, 195.0000000000000284 ) ) ;
#30206=FACE_OUTER_BOUND ( 'NONE', #16067, .T. ) ;
#30207=ORIENTED_EDGE ( 'NONE', *, *, #2942, .F. ) ;
#30208=CARTESIAN_POINT ( 'NONE',  ( 4.201500623656039934, 7.259684009079806266, 455.0000000000000568 ) ) ;
#30228=AXIS2_PLACEMENT_3D ( 'NONE', #23749, #24451, #8522 ) ;
#30232=DIRECTION ( 'NONE',  ( -0.7071067811865401342, 0.7071067811865550112, 1.365336182113289717E-30 ) ) ;
#30246=EDGE_LOOP ( 'NONE', ( #34844, #10011, #35483, #14772 ) ) ;
#30249=CARTESIAN_POINT ( 'NONE',  ( 12.00648345035336284, 7.813516549646607245, 195.0000000000000284 ) ) ;
#30268=VERTEX_POINT ( 'NONE', #26451 ) ;
#30271=VERTEX_POINT ( 'NONE', #3487 ) ;
#30273=CARTESIAN_POINT ( 'NONE',  ( 8.406483450353334774, 4.383466043307768345, 195.0000000000000284 ) ) ;
#30287=DIRECTION ( 'NONE',  ( 0.000000000000000000, -3.673940397442059868E-16, 1.000000000000000000 ) ) ;
#30298=DIRECTION ( 'NONE',  ( 9.050731179009442381E-15, 1.000000000000000000, 0.000000000000000000 ) ) ;
#30302=CARTESIAN_POINT ( 'NONE',  ( 4.396432944014576627, 8.393516549646587777, 455.0000000000000568 ) ) ;
#30306=EDGE_CURVE ( 'NONE', #35699, #45713, #31764, .T. ) ;
#30308=CYLINDRICAL_SURFACE ( 'NONE', #18346, 0.5999999999999994227 ) ;
#30312=CARTESIAN_POINT ( 'NONE',  ( -2.893516549646771630, -10.09643294401457680, 195.0000000000000284 ) ) ;
#30327=VECTOR ( 'NONE', #6198, 1000.000000000000000 ) ;
#30329=DIRECTION ( 'NONE',  ( -1.000000000000000000, 0.000000000000000000, 0.000000000000000000 ) ) ;
#30333=ORIENTED_EDGE ( 'NONE', *, *, #24853, .T. ) ;
#30353=EDGE_CURVE ( 'NONE', #5423, #60569, #27435, .T. ) ;
#30354=CARTESIAN_POINT ( 'NONE',  ( 11.78648345035333200, 4.173516549646566709, 195.0000000000000284 ) ) ;
#30355=DIRECTION ( 'NONE',  ( 0.8660254037844322683, -0.5000000000000111022, 6.723777587268230953E-17 ) ) ;
#30356=ORIENTED_EDGE ( 'NONE', *, *, #14742, .F. ) ;
#30360=VERTEX_POINT ( 'NONE', #64623 ) ;
#30365=DIRECTION ( 'NONE',  ( 8.673617379884068604E-15, 1.000000000000000000, 0.000000000000000000 ) ) ;
#30376=CARTESIAN_POINT ( 'NONE',  ( 7.265214908726092879, 5.380658396643145380, 195.0000000000000284 ) ) ;
#30377=VECTOR ( 'NONE', #37615, 1000.000000000000000 ) ;
#30379=CARTESIAN_POINT ( 'NONE',  ( 11.12648345035335851, 7.793516549646610336, 195.0000000000000284 ) ) ;
#30382=DIRECTION ( 'NONE',  ( -0.000000000000000000, 3.673940397442059868E-16, -1.000000000000000000 ) ) ;
#30384=FACE_OUTER_BOUND ( 'NONE', #64595, .T. ) ;
#30385=DIRECTION ( 'NONE',  ( 1.836970198721029934E-16, 1.836970198721010706E-16, -1.000000000000000000 ) ) ;
#30387=AXIS2_PLACEMENT_3D ( 'NONE', #24998, #9083, #25351 ) ;
#30388=VECTOR ( 'NONE', #21843, 1000.000000000000000 ) ;
#30393=ADVANCED_FACE ( 'NONE', ( #22872 ), #27144, .T. ) ;
#30395=ADVANCED_FACE ( 'NONE', ( #54709 ), #5240, .F. ) ;
#30405=CARTESIAN_POINT ( 'NONE',  ( 4.186483450353335023, -12.00648345035338238, 195.0000000000000284 ) ) ;
#30409=ORIENTED_EDGE ( 'NONE', *, *, #41560, .T. ) ;
#30423=LINE ( 'NONE', #2839, #58647 ) ;
#30432=ORIENTED_EDGE ( 'NONE', *, *, #48075, .F. ) ;
#30437=AXIS2_PLACEMENT_3D ( 'NONE', #8715, #4473, #29921 ) ;
#30449=VERTEX_POINT ( 'NONE', #44088 ) ;
#30451=DIRECTION ( 'NONE',  ( 0.000000000000000000, 1.000000000000000000, 0.000000000000000000 ) ) ;
#30456=LINE ( 'NONE', #52028, #62254 ) ;
#30462=DIRECTION ( 'NONE',  ( -1.000000000000000000, 1.047444401652939849E-14, -1.836970198721010706E-16 ) ) ;
#30464=LINE ( 'NONE', #69710, #61978 ) ;
#30468=CIRCLE ( 'NONE', #14378, 0.2000000000000005107 ) ;
#30474=CARTESIAN_POINT ( 'NONE',  ( -7.415254214038345282, -3.006483450353401032, 455.0000000000000568 ) ) ;
#30476=VERTEX_POINT ( 'NONE', #59705 ) ;
#30488=ORIENTED_EDGE ( 'NONE', *, *, #25989, .T. ) ;
#30497=ORIENTED_EDGE ( 'NONE', *, *, #11006, .T. ) ;
#30501=ORIENTED_EDGE ( 'NONE', *, *, #67057, .T. ) ;
#30523=VERTEX_POINT ( 'NONE', #65700 ) ;
#30524=EDGE_CURVE ( 'NONE', #31048, #20952, #44459, .T. ) ;
#30530=VERTEX_POINT ( 'NONE', #27876 ) ;
#30533=ORIENTED_EDGE ( 'NONE', *, *, #56801, .F. ) ;
#30538=PLANE ( 'NONE',  #1796 ) ;
#30539=VERTEX_POINT ( 'NONE', #49091 ) ;
#30556=LINE ( 'NONE', #58126, #49063 ) ;
#30558=AXIS2_PLACEMENT_3D ( 'NONE', #32629, #54204, #5761 ) ;
#30559=VERTEX_POINT ( 'NONE', #6980 ) ;
#30565=AXIS2_PLACEMENT_3D ( 'NONE', #20457, #10541, #64297 ) ;
#30566=DIRECTION ( 'NONE',  ( 0.7671651518153105309, -0.6414496315691445849, -0.000000000000000000 ) ) ;
#30576=EDGE_CURVE ( 'NONE', #26897, #61486, #50122, .T. ) ;
#30578=CARTESIAN_POINT ( 'NONE',  ( 4.740315990920191958, 4.188533722949208560, 455.0000000000000568 ) ) ;
#30583=DIRECTION ( 'NONE',  ( -1.000000000000000000, 0.000000000000000000, 0.000000000000000000 ) ) ;
#30586=VERTEX_POINT ( 'NONE', #43791 ) ;
#30587=CARTESIAN_POINT ( 'NONE',  ( -7.813516549646711162, 11.99351654964660341, 195.0000000000000284 ) ) ;
#30592=LINE ( 'NONE', #8675, #21759 ) ;
#30594=EDGE_LOOP ( 'NONE', ( #23789, #38622, #5330, #48003 ) ) ;
#30604=CARTESIAN_POINT ( 'NONE',  ( 7.616533956692213003, -8.606483450353492159, 455.0000000000000568 ) ) ;
#30612=ORIENTED_EDGE ( 'NONE', *, *, #54475, .F. ) ;
#30613=ORIENTED_EDGE ( 'NONE', *, *, #45062, .F. ) ;
#30618=CARTESIAN_POINT ( 'NONE',  ( 9.804883450353454322, 10.19191654964656912, 455.0000000000000568 ) ) ;
#30625=CIRCLE ( 'NONE', #2253, 0.1999999999999987899 ) ;
#30638=ORIENTED_EDGE ( 'NONE', *, *, #44602, .F. ) ;
#30640=DIRECTION ( 'NONE',  ( 1.000000000000000000, 0.000000000000000000, 0.000000000000000000 ) ) ;
#30646=DIRECTION ( 'NONE',  ( -0.7071067811865549002, -0.7071067811865401342, -2.597868168706466792E-16 ) ) ;
#30648=DIRECTION ( 'NONE',  ( -1.000000000000000000, 3.491481338843133355E-15, 1.836970198721036344E-16 ) ) ;
#30660=FACE_OUTER_BOUND ( 'NONE', #44450, .T. ) ;
#30671=CIRCLE ( 'NONE', #201, 0.2000000000000005107 ) ;
#30676=ORIENTED_EDGE ( 'NONE', *, *, #39294, .T. ) ;
#30687=ORIENTED_EDGE ( 'NONE', *, *, #25215, .F. ) ;
#30692=CARTESIAN_POINT ( 'NONE',  ( 2.906483450353420039, 10.91351654964658913, 455.0000000000000568 ) ) ;
#30694=DIRECTION ( 'NONE',  ( 1.836970198721029934E-16, 1.836970198721010706E-16, -1.000000000000000000 ) ) ;
#30697=AXIS2_PLACEMENT_3D ( 'NONE', #66471, #54836, #49865 ) ;
#30705=DIRECTION ( 'NONE',  ( -1.836970198721029934E-16, 1.836970198721036344E-16, -1.000000000000000000 ) ) ;
#30714=VERTEX_POINT ( 'NONE', #35233 ) ;
#30717=ORIENTED_EDGE ( 'NONE', *, *, #20368, .T. ) ;
#30722=DIRECTION ( 'NONE',  ( 1.000000000000000000, -1.047444401652939849E-14, 1.836970198721010706E-16 ) ) ;
#30723=CARTESIAN_POINT ( 'NONE',  ( 4.396432944014527777, -8.406483450353478659, 455.0000000000000568 ) ) ;
#30729=CARTESIAN_POINT ( 'NONE',  ( -7.259684009079916400, -4.201500623655988420, 195.0000000000000284 ) ) ;
#30731=CIRCLE ( 'NONE', #46513, 0.2000000000000005107 ) ;
#30736=CARTESIAN_POINT ( 'NONE',  ( -4.383466043307858939, 8.593516549646588842, 455.0000000000000568 ) ) ;
#30737=DIRECTION ( 'NONE',  ( 1.000000000000000000, -5.163402228214835223E-15, -1.836970198721039302E-16 ) ) ;
#30749=EDGE_CURVE ( 'NONE', #43736, #33316, #25002, .T. ) ;
#30755=FACE_OUTER_BOUND ( 'NONE', #7434, .T. ) ;
#30759=LINE ( 'NONE', #30405, #53472 ) ;
#30764=ORIENTED_EDGE ( 'NONE', *, *, #65775, .T. ) ;
#30766=VECTOR ( 'NONE', #10485, 1000.000000000000000 ) ;
#30775=CARTESIAN_POINT ( 'NONE',  ( 11.34648345035338046, -1.090483450353491035, 455.0000000000000568 ) ) ;
#30793=EDGE_CURVE ( 'NONE', #17426, #48590, #64244, .T. ) ;
#30797=FACE_OUTER_BOUND ( 'NONE', #4906, .T. ) ;
#30800=CARTESIAN_POINT ( 'NONE',  ( -7.798499376344067535, 4.727349090213367688, 195.0000000000000284 ) ) ;
#30817=ORIENTED_EDGE ( 'NONE', *, *, #14393, .T. ) ;
#30822=DIRECTION ( 'NONE',  ( -1.048062100069321163E-14, -1.000000000000000000, 0.000000000000000000 ) ) ;
#30829=EDGE_CURVE ( 'NONE', #35354, #45642, #9088, .T. ) ;
#30840=CARTESIAN_POINT ( 'NONE',  ( -1.677516549646825839, -10.74648345035347141, 455.0000000000000568 ) ) ;
#30842=ORIENTED_EDGE ( 'NONE', *, *, #65408, .T. ) ;
#30847=VECTOR ( 'NONE', #60386, 1000.000000000000000 ) ;
#30851=DIRECTION ( 'NONE',  ( -1.836970198721029934E-16, 1.836970198721036344E-16, -1.000000000000000000 ) ) ;
#30852=ORIENTED_EDGE ( 'NONE', *, *, #1802, .F. ) ;
#30856=CARTESIAN_POINT ( 'NONE',  ( 7.616533956692213003, -8.606483450353396236, 195.0000000000000284 ) ) ;
#30860=FACE_BOUND ( 'NONE', #59431, .T. ) ;
#30864=AXIS2_PLACEMENT_3D ( 'NONE', #40749, #42145, #41798 ) ;
#30873=CARTESIAN_POINT ( 'NONE',  ( -7.259684009079983902, -7.811466277050722162, 195.0000000000000284 ) ) ;
#30879=EDGE_CURVE ( 'NONE', #38207, #20840, #68843, .T. ) ;
#30885=ORIENTED_EDGE ( 'NONE', *, *, #62173, .T. ) ;
#30894=DIRECTION ( 'NONE',  ( -1.836970198721029934E-16, 1.836970198721036344E-16, -1.000000000000000000 ) ) ;
#30895=LINE ( 'NONE', #25604, #53836 ) ;
#30897=VECTOR ( 'NONE', #2735, 1000.000000000000000 ) ;
#30900=VECTOR ( 'NONE', #44048, 1000.000000000000000 ) ;
#30908=LINE ( 'NONE', #30208, #34847 ) ;
#30911=ORIENTED_EDGE ( 'NONE', *, *, #62299, .F. ) ;
#30912=DIRECTION ( 'NONE',  ( 0.7071067811865474617, 0.7071067811865474617, 0.000000000000000000 ) ) ;
#30929=DIRECTION ( 'NONE',  ( 1.000000000000000000, 0.000000000000000000, 0.000000000000000000 ) ) ;
#30930=LINE ( 'NONE', #52503, #67757 ) ;
#30939=DIRECTION ( 'NONE',  ( 1.836970198721029934E-16, 1.836970198721010706E-16, -1.000000000000000000 ) ) ;
#30941=EDGE_CURVE ( 'NONE', #46298, #15622, #18321, .T. ) ;
#30948=CARTESIAN_POINT ( 'NONE',  ( 9.306483450353418618, 10.91351654964656426, 455.0000000000000568 ) ) ;
#30952=ORIENTED_EDGE ( 'NONE', *, *, #6953, .F. ) ;
#30957=ORIENTED_EDGE ( 'NONE', *, *, #23570, .F. ) ;
#30960=VECTOR ( 'NONE', #38941, 1000.000000000000000 ) ;
#30967=DIRECTION ( 'NONE',  ( -1.000000000000000000, 0.000000000000000000, 0.000000000000000000 ) ) ;
#30969=LINE ( 'NONE', #47239, #52545 ) ;
#30974=ORIENTED_EDGE ( 'NONE', *, *, #38021, .T. ) ;
#30975=AXIS2_PLACEMENT_3D ( 'NONE', #36220, #63453, #57788 ) ;
#30987=CARTESIAN_POINT ( 'NONE',  ( 10.09643294401453240, 9.093516549646613711, 195.0000000000000284 ) ) ;
#31005=DIRECTION ( 'NONE',  ( -1.000000000000000000, 1.047444401652939849E-14, 0.000000000000000000 ) ) ;
#31009=DIRECTION ( 'NONE',  ( -3.614007241618349165E-15, -1.000000000000000000, 0.000000000000000000 ) ) ;
#31010=EDGE_CURVE ( 'NONE', #27141, #40597, #23984, .T. ) ;
#31035=DIRECTION ( 'NONE',  ( 1.836970198721029934E-16, 1.836970198721010706E-16, -1.000000000000000000 ) ) ;
#31039=FACE_OUTER_BOUND ( 'NONE', #25234, .T. ) ;
#31040=EDGE_CURVE ( 'NONE', #65081, #2958, #27389, .T. ) ;
#31048=VERTEX_POINT ( 'NONE', #60662 ) ;
#31051=VECTOR ( 'NONE', #40427, 1000.000000000000000 ) ;
#31054=EDGE_LOOP ( 'NONE', ( #64314, #8977, #23576, #9485 ) ) ;
#31058=CARTESIAN_POINT ( 'NONE',  ( -11.18071654964669825, 11.99351654964660341, 455.0000000000000568 ) ) ;
#31067=FACE_OUTER_BOUND ( 'NONE', #865, .T. ) ;
#31070=VERTEX_POINT ( 'NONE', #51086 ) ;
#31071=CIRCLE ( 'NONE', #588, 0.1999999999999987899 ) ;
#31084=LINE ( 'NONE', #36378, #31331 ) ;
#31089=CARTESIAN_POINT ( 'NONE',  ( -7.813516549646711162, 11.99351654964660341, 195.0000000000000284 ) ) ;
#31091=CYLINDRICAL_SURFACE ( 'NONE', #49360, 0.1999999999999996503 ) ;
#31092=DIRECTION ( 'NONE',  ( 1.000000000000000000, 0.000000000000000000, 0.000000000000000000 ) ) ;
#31093=EDGE_CURVE ( 'NONE', #10643, #34099, #23523, .T. ) ;
#31095=CARTESIAN_POINT ( 'NONE',  ( 7.272650909786598561, -7.811466277050860718, 455.0000000000000568 ) ) ;
#31097=CIRCLE ( 'NONE', #38998, 0.1999999999999992339 ) ;
#31101=AXIS2_PLACEMENT_3D ( 'NONE', #26886, #69675, #42781 ) ;
#31113=CARTESIAN_POINT ( 'NONE',  ( 11.78648345035340839, 7.813516549646560172, 455.0000000000000568 ) ) ;
#31118=ADVANCED_FACE ( 'NONE', ( #35510 ), #28466, .F. ) ;
#31119=CARTESIAN_POINT ( 'NONE',  ( -5.993516549646711766, 5.993516549646603409, 455.0000000000000568 ) ) ;
#31120=ORIENTED_EDGE ( 'NONE', *, *, #52166, .T. ) ;
#31145=ORIENTED_EDGE ( 'NONE', *, *, #1949, .F. ) ;
#31147=VERTEX_POINT ( 'NONE', #2305 ) ;
#31149=CARTESIAN_POINT ( 'NONE',  ( 7.272650909786602114, 4.188533722949199678, 455.0000000000000568 ) ) ;
#31171=DIRECTION ( 'NONE',  ( 1.836970198721029934E-16, 1.836970198721010706E-16, -1.000000000000000000 ) ) ;
#31174=ORIENTED_EDGE ( 'NONE', *, *, #33839, .T. ) ;
#31189=FACE_OUTER_BOUND ( 'NONE', #48147, .T. ) ;
#31196=CARTESIAN_POINT ( 'NONE',  ( -9.942044687070568543, 2.752095193409294982, 455.0000000000000568 ) ) ;
#31201=DIRECTION ( 'NONE',  ( -1.836970198721029934E-16, 1.836970198721036344E-16, -1.000000000000000000 ) ) ;
#31205=AXIS2_PLACEMENT_3D ( 'NONE', #761, #69364, #37201 ) ;
#31207=CARTESIAN_POINT ( 'NONE',  ( 3.606483450353369147, -7.428221114745098497, 455.0000000000000568 ) ) ;
#31209=DIRECTION ( 'NONE',  ( -1.053224967557348291E-14, -1.000000000000000000, 0.000000000000000000 ) ) ;
#31213=CARTESIAN_POINT ( 'NONE',  ( 7.826483450353374671, 11.99351654964662295, 195.0000000000000284 ) ) ;
#31215=CARTESIAN_POINT ( 'NONE',  ( -5.380658396643234198, 4.734785091273867152, 195.0000000000000284 ) ) ;
#31216=VECTOR ( 'NONE', #63394, 1000.000000000000000 ) ;
#31230=DIRECTION ( 'NONE',  ( -1.000000000000000000, 0.000000000000000000, 0.000000000000000000 ) ) ;
#31239=EDGE_CURVE ( 'NONE', #15146, #30523, #47542, .T. ) ;
#31251=CARTESIAN_POINT ( 'NONE',  ( -1.853252480934758584, 9.404046420173985510, 195.0000000000000284 ) ) ;
#31258=ADVANCED_FACE ( 'NONE', ( #63457 ), #36948, .F. ) ;
#31260=DIRECTION ( 'NONE',  ( 1.000000000000000000, -1.920292680692490463E-14, 1.836970198720994682E-16 ) ) ;
#31273=CARTESIAN_POINT ( 'NONE',  ( 3.430747519065294071, -7.852485183457023510, 455.0000000000000568 ) ) ;
#31274=VECTOR ( 'NONE', #68166, 1000.000000000000000 ) ;
#31276=FACE_OUTER_BOUND ( 'NONE', #12441, .T. ) ;
#31277=DIRECTION ( 'NONE',  ( 0.000000000000000000, -1.000000000000000000, -3.673940397442060361E-16 ) ) ;
#31280=CARTESIAN_POINT ( 'NONE',  ( 9.955011587777235604, -2.765062094116182312, 455.0000000000000568 ) ) ;
#31281=VECTOR ( 'NONE', #14195, 1000.000000000000000 ) ;
#31288=CARTESIAN_POINT ( 'NONE',  ( 11.08848345035334404, -11.48848345035349183, 455.0000000000000568 ) ) ;
#31293=CARTESIAN_POINT ( 'NONE',  ( -7.813516549646836395, -11.78648345035340661, 455.0000000000000568 ) ) ;
#31297=EDGE_CURVE ( 'NONE', #46798, #31830, #37988, .T. ) ;
#31300=EDGE_LOOP ( 'NONE', ( #58483, #47810, #53708, #9269 ) ) ;
#31318=CARTESIAN_POINT ( 'NONE',  ( -9.404046420174124066, 1.853252480934674873, 455.0000000000000568 ) ) ;
#31320=CIRCLE ( 'NONE', #49375, 0.4000000000000010214 ) ;
#31321=AXIS2_PLACEMENT_3D ( 'NONE', #24771, #3557, #25120 ) ;
#31327=ORIENTED_EDGE ( 'NONE', *, *, #28860, .F. ) ;
#31331=VECTOR ( 'NONE', #26134, 1000.000000000000000 ) ;
#31336=LINE ( 'NONE', #43666, #13582 ) ;
#31338=ORIENTED_EDGE ( 'NONE', *, *, #41917, .F. ) ;
#31340=VERTEX_POINT ( 'NONE', #22747 ) ;
#31341=CARTESIAN_POINT ( 'NONE',  ( -8.393516549646712122, 6.331612867284047041, 455.0000000000000568 ) ) ;
#31344=VERTEX_POINT ( 'NONE', #17434 ) ;
#31349=VECTOR ( 'NONE', #8989, 1000.000000000000114 ) ;
#31351=ORIENTED_EDGE ( 'NONE', *, *, #17978, .F. ) ;
#31352=CARTESIAN_POINT ( 'NONE',  ( 12.00648345035338060, -4.186483450353492231, 455.0000000000000568 ) ) ;
#31356=EDGE_LOOP ( 'NONE', ( #2006, #6075, #30638, #66825 ) ) ;
#31360=ORIENTED_EDGE ( 'NONE', *, *, #3002, .F. ) ;
#31368=CARTESIAN_POINT ( 'NONE',  ( 2.906483450353420928, 11.11351654964658842, 455.0000000000000568 ) ) ;
#31370=PLANE ( 'NONE',  #11649 ) ;
#31375=CARTESIAN_POINT ( 'NONE',  ( 6.006483450353377940, 7.393516549646627745, 195.0000000000000284 ) ) ;
#31385=LINE ( 'NONE', #31724, #10785 ) ;
#31390=ORIENTED_EDGE ( 'NONE', *, *, #57347, .F. ) ;
#31395=DIRECTION ( 'NONE',  ( -1.836970198721029934E-16, 1.836970198721036344E-16, -1.000000000000000000 ) ) ;
#31400=ORIENTED_EDGE ( 'NONE', *, *, #51300, .T. ) ;
#31402=DIRECTION ( 'NONE',  ( -0.000000000000000000, 3.673940397442059868E-16, -1.000000000000000000 ) ) ;
#31405=DIRECTION ( 'NONE',  ( 1.000000000000000000, 0.000000000000000000, 0.000000000000000000 ) ) ;
#31406=DIRECTION ( 'NONE',  ( -1.000000000000000000, 0.000000000000000000, 0.000000000000000000 ) ) ;
#31408=VERTEX_POINT ( 'NONE', #5468 ) ;
#31409=CARTESIAN_POINT ( 'NONE',  ( 4.186483450353423841, 11.99351654964658742, 455.0000000000000568 ) ) ;
#31419=DIRECTION ( 'NONE',  ( 9.799566706031580591E-15, 1.000000000000000000, 1.836970198721018348E-16 ) ) ;
#31421=ORIENTED_EDGE ( 'NONE', *, *, #54841, .F. ) ;
#31427=ORIENTED_EDGE ( 'NONE', *, *, #22280, .F. ) ;
#31438=ORIENTED_EDGE ( 'NONE', *, *, #67789, .F. ) ;
#31442=VECTOR ( 'NONE', #6731, 1000.000000000000000 ) ;
#31451=CARTESIAN_POINT ( 'NONE',  ( 6.006483450353379716, -6.006483450353490738, 455.0000000000000568 ) ) ;
#31455=FACE_OUTER_BOUND ( 'NONE', #30182, .T. ) ;
#31458=EDGE_LOOP ( 'NONE', ( #25927, #40148, #8969, #15816 ) ) ;
#31461=CARTESIAN_POINT ( 'NONE',  ( -10.91351654964680584, -9.306483450353375986, 455.0000000000000568 ) ) ;
#31465=ORIENTED_EDGE ( 'NONE', *, *, #65837, .F. ) ;
#31470=PLANE ( 'NONE',  #61427 ) ;
#31474=VERTEX_POINT ( 'NONE', #29784 ) ;
#31480=FACE_OUTER_BOUND ( 'NONE', #53146, .T. ) ;
#31491=EDGE_CURVE ( 'NONE', #22868, #66424, #24496, .T. ) ;
#31498=ORIENTED_EDGE ( 'NONE', *, *, #26181, .T. ) ;
#31503=AXIS2_PLACEMENT_3D ( 'NONE', #15475, #58604, #63198 ) ;
#31516=CARTESIAN_POINT ( 'NONE',  ( 4.740315990920172418, 7.798499376343941414, 455.0000000000000568 ) ) ;
#31533=DIRECTION ( 'NONE',  ( -0.7071067811865361374, 0.7071067811865588970, 2.810316974849854557E-30 ) ) ;
#31534=ORIENTED_EDGE ( 'NONE', *, *, #55417, .F. ) ;
#31545=VECTOR ( 'NONE', #28765, 1000.000000000000000 ) ;
#31553=CARTESIAN_POINT ( 'NONE',  ( -8.393516549646712122, 5.655420232009161552, 195.0000000000000284 ) ) ;
#31555=EDGE_CURVE ( 'NONE', #51662, #16082, #40993, .T. ) ;
#31560=EDGE_CURVE ( 'NONE', #40309, #47485, #2220, .T. ) ;
#31564=VERTEX_POINT ( 'NONE', #31215 ) ;
#31577=CARTESIAN_POINT ( 'NONE',  ( 6.344579767990805585, 8.393516549646626856, 195.0000000000000284 ) ) ;
#31579=ORIENTED_EDGE ( 'NONE', *, *, #13491, .T. ) ;
#31596=VERTEX_POINT ( 'NONE', #35792 ) ;
#31597=DIRECTION ( 'NONE',  ( -1.920885163218982051E-15, -1.000000000000000000, 0.000000000000000000 ) ) ;
#31599=LINE ( 'NONE', #58818, #67268 ) ;
#31619=VECTOR ( 'NONE', #492, 1000.000000000000000 ) ;
#31625=AXIS2_PLACEMENT_3D ( 'NONE', #14994, #3332, #68740 ) ;
#31643=EDGE_CURVE ( 'NONE', #43706, #42184, #47799, .T. ) ;
#31646=ADVANCED_FACE ( 'NONE', ( #69023 ), #20231, .T. ) ;
#31655=DIRECTION ( 'NONE',  ( -0.000000000000000000, -0.000000000000000000, -1.000000000000000000 ) ) ;
#31659=CIRCLE ( 'NONE', #2258, 0.2000000000000000944 ) ;
#31667=DIRECTION ( 'NONE',  ( -0.7071067811865446862, 0.7071067811865503483, 0.000000000000000000 ) ) ;
#31669=CARTESIAN_POINT ( 'NONE',  ( 9.306483450353418618, 10.91351654964656426, 455.0000000000000568 ) ) ;
#31671=VERTEX_POINT ( 'NONE', #9632 ) ;
#31673=VECTOR ( 'NONE', #52756, 1000.000000000000000 ) ;
#31687=VECTOR ( 'NONE', #20100, 1000.000000000000000 ) ;
#31691=EDGE_LOOP ( 'NONE', ( #35128, #36760, #3782, #21963 ) ) ;
#31701=ORIENTED_EDGE ( 'NONE', *, *, #4546, .T. ) ;
#31702=CARTESIAN_POINT ( 'NONE',  ( 11.32648345035337734, -4.206483450353492692, 455.0000000000000568 ) ) ;
#31706=DIRECTION ( 'NONE',  ( -2.135044278125301343E-15, 1.000000000000000000, 0.000000000000000000 ) ) ;
#31710=CARTESIAN_POINT ( 'NONE',  ( 3.606483450353406450, 7.415254214038213831, 455.0000000000000568 ) ) ;
#31724=CARTESIAN_POINT ( 'NONE',  ( -4.188533722949421723, -7.272650909786664286, 455.0000000000000568 ) ) ;
#31728=DIRECTION ( 'NONE',  ( 1.000000000000000000, 0.000000000000000000, 0.000000000000000000 ) ) ;
#31731=VERTEX_POINT ( 'NONE', #31904 ) ;
#31735=CARTESIAN_POINT ( 'NONE',  ( -7.793516549646827940, -11.12648345035340647, 455.0000000000000568 ) ) ;
#31738=CARTESIAN_POINT ( 'NONE',  ( 4.396432944014529554, 8.393516549646633962, 195.0000000000000284 ) ) ;
#31740=CARTESIAN_POINT ( 'NONE',  ( -5.993516549646711766, 5.993516549646603409, 195.0000000000000284 ) ) ;
#31743=CARTESIAN_POINT ( 'NONE',  ( 7.826483450353380000, -11.78648345035349010, 455.0000000000000568 ) ) ;
#31749=VECTOR ( 'NONE', #14665, 1000.000000000000000 ) ;
#31750=LINE ( 'NONE', #4870, #23108 ) ;
#31755=LINE ( 'NONE', #37403, #3341 ) ;
#31762=ORIENTED_EDGE ( 'NONE', *, *, #37220, .F. ) ;
#31764=LINE ( 'NONE', #58970, #59086 ) ;
#31768=DIRECTION ( 'NONE',  ( 1.836970198721029934E-16, 1.836970198721010706E-16, -1.000000000000000000 ) ) ;
#31773=EDGE_CURVE ( 'NONE', #4905, #48072, #69374, .T. ) ;
#31778=CARTESIAN_POINT ( 'NONE',  ( 10.92648345035337343, -9.306483450353493225, 455.0000000000000568 ) ) ;
#31781=ORIENTED_EDGE ( 'NONE', *, *, #42488, .F. ) ;
#31789=DIRECTION ( 'NONE',  ( -1.000000000000000000, 3.016910393003147986E-15, 1.108394896831706469E-30 ) ) ;
#31792=FACE_OUTER_BOUND ( 'NONE', #62528, .T. ) ;
#31794=CARTESIAN_POINT ( 'NONE',  ( 8.606483450353406894, 7.603567055985405609, 455.0000000000000568 ) ) ;
#31798=CARTESIAN_POINT ( 'NONE',  ( 2.906483450353349429, -10.09643294401453950, 195.0000000000000284 ) ) ;
#31802=DIRECTION ( 'NONE',  ( 0.000000000000000000, 1.000000000000000000, 0.000000000000000000 ) ) ;
#31806=ORIENTED_EDGE ( 'NONE', *, *, #10433, .T. ) ;
#31809=ORIENTED_EDGE ( 'NONE', *, *, #34549, .F. ) ;
#31812=AXIS2_PLACEMENT_3D ( 'NONE', #38169, #20496, #42063 ) ;
#31818=ORIENTED_EDGE ( 'NONE', *, *, #11856, .F. ) ;
#31830=VERTEX_POINT ( 'NONE', #22343 ) ;
#31833=DIRECTION ( 'NONE',  ( 0.7071067811865451302, -0.7071067811865500152, -2.597868168706484048E-16 ) ) ;
#31835=ORIENTED_EDGE ( 'NONE', *, *, #66271, .T. ) ;
#31840=VECTOR ( 'NONE', #10031, 1000.000000000000000 ) ;
#31845=VERTEX_POINT ( 'NONE', #78 ) ;
#31857=AXIS2_PLACEMENT_3D ( 'NONE', #23888, #18575, #40493 ) ;
#31862=LINE ( 'NONE', #32196, #52 ) ;
#31874=LINE ( 'NONE', #5358, #21693 ) ;
#31875=DIRECTION ( 'NONE',  ( 1.000000000000000000, 3.016910393003147986E-15, 1.108394896831706469E-30 ) ) ;
#31898=EDGE_CURVE ( 'NONE', #54850, #43836, #67460, .T. ) ;
#31904=CARTESIAN_POINT ( 'NONE',  ( 7.757955312929553315, 8.452095193409265406, 455.0000000000000568 ) ) ;
#31909=ADVANCED_FACE ( 'NONE', ( #29964 ), #51893, .F. ) ;
#31922=VERTEX_POINT ( 'NONE', #57537 ) ;
#31933=ORIENTED_EDGE ( 'NONE', *, *, #53670, .T. ) ;
#31937=ORIENTED_EDGE ( 'NONE', *, *, #61496, .T. ) ;
#31938=EDGE_CURVE ( 'NONE', #66510, #4435, #9102, .T. ) ;
#31939=VERTEX_POINT ( 'NONE', #65802 ) ;
#31940=CARTESIAN_POINT ( 'NONE',  ( 12.00648345035336284, 7.813516549646607245, 195.0000000000000284 ) ) ;
#31947=ADVANCED_FACE ( 'NONE', ( #13701 ), #49544, .F. ) ;
#31949=ORIENTED_EDGE ( 'NONE', *, *, #40526, .F. ) ;
#31951=CARTESIAN_POINT ( 'NONE',  ( 3.606483450353350051, 4.609516549646638595, 195.0000000000000284 ) ) ;
#31954=DIRECTION ( 'NONE',  ( -1.836970198721029934E-16, 1.836970198721036344E-16, -1.000000000000000000 ) ) ;
#31955=LINE ( 'NONE', #48221, #2977 ) ;
#31958=ORIENTED_EDGE ( 'NONE', *, *, #21816, .F. ) ;
#31961=CARTESIAN_POINT ( 'NONE',  ( -3.593516549646712299, 4.609516549646604844, 455.0000000000000568 ) ) ;
#31970=CARTESIAN_POINT ( 'NONE',  ( -2.693516549646675529, 10.91351654964657314, 455.0000000000000568 ) ) ;
#31974=ORIENTED_EDGE ( 'NONE', *, *, #56460, .T. ) ;
#31978=VECTOR ( 'NONE', #21248, 1000.000000000000000 ) ;
#31981=CARTESIAN_POINT ( 'NONE',  ( 11.78648345035337819, -4.186483450353492231, 455.0000000000000568 ) ) ;
#31984=ORIENTED_EDGE ( 'NONE', *, *, #22319, .F. ) ;
#31986=CARTESIAN_POINT ( 'NONE',  ( 8.406483450353398723, 5.655420232009111814, 455.0000000000000568 ) ) ;
#32001=FACE_OUTER_BOUND ( 'NONE', #57243, .T. ) ;
#32004=VECTOR ( 'NONE', #50162, 1000.000000000000000 ) ;
#32016=CIRCLE ( 'NONE', #3735, 0.3999999999999993006 ) ;
#32018=EDGE_LOOP ( 'NONE', ( #34918, #64000, #366, #27527 ) ) ;
#32022=ORIENTED_EDGE ( 'NONE', *, *, #53461, .T. ) ;
#32023=DIRECTION ( 'NONE',  ( 0.5000000000000004441, -0.8660254037844383745, 0.000000000000000000 ) ) ;
#32039=ORIENTED_EDGE ( 'NONE', *, *, #26741, .F. ) ;
#32047=CARTESIAN_POINT ( 'NONE',  ( -10.73351654964669599, -1.690483450353341910, 455.0000000000000568 ) ) ;
#32049=DIRECTION ( 'NONE',  ( -0.000000000000000000, -0.000000000000000000, -1.000000000000000000 ) ) ;
#32077=CARTESIAN_POINT ( 'NONE',  ( -1.677516549646826061, -10.74648345035347141, 455.0000000000000568 ) ) ;
#32091=DIRECTION ( 'NONE',  ( 1.067128122525083795E-14, 1.000000000000000000, 0.000000000000000000 ) ) ;
#32097=DIRECTION ( 'NONE',  ( 0.000000000000000000, 3.673940397442059868E-16, -1.000000000000000000 ) ) ;
#32105=ORIENTED_EDGE ( 'NONE', *, *, #69540, .F. ) ;
#32109=LINE ( 'NONE', #15514, #33497 ) ;
#32112=VERTEX_POINT ( 'NONE', #42675 ) ;
#32114=CARTESIAN_POINT ( 'NONE',  ( -8.452095193409402185, 7.744988412222746810, 455.0000000000000568 ) ) ;
#32115=ADVANCED_FACE ( 'NONE', ( #59972 ), #54340, .F. ) ;
#32119=ADVANCED_FACE ( 'NONE', ( #27458 ), #53995, .F. ) ;
#32131=CARTESIAN_POINT ( 'NONE',  ( 11.32648345035335780, 7.593516549646611047, 195.0000000000000284 ) ) ;
#32133=FACE_OUTER_BOUND ( 'NONE', #51630, .T. ) ;
#32134=LINE ( 'NONE', #20820, #66094 ) ;
#32138=VECTOR ( 'NONE', #29700, 1000.000000000000000 ) ;
#32160=CIRCLE ( 'NONE', #44594, 0.3999999999999993006 ) ;
#32165=ORIENTED_EDGE ( 'NONE', *, *, #68472, .F. ) ;
#32166=ORIENTED_EDGE ( 'NONE', *, *, #21260, .F. ) ;
#32168=ORIENTED_EDGE ( 'NONE', *, *, #49203, .F. ) ;
#32177=LINE ( 'NONE', #54785, #7453 ) ;
#32179=CYLINDRICAL_SURFACE ( 'NONE', #61546, 1.399999999999999245 ) ;
#32190=CARTESIAN_POINT ( 'NONE',  ( 6.006483450353401921, 5.993516549646582092, 455.0000000000000568 ) ) ;
#32191=VECTOR ( 'NONE', #21719, 1000.000000000000000 ) ;
#32196=CARTESIAN_POINT ( 'NONE',  ( 9.247904806590689475, -9.955011587777349291, 455.0000000000000568 ) ) ;
#32198=EDGE_LOOP ( 'NONE', ( #1509, #49973, #44838, #68640 ) ) ;
#32201=EDGE_CURVE ( 'NONE', #7017, #44833, #27809, .T. ) ;
#32202=PLANE ( 'NONE',  #9790 ) ;
#32208=ORIENTED_EDGE ( 'NONE', *, *, #52625, .T. ) ;
#32211=VECTOR ( 'NONE', #35447, 1000.000000000000000 ) ;
#32212=LINE ( 'NONE', #53790, #58939 ) ;
#32215=CARTESIAN_POINT ( 'NONE',  ( -2.693516549646682190, 10.08346604330774454, 455.0000000000000568 ) ) ;
#32219=CARTESIAN_POINT ( 'NONE',  ( -11.31351654964674047, -7.606483450353325182, 195.0000000000000284 ) ) ;
#32223=CARTESIAN_POINT ( 'NONE',  ( -4.609516549646752281, -3.606483450353441533, 455.0000000000000568 ) ) ;
#32230=ORIENTED_EDGE ( 'NONE', *, *, #38429, .T. ) ;
#32236=ORIENTED_EDGE ( 'NONE', *, *, #40375, .T. ) ;
#32241=EDGE_CURVE ( 'NONE', #31340, #57095, #36066, .T. ) ;
#32242=DIRECTION ( 'NONE',  ( 0.7671651518153065341, 0.6414496315691495809, -0.000000000000000000 ) ) ;
#32248=ORIENTED_EDGE ( 'NONE', *, *, #37008, .F. ) ;
#32255=DIRECTION ( 'NONE',  ( -3.540573132209558464E-15, -1.000000000000000000, 0.000000000000000000 ) ) ;
#32262=VERTEX_POINT ( 'NONE', #16507 ) ;
#32273=DIRECTION ( 'NONE',  ( 0.7671651518152998728, -0.6414496315691575745, 2.309356642088859447E-17 ) ) ;
#32274=ORIENTED_EDGE ( 'NONE', *, *, #21260, .T. ) ;
#32279=DIRECTION ( 'NONE',  ( -1.836970198721029934E-16, 1.836970198721036344E-16, -1.000000000000000000 ) ) ;
#32280=LINE ( 'NONE', #59147, #16458 ) ;
#32283=DIRECTION ( 'NONE',  ( -1.000000000000000000, 1.920885163218982051E-15, 1.836970198721033385E-16 ) ) ;
#32288=ADVANCED_FACE ( 'NONE', ( #66330 ), #56062, .F. ) ;
#32289=CARTESIAN_POINT ( 'NONE',  ( 7.806483450353418618, 11.31351654964657172, 455.0000000000000568 ) ) ;
#32294=ORIENTED_EDGE ( 'NONE', *, *, #36682, .T. ) ;
#32303=VECTOR ( 'NONE', #10630, 1000.000000000000000 ) ;
#32306=FACE_BOUND ( 'NONE', #44162, .T. ) ;
#32312=LINE ( 'NONE', #4406, #68651 ) ;
#32336=FACE_OUTER_BOUND ( 'NONE', #37076, .T. ) ;
#32338=CARTESIAN_POINT ( 'NONE',  ( -10.19191654964671301, 11.47551654964660450, 455.0000000000000568 ) ) ;
#32346=CARTESIAN_POINT ( 'NONE',  ( 7.826483450353380000, -12.00648345035349251, 455.0000000000000568 ) ) ;
#32348=VECTOR ( 'NONE', #39022, 1000.000000000000000 ) ;
#32353=CARTESIAN_POINT ( 'NONE',  ( -2.893516549646782732, -11.12648345035340647, 195.0000000000000284 ) ) ;
#32355=DIRECTION ( 'NONE',  ( 1.000000000000000000, 0.000000000000000000, 0.000000000000000000 ) ) ;
#32356=AXIS2_PLACEMENT_3D ( 'NONE', #22034, #64824, #27346 ) ;
#32360=ORIENTED_EDGE ( 'NONE', *, *, #14975, .F. ) ;
#32362=PLANE ( 'NONE',  #39555 ) ;
#32367=ORIENTED_EDGE ( 'NONE', *, *, #59901, .F. ) ;
#32374=UNCERTAINTY_MEASURE_WITH_UNIT (LENGTH_MEASURE( 1.000000000000000082E-05 ), #37190, 'distance_accuracy_value', 'NONE');
#32377=EDGE_CURVE ( 'NONE', #62134, #29982, #58749, .T. ) ;
#32385=EDGE_CURVE ( 'NONE', #60382, #17661, #47426, .T. ) ;
#32389=ORIENTED_EDGE ( 'NONE', *, *, #51972, .T. ) ;
#32393=CARTESIAN_POINT ( 'NONE',  ( 9.306483450353379538, -10.09643294401465852, 455.0000000000000568 ) ) ;
#32415=ORIENTED_EDGE ( 'NONE', *, *, #26224, .F. ) ;
#32416=LINE ( 'NONE', #26408, #63757 ) ;
#32418=FACE_OUTER_BOUND ( 'NONE', #16674, .T. ) ;
#32419=EDGE_CURVE ( 'NONE', #31147, #47898, #15832, .T. ) ;
#32424=VERTEX_POINT ( 'NONE', #36237 ) ;
#32425=EDGE_CURVE ( 'NONE', #51349, #14532, #40655, .T. ) ;
#32430=ORIENTED_EDGE ( 'NONE', *, *, #42968, .F. ) ;
#32437=ORIENTED_EDGE ( 'NONE', *, *, #24208, .F. ) ;
#32440=PLANE ( 'NONE',  #8040 ) ;
#32451=CARTESIAN_POINT ( 'NONE',  ( 2.906483450353342324, -11.12648345035346331, 455.0000000000000568 ) ) ;
#32456=ORIENTED_EDGE ( 'NONE', *, *, #16335, .F. ) ;
#32458=AXIS2_PLACEMENT_3D ( 'NONE', #65272, #15771, #5861 ) ;
#32460=CARTESIAN_POINT ( 'NONE',  ( 2.906483450353343656, -10.92648345035346402, 455.0000000000000568 ) ) ;
#32470=LINE ( 'NONE', #21160, #13152 ) ;
#32476=EDGE_CURVE ( 'NONE', #33832, #53367, #57804, .T. ) ;
#32491=DIRECTION ( 'NONE',  ( 0.000000000000000000, 1.000000000000000000, 0.000000000000000000 ) ) ;
#32492=DIRECTION ( 'NONE',  ( -1.047444401652940007E-14, -1.000000000000000000, -1.836970198721029934E-16 ) ) ;
#32495=DIRECTION ( 'NONE',  ( -0.000000000000000000, -0.000000000000000000, -1.000000000000000000 ) ) ;
#32503=DIRECTION ( 'NONE',  ( 0.000000000000000000, 3.673940397442059868E-16, -1.000000000000000000 ) ) ;
#32505=PLANE ( 'NONE',  #62553 ) ;
#32511=ORIENTED_EDGE ( 'NONE', *, *, #23176, .T. ) ;
#32513=DIRECTION ( 'NONE',  ( -1.000000000000000000, 0.000000000000000000, 0.000000000000000000 ) ) ;
#32517=ORIENTED_EDGE ( 'NONE', *, *, #49405, .F. ) ;
#32519=CARTESIAN_POINT ( 'NONE',  ( -4.193516549646675529, 11.11351654964658842, 195.0000000000000284 ) ) ;
#32521=VECTOR ( 'NONE', #56766, 1000.000000000000114 ) ;
#32526=EDGE_LOOP ( 'NONE', ( #32456, #46034, #6342, #37877 ) ) ;
#32528=ORIENTED_EDGE ( 'NONE', *, *, #2571, .F. ) ;
#32532=ORIENTED_EDGE ( 'NONE', *, *, #4683, .F. ) ;
#32535=CARTESIAN_POINT ( 'NONE',  ( 8.406483450353379183, -5.668387132716048882, 455.0000000000000568 ) ) ;
#32561=EDGE_CURVE ( 'NONE', #59963, #7366, #49970, .T. ) ;
#32568=ORIENTED_EDGE ( 'NONE', *, *, #8638, .F. ) ;
#32569=EDGE_CURVE ( 'NONE', #28387, #14058, #5479, .T. ) ;
#32571=VECTOR ( 'NONE', #13020, 1000.000000000000000 ) ;
#32581=EDGE_LOOP ( 'NONE', ( #57132, #4608, #7895, #3670 ) ) ;
#32587=DIRECTION ( 'NONE',  ( -8.673617379884087537E-15, -1.000000000000000000, 0.000000000000000000 ) ) ;
#32598=CARTESIAN_POINT ( 'NONE',  ( 6.619341603356837744, -4.747751991980742936, 455.0000000000000568 ) ) ;
#32603=EDGE_CURVE ( 'NONE', #44836, #46298, #42941, .T. ) ;
#32610=DIRECTION ( 'NONE',  ( -1.836970198721029934E-16, 1.836970198721036344E-16, -1.000000000000000000 ) ) ;
#32612=EDGE_CURVE ( 'NONE', #33806, #23316, #27034, .T. ) ;
#32613=PLANE ( 'NONE',  #59056 ) ;
#32620=ORIENTED_EDGE ( 'NONE', *, *, #53279, .F. ) ;
#32625=DIRECTION ( 'NONE',  ( -1.000000000000000000, 0.000000000000000000, 0.000000000000000000 ) ) ;
#32626=ORIENTED_EDGE ( 'NONE', *, *, #14123, .F. ) ;
#32629=CARTESIAN_POINT ( 'NONE',  ( -11.11351654964671098, 7.793516549646603231, 455.0000000000000568 ) ) ;
#32635=DIRECTION ( 'NONE',  ( 0.000000000000000000, -3.673940397442059868E-16, 1.000000000000000000 ) ) ;
#32637=DIRECTION ( 'NONE',  ( -3.491481338843133355E-15, -1.000000000000000000, -1.836970198721029934E-16 ) ) ;
#32638=DIRECTION ( 'NONE',  ( 1.836970198721029934E-16, 1.836970198721010706E-16, -1.000000000000000000 ) ) ;
#32643=ADVANCED_FACE ( 'NONE', ( #33714 ), #53919, .F. ) ;
#32646=DIRECTION ( 'NONE',  ( 1.000000000000000000, 0.000000000000000000, 0.000000000000000000 ) ) ;
#32647=LINE ( 'NONE', #1492, #13157 ) ;
#32652=DIRECTION ( 'NONE',  ( -1.836970198721029934E-16, 1.836970198721036344E-16, -1.000000000000000000 ) ) ;
#32658=AXIS2_PLACEMENT_3D ( 'NONE', #1496, #23765, #33341 ) ;
#32659=DIRECTION ( 'NONE',  ( 0.7071067811865550112, 0.7071067811865401342, 2.597868168706466299E-16 ) ) ;
#32660=EDGE_LOOP ( 'NONE', ( #64661, #60933, #21814, #21312 ) ) ;
#32662=PLANE ( 'NONE',  #42677 ) ;
#32665=ORIENTED_EDGE ( 'NONE', *, *, #31239, .F. ) ;
#32667=CARTESIAN_POINT ( 'NONE',  ( -11.31351654964671027, 7.593516549646603941, 455.0000000000000568 ) ) ;
#32671=VERTEX_POINT ( 'NONE', #43975 ) ;
#32675=CARTESIAN_POINT ( 'NONE',  ( -4.383466043307859827, 8.393516549646591329, 195.0000000000000284 ) ) ;
#32681=EDGE_CURVE ( 'NONE', #43112, #15685, #68886, .T. ) ;
#32688=LINE ( 'NONE', #518, #68029 ) ;
#32693=EDGE_CURVE ( 'NONE', #4940, #20447, #7174, .T. ) ;
#32701=VERTEX_POINT ( 'NONE', #28748 ) ;
#32702=EDGE_LOOP ( 'NONE', ( #60621, #28715, #58443, #32511 ) ) ;
#32709=ORIENTED_EDGE ( 'NONE', *, *, #15986, .F. ) ;
#32715=CARTESIAN_POINT ( 'NONE',  ( 11.32648345035337734, -4.406483450353491982, 455.0000000000000568 ) ) ;
#32717=ORIENTED_EDGE ( 'NONE', *, *, #10358, .F. ) ;
#32728=DIRECTION ( 'NONE',  ( 1.000000000000000000, 0.000000000000000000, 0.000000000000000000 ) ) ;
#32730=EDGE_CURVE ( 'NONE', #5474, #33142, #7873, .T. ) ;
#32733=CARTESIAN_POINT ( 'NONE',  ( -2.693516549646675529, 10.91351654964657314, 455.0000000000000568 ) ) ;
#32734=VECTOR ( 'NONE', #16427, 1000.000000000000000 ) ;
#32735=CARTESIAN_POINT ( 'NONE',  ( 9.955011587777235604, -9.247904806590801385, 455.0000000000000568 ) ) ;
#32741=EDGE_CURVE ( 'NONE', #52360, #68006, #12366, .T. ) ;
#32742=LINE ( 'NONE', #38737, #27417 ) ;
#32753=CARTESIAN_POINT ( 'NONE',  ( 7.806483450353379538, -11.32648345035348925, 455.0000000000000568 ) ) ;
#32761=DIRECTION ( 'NONE',  ( -0.000000000000000000, -0.000000000000000000, -1.000000000000000000 ) ) ;
#32772=ORIENTED_EDGE ( 'NONE', *, *, #53464, .F. ) ;
#32781=LINE ( 'NONE', #55061, #16413 ) ;
#32788=CARTESIAN_POINT ( 'NONE',  ( 7.272650909786644746, 7.798499376343933420, 455.0000000000000568 ) ) ;
#32792=DIRECTION ( 'NONE',  ( -1.000000000000000000, 8.540177112501197482E-15, 3.137610169492823463E-30 ) ) ;
#32800=VECTOR ( 'NONE', #118, 1000.000000000000000 ) ;
#32803=CARTESIAN_POINT ( 'NONE',  ( -5.993516549646776603, -6.006483450353426790, 455.0000000000000568 ) ) ;
#32806=ORIENTED_EDGE ( 'NONE', *, *, #46210, .F. ) ;
#32808=ADVANCED_FACE ( 'NONE', ( #13537 ), #13888, .F. ) ;
#32822=CARTESIAN_POINT ( 'NONE',  ( -4.193516549646831848, -11.12648345035344377, 455.0000000000000568 ) ) ;
#32823=ORIENTED_EDGE ( 'NONE', *, *, #58008, .F. ) ;
#32827=EDGE_CURVE ( 'NONE', #354, #8396, #20941, .T. ) ;
#32833=CARTESIAN_POINT ( 'NONE',  ( 7.428221114745003462, -3.606483450353489939, 455.0000000000000568 ) ) ;
#32844=AXIS2_PLACEMENT_3D ( 'NONE', #6376, #12338, #6702 ) ;
#32849=CARTESIAN_POINT ( 'NONE',  ( -11.77351654964670935, 4.393516549646602876, 455.0000000000000568 ) ) ;
#32859=FACE_OUTER_BOUND ( 'NONE', #61082, .T. ) ;
#32863=VERTEX_POINT ( 'NONE', #68701 ) ;
#32870=CIRCLE ( 'NONE', #12503, 0.2000000000000005107 ) ;
#32874=EDGE_LOOP ( 'NONE', ( #9265, #34514, #27402, #61283 ) ) ;
#32876=ORIENTED_EDGE ( 'NONE', *, *, #43622, .F. ) ;
#32877=EDGE_LOOP ( 'NONE', ( #6361, #60927, #48184, #55102, #24444, #37628, #48093, #65203, #15392, #37666, #47098, #2169, #68026, #39859, #47475, #4964, #1449, #36800, #48677, #5085, #462, #21533, #55141, #51684, #46271, #68077, #18082, #33880, #6312, #600, #15948, #46135, #53687, #25769, #28179, #36543, #61276, #39268, #36050, #33116, #24140, #67516, #13839, #49841, #20961, #49135, #25485, #17521, #41321, #58359, #65058, #3654, #6614, #26231, #410, #69393, #63219, #19024, #10701, #55990, #60600, #33788, #68225, #58075, #67616, #12071, #59516, #799, #20894, #12438, #28331, #19724, #6815, #43305, #21369, #48916, #50822, #16046, #35796, #3986, #32389, #33398, #29635, #1935, #58751, #6817, #22861, #46994, #27478, #63645, #13992, #51241, #49542, #48138, #58178, #39350, #25645, #7527, #50881, #49434, #9760, #17902, #14172, #63157, #15038, #33679, #6544, #43186, #9152, #65552, #61887, #64639, #48355, #53550, #27299, #25699, #51543, #45542, #17554, #19791, #32022, #5499, #34418, #293, #56749, #35833, #49995, #54986, #66140, #60637, #33403, #14024, #29611, #23582, #58948, #13559, #20359, #7894, #11674, #1884, #60838, #40772, #1223, #39802, #37149, #39942, #15315, #38529, #26622, #32230, #32958, #45912, #22171, #44225, #5723, #29818, #31579, #241, #58335, #52031, #48375, #41846, #36433, #62016, #33694, #62667, #15659, #62621, #29899, #24838, #30497, #46085, #68172, #12259, #33343, #2306, #43924, #55808, #44560, #15575, #58975, #52976, #61268, #43544, #59220, #51044, #66762, #39925, #31937, #47233, #61938, #17649, #59393, #62055, #52927, #23706, #41572, #41489, #47576, #38677, #51780, #58688, #9726, #13912, #14213, #18412, #19355, #64305, #30842, #60012, #20522, #47943, #54370, #49242 ) ) ;
#32884=DIRECTION ( 'NONE',  ( -3.491481338843132961E-15, -1.000000000000000000, 0.000000000000000000 ) ) ;
#32885=CARTESIAN_POINT ( 'NONE',  ( 10.09643294401454661, -2.906483450353395614, 195.0000000000000284 ) ) ;
#32887=CARTESIAN_POINT ( 'NONE',  ( 11.19368345035335821, 11.18071654964659523, 195.0000000000000284 ) ) ;
#32891=ORIENTED_EDGE ( 'NONE', *, *, #3609, .T. ) ;
#32892=EDGE_CURVE ( 'NONE', #47649, #14243, #15653, .T. ) ;
#32898=CARTESIAN_POINT ( 'NONE',  ( 10.74648345035338082, -1.090483450353491035, 455.0000000000000568 ) ) ;
#32913=VECTOR ( 'NONE', #26953, 1000.000000000000000 ) ;
#32914=CARTESIAN_POINT ( 'NONE',  ( -9.293516549646817282, -10.09643294401455904, 455.0000000000000568 ) ) ;
#32917=VERTEX_POINT ( 'NONE', #25205 ) ;
#32947=LINE ( 'NONE', #44235, #41670 ) ;
#32948=DIRECTION ( 'NONE',  ( 1.836970198721029934E-16, 1.836970198721010706E-16, -1.000000000000000000 ) ) ;
#32958=ORIENTED_EDGE ( 'NONE', *, *, #55674, .T. ) ;
#32972=ORIENTED_EDGE ( 'NONE', *, *, #60355, .F. ) ;
#32984=DIRECTION ( 'NONE',  ( -1.836970198721029934E-16, 1.836970198721036344E-16, -1.000000000000000000 ) ) ;
#32985=LINE ( 'NONE', #65184, #53253 ) ;
#32986=EDGE_CURVE ( 'NONE', #20073, #144, #53486, .T. ) ;
#33003=LINE ( 'NONE', #54580, #13721 ) ;
#33004=DIRECTION ( 'NONE',  ( -1.000000000000000000, 1.047444401652939849E-14, 0.000000000000000000 ) ) ;
#33012=ORIENTED_EDGE ( 'NONE', *, *, #65745, .T. ) ;
#33020=CARTESIAN_POINT ( 'NONE',  ( 11.32648345035337734, -4.206483450353396769, 195.0000000000000284 ) ) ;
#33024=ORIENTED_EDGE ( 'NONE', *, *, #10333, .F. ) ;
#33030=ORIENTED_EDGE ( 'NONE', *, *, #42189, .T. ) ;
#33031=EDGE_CURVE ( 'NONE', #14864, #50893, #59478, .T. ) ;
#33033=FACE_OUTER_BOUND ( 'NONE', #2537, .T. ) ;
#33037=EDGE_CURVE ( 'NONE', #47485, #31671, #20749, .T. ) ;
#33046=VERTEX_POINT ( 'NONE', #59128 ) ;
#33062=VECTOR ( 'NONE', #17869, 1000.000000000000000 ) ;
#33072=DIRECTION ( 'NONE',  ( 1.836970198721029934E-16, -1.836970198721036344E-16, 1.000000000000000000 ) ) ;
#33084=VECTOR ( 'NONE', #45411, 1000.000000000000000 ) ;
#33086=ADVANCED_FACE ( 'NONE', ( #35012 ), #39960, .F. ) ;
#33087=FACE_OUTER_BOUND ( 'NONE', #60724, .T. ) ;
#33091=VECTOR ( 'NONE', #55482, 1000.000000000000000 ) ;
#33093=DIRECTION ( 'NONE',  ( 0.000000000000000000, -1.000000000000000000, 0.000000000000000000 ) ) ;
#33094=EDGE_LOOP ( 'NONE', ( #62057, #37563, #52176, #46092 ) ) ;
#33101=AXIS2_PLACEMENT_3D ( 'NONE', #89, #49221, #32255 ) ;
#33110=EDGE_CURVE ( 'NONE', #43306, #15138, #61527, .T. ) ;
#33111=CARTESIAN_POINT ( 'NONE',  ( -10.91351654964670637, 2.693516549646604030, 455.0000000000000568 ) ) ;
#33116=ORIENTED_EDGE ( 'NONE', *, *, #60529, .T. ) ;
#33119=DIRECTION ( 'NONE',  ( -0.000000000000000000, 3.673940397442059868E-16, -1.000000000000000000 ) ) ;
#33129=EDGE_CURVE ( 'NONE', #60174, #13060, #13454, .T. ) ;
#33141=PLANE ( 'NONE',  #16631 ) ;
#33142=VERTEX_POINT ( 'NONE', #66843 ) ;
#33148=LINE ( 'NONE', #17918, #42150 ) ;
#33154=FACE_OUTER_BOUND ( 'NONE', #26638, .T. ) ;
#33156=EDGE_CURVE ( 'NONE', #6256, #13195, #50930, .T. ) ;
#33165=CARTESIAN_POINT ( 'NONE',  ( 11.12648345035337982, -7.806483450353490561, 455.0000000000000568 ) ) ;
#33166=FACE_OUTER_BOUND ( 'NONE', #12580, .T. ) ;
#33168=EDGE_CURVE ( 'NONE', #191, #28622, #12394, .T. ) ;
#33170=CYLINDRICAL_SURFACE ( 'NONE', #8703, 2.204799999999997429 ) ;
#33177=EDGE_CURVE ( 'NONE', #23727, #24032, #67197, .T. ) ;
#33186=DIRECTION ( 'NONE',  ( 0.7071067811865435759, -0.7071067811865515695, -2.597868168706494402E-16 ) ) ;
#33191=ADVANCED_FACE ( 'NONE', ( #23376 ), #28323, .F. ) ;
#33211=DIRECTION ( 'NONE',  ( 1.836970198721029934E-16, 1.836970198721010706E-16, -1.000000000000000000 ) ) ;
#33222=DIRECTION ( 'NONE',  ( -0.000000000000000000, -0.000000000000000000, -1.000000000000000000 ) ) ;
#33223=ORIENTED_EDGE ( 'NONE', *, *, #29943, .T. ) ;
#33238=EDGE_CURVE ( 'NONE', #35699, #3732, #9923, .T. ) ;
#33248=DIRECTION ( 'NONE',  ( -0.7671651518153065341, -0.6414496315691495809, -2.356647714346224881E-16 ) ) ;
#33258=LINE ( 'NONE', #49520, #2879 ) ;
#33265=CYLINDRICAL_SURFACE ( 'NONE', #55009, 0.8128000000000145109 ) ;
#33269=ORIENTED_EDGE ( 'NONE', *, *, #356, .F. ) ;
#33270=LINE ( 'NONE', #54500, #19573 ) ;
#33273=CARTESIAN_POINT ( 'NONE',  ( -3.593516549646762481, -4.622483450353452206, 455.0000000000000568 ) ) ;
#33281=VERTEX_POINT ( 'NONE', #20168 ) ;
#33287=DIRECTION ( 'NONE',  ( -1.000000000000000000, 1.130039751537441866E-14, 0.000000000000000000 ) ) ;
#33294=FACE_OUTER_BOUND ( 'NONE', #53920, .T. ) ;
#33297=EDGE_CURVE ( 'NONE', #44963, #50749, #63664, .T. ) ;
#33299=CARTESIAN_POINT ( 'NONE',  ( -7.813516549646711162, 11.77351654964660277, 455.0000000000000568 ) ) ;
#33300=LINE ( 'NONE', #49560, #10849 ) ;
#33303=DIRECTION ( 'NONE',  ( 0.000000000000000000, 0.000000000000000000, 1.000000000000000000 ) ) ;
#33308=DIRECTION ( 'NONE',  ( -1.836970198721029934E-16, 1.836970198721036344E-16, -1.000000000000000000 ) ) ;
#33312=VECTOR ( 'NONE', #8416, 1000.000000000000000 ) ;
#33315=ORIENTED_EDGE ( 'NONE', *, *, #48728, .F. ) ;
#33316=VERTEX_POINT ( 'NONE', #3207 ) ;
#33318=CARTESIAN_POINT ( 'NONE',  ( -9.093516549646711411, 10.91351654964659978, 455.0000000000000568 ) ) ;
#33320=EDGE_LOOP ( 'NONE', ( #37943, #12901, #66921, #53062 ) ) ;
#33331=VERTEX_POINT ( 'NONE', #20513 ) ;
#33335=CARTESIAN_POINT ( 'NONE',  ( -11.11351654964670743, 9.093516549646603053, 455.0000000000000568 ) ) ;
#33337=CARTESIAN_POINT ( 'NONE',  ( -7.798499376344067535, 4.727349090213368576, 455.0000000000000568 ) ) ;
#33338=DIRECTION ( 'NONE',  ( -0.000000000000000000, -0.000000000000000000, -1.000000000000000000 ) ) ;
#33339=EDGE_CURVE ( 'NONE', #60888, #15307, #47386, .T. ) ;
#33341=DIRECTION ( 'NONE',  ( -0.5000000000000004441, 0.8660254037844382635, 0.000000000000000000 ) ) ;
#33343=ORIENTED_EDGE ( 'NONE', *, *, #65103, .T. ) ;
#33344=DIRECTION ( 'NONE',  ( -0.7071067811865486830, -0.7071067811865464625, -2.597868168706476160E-16 ) ) ;
#33351=ORIENTED_EDGE ( 'NONE', *, *, #57895, .T. ) ;
#33354=CARTESIAN_POINT ( 'NONE',  ( -8.198316549646774476, -6.006483450353403697, 455.0000000000000568 ) ) ;
#33362=CARTESIAN_POINT ( 'NONE',  ( -11.31351654964670850, 7.793516549646603231, 195.0000000000000284 ) ) ;
#33368=CARTESIAN_POINT ( 'NONE',  ( -1.677516549646683730, 9.828310488885911411, 195.0000000000000284 ) ) ;
#33374=ORIENTED_EDGE ( 'NONE', *, *, #66758, .T. ) ;
#33377=PLANE ( 'NONE',  #30106 ) ;
#33383=CARTESIAN_POINT ( 'NONE',  ( -9.942044687070573872, -2.765062094116047309, 455.0000000000000568 ) ) ;
#33389=CARTESIAN_POINT ( 'NONE',  ( -11.99351654964683078, -11.19368345035334933, 455.0000000000000568 ) ) ;
#33391=ADVANCED_FACE ( 'NONE', ( #21904 ), #43822, .F. ) ;
#33392=LINE ( 'NONE', #15742, #52397 ) ;
#33393=CARTESIAN_POINT ( 'NONE',  ( 7.806483450353379538, -11.12648345035348996, 455.0000000000000568 ) ) ;
#33398=ORIENTED_EDGE ( 'NONE', *, *, #66314, .T. ) ;
#33403=ORIENTED_EDGE ( 'NONE', *, *, #69062, .T. ) ;
#33408=EDGE_LOOP ( 'NONE', ( #54381, #59831, #28822, #60421 ) ) ;
#33413=DIRECTION ( 'NONE',  ( -1.000000000000000000, 0.000000000000000000, 0.000000000000000000 ) ) ;
#33415=ORIENTED_EDGE ( 'NONE', *, *, #26431, .T. ) ;
#33426=VERTEX_POINT ( 'NONE', #16618 ) ;
#33432=DIRECTION ( 'NONE',  ( 4.336808689942043768E-15, 1.000000000000000000, 0.000000000000000000 ) ) ;
#33442=LINE ( 'NONE', #43344, #68086 ) ;
#33443=CARTESIAN_POINT ( 'NONE',  ( -5.098491296477297929, 7.878491296477155181, 195.0000000000000284 ) ) ;
#33445=EDGE_LOOP ( 'NONE', ( #21276, #47235, #59030, #48197 ) ) ;
#33450=DIRECTION ( 'NONE',  ( 0.000000000000000000, -3.673940397442059868E-16, 1.000000000000000000 ) ) ;
#33455=AXIS2_PLACEMENT_3D ( 'NONE', #32190, #22288, #59061 ) ;
#33461=CIRCLE ( 'NONE', #42505, 2.204799999999997429 ) ;
#33463=ORIENTED_EDGE ( 'NONE', *, *, #22335, .T. ) ;
#33467=CARTESIAN_POINT ( 'NONE',  ( -5.993516549646711766, 5.993516549646603409, 455.0000000000000568 ) ) ;
#33469=ORIENTED_EDGE ( 'NONE', *, *, #65185, .F. ) ;
#33472=FACE_OUTER_BOUND ( 'NONE', #19905, .T. ) ;
#33490=AXIS2_PLACEMENT_3D ( 'NONE', #50325, #45358, #34752 ) ;
#33497=VECTOR ( 'NONE', #38128, 1000.000000000000000 ) ;
#33514=DIRECTION ( 'NONE',  ( -1.000000000000000000, 7.304098846218132892E-15, 0.000000000000000000 ) ) ;
#33515=CARTESIAN_POINT ( 'NONE',  ( -11.31351654964674402, -4.406483450353330333, 455.0000000000000568 ) ) ;
#33518=AXIS2_PLACEMENT_3D ( 'NONE', #20551, #36833, #58401 ) ;
#33526=DIRECTION ( 'NONE',  ( -0.000000000000000000, -0.000000000000000000, -1.000000000000000000 ) ) ;
#33527=DIRECTION ( 'NONE',  ( 0.7071067811865500152, 0.7071067811865451302, -4.683861624749757595E-31 ) ) ;
#33528=CARTESIAN_POINT ( 'NONE',  ( 4.740315990920173306, 7.798499376343941414, 455.0000000000000568 ) ) ;
#33538=AXIS2_PLACEMENT_3D ( 'NONE', #33165, #1006, #21864 ) ;
#33551=ADVANCED_FACE ( 'NONE', ( #8052 ), #22601, .F. ) ;
#33554=AXIS2_PLACEMENT_3D ( 'NONE', #4132, #58212, #37013 ) ;
#33562=ORIENTED_EDGE ( 'NONE', *, *, #52399, .T. ) ;
#33578=ORIENTED_EDGE ( 'NONE', *, *, #33770, .T. ) ;
#33589=CARTESIAN_POINT ( 'NONE',  ( -8.393516549646697911, -4.396432944014502020, 195.0000000000000284 ) ) ;
#33590=DIRECTION ( 'NONE',  ( -1.836970198721029934E-16, 1.836970198721036344E-16, -1.000000000000000000 ) ) ;
#33592=VECTOR ( 'NONE', #67505, 1000.000000000000114 ) ;
#33614=CARTESIAN_POINT ( 'NONE',  ( 4.201500623656052369, 4.727349090213339267, 455.0000000000000568 ) ) ;
#33615=CARTESIAN_POINT ( 'NONE',  ( -11.99351654964671354, 11.18071654964658990, 195.0000000000000284 ) ) ;
#33618=AXIS2_PLACEMENT_3D ( 'NONE', #4135, #20383, #30298 ) ;
#33625=DIRECTION ( 'NONE',  ( 0.000000000000000000, 0.000000000000000000, 1.000000000000000000 ) ) ;
#33631=VERTEX_POINT ( 'NONE', #2412 ) ;
#33632=ORIENTED_EDGE ( 'NONE', *, *, #2972, .T. ) ;
#33646=VERTEX_POINT ( 'NONE', #41994 ) ;
#33649=ADVANCED_FACE ( 'NONE', ( #57206 ), #24687, .F. ) ;
#33652=DIRECTION ( 'NONE',  ( -1.000000000000000000, -3.016910393003147986E-15, 0.000000000000000000 ) ) ;
#33659=LINE ( 'NONE', #40349, #39054 ) ;
#33662=CARTESIAN_POINT ( 'NONE',  ( -9.942044687070573872, -2.765062094116046865, 455.0000000000000568 ) ) ;
#33679=ORIENTED_EDGE ( 'NONE', *, *, #69936, .T. ) ;
#33686=ADVANCED_FACE ( 'NONE', ( #31039 ), #62863, .F. ) ;
#33694=ORIENTED_EDGE ( 'NONE', *, *, #12480, .T. ) ;
#33705=EDGE_CURVE ( 'NONE', #11614, #8621, #44553, .T. ) ;
#33707=CARTESIAN_POINT ( 'NONE',  ( -5.993516549646711766, 5.993516549646603409, 455.0000000000000568 ) ) ;
#33712=AXIS2_PLACEMENT_3D ( 'NONE', #16752, #143, #33004 ) ;
#33714=FACE_OUTER_BOUND ( 'NONE', #8680, .T. ) ;
#33721=EDGE_LOOP ( 'NONE', ( #2496, #14204, #18074, #56494 ) ) ;
#33724=DIRECTION ( 'NONE',  ( -0.000000000000000000, -0.000000000000000000, -1.000000000000000000 ) ) ;
#33733=PLANE ( 'NONE',  #18110 ) ;
#33734=VERTEX_POINT ( 'NONE', #25385 ) ;
#33753=CARTESIAN_POINT ( 'NONE',  ( 11.78648345035337819, -4.406483450353394282, 195.0000000000000284 ) ) ;
#33754=AXIS2_PLACEMENT_3D ( 'NONE', #69184, #4493, #62828 ) ;
#33765=EDGE_CURVE ( 'NONE', #54840, #27500, #49114, .T. ) ;
#33770=EDGE_CURVE ( 'NONE', #19534, #3474, #38352, .T. ) ;
#33774=VERTEX_POINT ( 'NONE', #28412 ) ;
#33778=DIRECTION ( 'NONE',  ( -1.011922027653137735E-14, -1.000000000000000000, 0.000000000000000000 ) ) ;
#33780=ORIENTED_EDGE ( 'NONE', *, *, #11192, .F. ) ;
#33782=CARTESIAN_POINT ( 'NONE',  ( -11.47551654964677326, -10.20488345035332145, 195.0000000000000284 ) ) ;
#33784=VECTOR ( 'NONE', #12835, 1000.000000000000000 ) ;
#33788=ORIENTED_EDGE ( 'NONE', *, *, #5539, .T. ) ;
#33793=AXIS2_PLACEMENT_3D ( 'NONE', #53364, #15180, #31092 ) ;
#33796=VECTOR ( 'NONE', #21071, 1000.000000000000000 ) ;
#33798=ORIENTED_EDGE ( 'NONE', *, *, #55674, .F. ) ;
#33806=VERTEX_POINT ( 'NONE', #47648 ) ;
#33808=EDGE_CURVE ( 'NONE', #21629, #23669, #49318, .T. ) ;
#33813=ORIENTED_EDGE ( 'NONE', *, *, #26898, .F. ) ;
#33821=VERTEX_POINT ( 'NONE', #33389 ) ;
#33822=VERTEX_POINT ( 'NONE', #895 ) ;
#33832=VERTEX_POINT ( 'NONE', #21133 ) ;
#33835=AXIS2_PLACEMENT_3D ( 'NONE', #19331, #40897, #14026 ) ;
#33836=EDGE_CURVE ( 'NONE', #20610, #28387, #12495, .T. ) ;
#33837=CARTESIAN_POINT ( 'NONE',  ( 7.852485183456931139, -3.430747519065418860, 455.0000000000000568 ) ) ;
#33839=EDGE_CURVE ( 'NONE', #44460, #15622, #31750, .T. ) ;
#33853=CARTESIAN_POINT ( 'NONE',  ( -7.813516549646789322, -11.78648345035335865, 195.0000000000000284 ) ) ;
#33874=DIRECTION ( 'NONE',  ( 0.6414496315691645689, 0.7671651518152939886, 0.000000000000000000 ) ) ;
#33880=ORIENTED_EDGE ( 'NONE', *, *, #22280, .T. ) ;
#33881=CARTESIAN_POINT ( 'NONE',  ( 9.804883450353409913, 11.07551654964657928, 195.0000000000000284 ) ) ;
#33886=EDGE_CURVE ( 'NONE', #50749, #29795, #49642, .T. ) ;
#33888=EDGE_CURVE ( 'NONE', #67654, #47898, #1217, .T. ) ;
#33895=ORIENTED_EDGE ( 'NONE', *, *, #13272, .T. ) ;
#33897=ADVANCED_FACE ( 'NONE', ( #61984 ), #24863, .F. ) ;
#33905=VECTOR ( 'NONE', #45576, 1000.000000000000000 ) ;
#33910=CARTESIAN_POINT ( 'NONE',  ( 8.406483450353379183, -5.668387132715952959, 195.0000000000000284 ) ) ;
#33912=VERTEX_POINT ( 'NONE', #3294 ) ;
#33918=LINE ( 'NONE', #7046, #10892 ) ;
#33927=CARTESIAN_POINT ( 'NONE',  ( -9.234937905884020637, 9.942044687070460185, 195.0000000000000284 ) ) ;
#33936=ADVANCED_FACE ( 'NONE', ( #13199 ), #46423, .F. ) ;
#33937=PLANE ( 'NONE',  #44256 ) ;
#33939=EDGE_CURVE ( 'NONE', #4203, #44680, #34057, .T. ) ;
#33953=ORIENTED_EDGE ( 'NONE', *, *, #45409, .T. ) ;
#33958=AXIS2_PLACEMENT_3D ( 'NONE', #38478, #60025, #66381 ) ;
#33963=ORIENTED_EDGE ( 'NONE', *, *, #63737, .T. ) ;
#33964=FACE_OUTER_BOUND ( 'NONE', #57555, .T. ) ;
#33976=VERTEX_POINT ( 'NONE', #50677 ) ;
#33978=EDGE_CURVE ( 'NONE', #36409, #14259, #19204, .T. ) ;
#33991=AXIS2_PLACEMENT_3D ( 'NONE', #33707, #7169, #66237 ) ;
#33999=VECTOR ( 'NONE', #19408, 1000.000000000000000 ) ;
#34004=VECTOR ( 'NONE', #485, 1000.000000000000000 ) ;
#34005=DIRECTION ( 'NONE',  ( -0.000000000000000000, -0.000000000000000000, -1.000000000000000000 ) ) ;
#34018=CIRCLE ( 'NONE', #36302, 0.1999999999999987899 ) ;
#34021=DIRECTION ( 'NONE',  ( 0.000000000000000000, 1.000000000000000000, 0.000000000000000000 ) ) ;
#34027=AXIS2_PLACEMENT_3D ( 'NONE', #54568, #11079, #32646 ) ;
#34037=ORIENTED_EDGE ( 'NONE', *, *, #33888, .F. ) ;
#34038=CARTESIAN_POINT ( 'NONE',  ( 4.740315990920131561, -7.811466277050838514, 455.0000000000000568 ) ) ;
#34039=EDGE_CURVE ( 'NONE', #54700, #9609, #24520, .T. ) ;
#34046=DIRECTION ( 'NONE',  ( -1.000000000000000000, 0.000000000000000000, 0.000000000000000000 ) ) ;
#34048=DIRECTION ( 'NONE',  ( 0.000000000000000000, 1.000000000000000000, 0.000000000000000000 ) ) ;
#34057=LINE ( 'NONE', #8238, #52505 ) ;
#34073=EDGE_CURVE ( 'NONE', #7012, #54514, #47478, .T. ) ;
#34081=EDGE_CURVE ( 'NONE', #14703, #44963, #52445, .T. ) ;
#34082=CARTESIAN_POINT ( 'NONE',  ( -4.173516549646669738, 11.77351654964658678, 455.0000000000000568 ) ) ;
#34086=CARTESIAN_POINT ( 'NONE',  ( -11.11351654964671098, 7.793516549646603231, 455.0000000000000568 ) ) ;
#34096=FACE_OUTER_BOUND ( 'NONE', #13364, .T. ) ;
#34099=VERTEX_POINT ( 'NONE', #42868 ) ;
#34105=CARTESIAN_POINT ( 'NONE',  ( 9.804883450353379715, -10.20488345035343336, 195.0000000000000284 ) ) ;
#34108=FACE_OUTER_BOUND ( 'NONE', #54544, .T. ) ;
#34109=CARTESIAN_POINT ( 'NONE',  ( -3.593516549646776248, -6.006483450353452547, 455.0000000000000568 ) ) ;
#34112=DIRECTION ( 'NONE',  ( 0.000000000000000000, -3.673940397442059868E-16, 1.000000000000000000 ) ) ;
#34117=ORIENTED_EDGE ( 'NONE', *, *, #9041, .F. ) ;
#34119=LINE ( 'NONE', #22499, #55356 ) ;
#34123=CARTESIAN_POINT ( 'NONE',  ( 11.78648345035337996, 4.393516549646516722, 455.0000000000000568 ) ) ;
#34139=CARTESIAN_POINT ( 'NONE',  ( -9.404046420174124066, 1.853252480934674651, 195.0000000000000284 ) ) ;
#34147=DIRECTION ( 'NONE',  ( -3.717264591378874374E-15, -1.000000000000000000, 0.000000000000000000 ) ) ;
#34152=VERTEX_POINT ( 'NONE', #22004 ) ;
#34153=CARTESIAN_POINT ( 'NONE',  ( -7.603567055985545942, 8.393516549646601987, 455.0000000000000568 ) ) ;
#34163=EDGE_CURVE ( 'NONE', #46020, #58177, #44249, .T. ) ;
#34175=PLANE ( 'NONE',  #29586 ) ;
#34192=ORIENTED_EDGE ( 'NONE', *, *, #5494, .F. ) ;
#34203=EDGE_LOOP ( 'NONE', ( #60948, #65705, #35729, #39259 ) ) ;
#34205=ORIENTED_EDGE ( 'NONE', *, *, #21816, .T. ) ;
#34228=ORIENTED_EDGE ( 'NONE', *, *, #14642, .F. ) ;
#34235=CARTESIAN_POINT ( 'NONE',  ( 10.20488345035345290, 9.791916549646566992, 455.0000000000000568 ) ) ;
#34247=VECTOR ( 'NONE', #32273, 999.9999999999998863 ) ;
#34258=CARTESIAN_POINT ( 'NONE',  ( -5.993516549646776603, -6.006483450353426790, 455.0000000000000568 ) ) ;
#34260=DIRECTION ( 'NONE',  ( 0.000000000000000000, 3.673940397442059868E-16, -1.000000000000000000 ) ) ;
#34266=LINE ( 'NONE', #50887, #43221 ) ;
#34275=EDGE_CURVE ( 'NONE', #58272, #67938, #48885, .T. ) ;
#34280=DIRECTION ( 'NONE',  ( 1.836970198721029934E-16, 1.836970198721010706E-16, -1.000000000000000000 ) ) ;
#34288=DIRECTION ( 'NONE',  ( -1.000000000000000000, 0.000000000000000000, 0.000000000000000000 ) ) ;
#34290=CIRCLE ( 'NONE', #35458, 0.1999999999999992339 ) ;
#34293=ORIENTED_EDGE ( 'NONE', *, *, #32385, .F. ) ;
#34295=DIRECTION ( 'NONE',  ( -1.000000000000000000, 1.671920889371702854E-15, 6.142537696789956391E-31 ) ) ;
#34306=CARTESIAN_POINT ( 'NONE',  ( 4.201500623656003519, -7.272650909786602114, 195.0000000000000284 ) ) ;
#34310=CARTESIAN_POINT ( 'NONE',  ( 7.265214908726123078, -5.393625297349927017, 195.0000000000000284 ) ) ;
#34311=LINE ( 'NONE', #40337, #42261 ) ;
#34313=VERTEX_POINT ( 'NONE', #53028 ) ;
#34316=ORIENTED_EDGE ( 'NONE', *, *, #13817, .T. ) ;
#34322=DIRECTION ( 'NONE',  ( 1.836970198721029934E-16, 1.836970198721010706E-16, -1.000000000000000000 ) ) ;
#34323=ORIENTED_EDGE ( 'NONE', *, *, #28920, .F. ) ;
#34328=ORIENTED_EDGE ( 'NONE', *, *, #10064, .T. ) ;
#34329=ORIENTED_EDGE ( 'NONE', *, *, #15717, .F. ) ;
#34330=FACE_OUTER_BOUND ( 'NONE', #67036, .T. ) ;
#34361=EDGE_CURVE ( 'NONE', #33331, #56963, #37111, .T. ) ;
#34369=EDGE_LOOP ( 'NONE', ( #51674, #13714, #1773, #46649 ) ) ;
#34378=DIRECTION ( 'NONE',  ( 0.000000000000000000, 0.000000000000000000, 1.000000000000000000 ) ) ;
#34379=EDGE_LOOP ( 'NONE', ( #57826, #65883, #52905, #36233 ) ) ;
#34390=CARTESIAN_POINT ( 'NONE',  ( -8.393516549646779623, -6.344579767990844665, 455.0000000000000568 ) ) ;
#34399=LINE ( 'NONE', #39033, #33784 ) ;
#34405=EDGE_CURVE ( 'NONE', #3671, #62585, #68581, .T. ) ;
#34408=CARTESIAN_POINT ( 'NONE',  ( -9.828310488886053520, 1.677516549646603794, 195.0000000000000284 ) ) ;
#34418=ORIENTED_EDGE ( 'NONE', *, *, #61297, .T. ) ;
#34432=VECTOR ( 'NONE', #50772, 1000.000000000000000 ) ;
#34433=AXIS2_PLACEMENT_3D ( 'NONE', #31798, #9884, #43424 ) ;
#34439=DIRECTION ( 'NONE',  ( 1.570596175624152093E-15, -1.000000000000000000, 0.000000000000000000 ) ) ;
#34444=EDGE_CURVE ( 'NONE', #41049, #49618, #13053, .T. ) ;
#34453=DIRECTION ( 'NONE',  ( 1.836970198721029934E-16, 1.836970198721010706E-16, -1.000000000000000000 ) ) ;
#34469=DIRECTION ( 'NONE',  ( -0.5000000000000049960, -0.8660254037844358210, -6.723777587268365305E-17 ) ) ;
#34479=EDGE_CURVE ( 'NONE', #14683, #24763, #69236, .T. ) ;
#34488=CARTESIAN_POINT ( 'NONE',  ( -7.793516549646712477, 11.31351654964660014, 455.0000000000000568 ) ) ;
#34499=VECTOR ( 'NONE', #16550, 1000.000000000000000 ) ;
#34510=EDGE_CURVE ( 'NONE', #28681, #20324, #15506, .T. ) ;
#34514=ORIENTED_EDGE ( 'NONE', *, *, #68540, .F. ) ;
#34532=ORIENTED_EDGE ( 'NONE', *, *, #61992, .F. ) ;
#34538=VECTOR ( 'NONE', #37363, 1000.000000000000000 ) ;
#34544=VECTOR ( 'NONE', #16342, 1000.000000000000114 ) ;
#34545=AXIS2_PLACEMENT_3D ( 'NONE', #61102, #50845, #50512 ) ;
#34549=EDGE_CURVE ( 'NONE', #55545, #67463, #5242, .T. ) ;
#34550=DIRECTION ( 'NONE',  ( 5.120954910632640039E-15, 1.000000000000000000, -0.000000000000000000 ) ) ;
#34561=AXIS2_PLACEMENT_3D ( 'NONE', #29836, #35482, #18890 ) ;
#34570=CARTESIAN_POINT ( 'NONE',  ( -9.791916549646712653, 10.19191654964664018, 195.0000000000000284 ) ) ;
#34574=VERTEX_POINT ( 'NONE', #66358 ) ;
#34589=AXIS2_PLACEMENT_3D ( 'NONE', #3515, #68572, #40980 ) ;
#34599=CARTESIAN_POINT ( 'NONE',  ( 8.406483450353379183, -7.616533956692325802, 455.0000000000000568 ) ) ;
#34623=DIRECTION ( 'NONE',  ( -0.000000000000000000, 3.673940397442059868E-16, -1.000000000000000000 ) ) ;
#34640=ORIENTED_EDGE ( 'NONE', *, *, #3002, .T. ) ;
#34642=CARTESIAN_POINT ( 'NONE',  ( -4.173516549646837603, -11.78648345035344214, 455.0000000000000568 ) ) ;
#34648=FACE_OUTER_BOUND ( 'NONE', #26085, .T. ) ;
#34649=AXIS2_PLACEMENT_3D ( 'NONE', #68842, #48322, #53633 ) ;
#34655=VERTEX_POINT ( 'NONE', #17562 ) ;
#34657=DIRECTION ( 'NONE',  ( -1.000000000000000000, -2.135044278125301343E-15, -7.844025423732065664E-31 ) ) ;
#34659=AXIS2_PLACEMENT_3D ( 'NONE', #11620, #44155, #38188 ) ;
#34675=CARTESIAN_POINT ( 'NONE',  ( -8.393516549646712122, 7.603567055985436696, 455.0000000000000568 ) ) ;
#34678=EDGE_LOOP ( 'NONE', ( #43839, #19903, #15033, #65998 ) ) ;
#34679=DIRECTION ( 'NONE',  ( 0.7671651518152939886, -0.6414496315691644579, -2.587583378555133721E-16 ) ) ;
#34686=LINE ( 'NONE', #39977, #61592 ) ;
#34688=VERTEX_POINT ( 'NONE', #7985 ) ;
#34694=FACE_OUTER_BOUND ( 'NONE', #59924, .T. ) ;
#34702=ORIENTED_EDGE ( 'NONE', *, *, #53461, .F. ) ;
#34706=CARTESIAN_POINT ( 'NONE',  ( 11.12648345035337627, -9.106483450353492159, 455.0000000000000568 ) ) ;
#34707=AXIS2_PLACEMENT_3D ( 'NONE', #26433, #16170, #41641 ) ;
#34708=CARTESIAN_POINT ( 'NONE',  ( 12.00648345035337350, 11.18071654964659345, 195.0000000000000284 ) ) ;
#34711=CARTESIAN_POINT ( 'NONE',  ( -9.293516549646710700, 10.91351654964659801, 455.0000000000000568 ) ) ;
#34712=DIRECTION ( 'NONE',  ( -0.000000000000000000, 3.673940397442059868E-16, -1.000000000000000000 ) ) ;
#34721=PLANE ( 'NONE',  #35881 ) ;
#34725=DIRECTION ( 'NONE',  ( -1.836970198721029934E-16, -1.836970198721010706E-16, 1.000000000000000000 ) ) ;
#34730=DIRECTION ( 'NONE',  ( 1.000000000000000000, -1.047444401652940007E-14, 1.836970198721010706E-16 ) ) ;
#34733=ORIENTED_EDGE ( 'NONE', *, *, #14246, .F. ) ;
#34734=CARTESIAN_POINT ( 'NONE',  ( -4.383466043307968185, -8.406483450353443132, 455.0000000000000568 ) ) ;
#34741=LINE ( 'NONE', #34038, #24301 ) ;
#34743=CARTESIAN_POINT ( 'NONE',  ( -5.993516549646711766, 5.993516549646603409, 455.0000000000000568 ) ) ;
#34746=CARTESIAN_POINT ( 'NONE',  ( 6.006483450353379716, -6.006483450353490738, 455.0000000000000568 ) ) ;
#34747=ORIENTED_EDGE ( 'NONE', *, *, #5135, .F. ) ;
#34749=AXIS2_PLACEMENT_3D ( 'NONE', #38928, #60487, #33625 ) ;
#34752=DIRECTION ( 'NONE',  ( -1.156482317317873342E-14, -1.000000000000000000, 0.000000000000000000 ) ) ;
#34765=FACE_OUTER_BOUND ( 'NONE', #10019, .T. ) ;
#34769=ORIENTED_EDGE ( 'NONE', *, *, #42493, .F. ) ;
#34777=EDGE_CURVE ( 'NONE', #31939, #59906, #67412, .T. ) ;
#34781=DIRECTION ( 'NONE',  ( 0.000000000000000000, 1.000000000000000000, 3.673940397442059868E-16 ) ) ;
#34807=EDGE_CURVE ( 'NONE', #68360, #15497, #20954, .T. ) ;
#34810=ORIENTED_EDGE ( 'NONE', *, *, #1672, .F. ) ;
#34830=CARTESIAN_POINT ( 'NONE',  ( 5.668387132715968058, 8.393516549646582448, 455.0000000000000568 ) ) ;
#34831=DIRECTION ( 'NONE',  ( 0.7071067811865474617, -0.7071067811865474617, 0.000000000000000000 ) ) ;
#34835=VECTOR ( 'NONE', #48276, 1000.000000000000000 ) ;
#34839=DIRECTION ( 'NONE',  ( 1.836970198721029934E-16, 1.836970198721010706E-16, -1.000000000000000000 ) ) ;
#34840=CARTESIAN_POINT ( 'NONE',  ( -10.91351654964670637, 9.293516549646604119, 455.0000000000000568 ) ) ;
#34843=DIRECTION ( 'NONE',  ( 1.000000000000000000, 0.000000000000000000, 0.000000000000000000 ) ) ;
#34844=ORIENTED_EDGE ( 'NONE', *, *, #35120, .T. ) ;
#34845=ORIENTED_EDGE ( 'NONE', *, *, #29459, .T. ) ;
#34847=VECTOR ( 'NONE', #8978, 1000.000000000000000 ) ;
#34851=VERTEX_POINT ( 'NONE', #68098 ) ;
#34869=LINE ( 'NONE', #46535, #40064 ) ;
#34876=EDGE_CURVE ( 'NONE', #37791, #16514, #20013, .T. ) ;
#34880=DIRECTION ( 'NONE',  ( -1.836970198721029934E-16, -1.836970198721010706E-16, 1.000000000000000000 ) ) ;
#34895=CARTESIAN_POINT ( 'NONE',  ( -5.993516549646728642, -6.006483450353378828, 195.0000000000000284 ) ) ;
#34899=EDGE_CURVE ( 'NONE', #25493, #33142, #21063, .T. ) ;
#34911=ORIENTED_EDGE ( 'NONE', *, *, #47864, .T. ) ;
#34918=ORIENTED_EDGE ( 'NONE', *, *, #17311, .T. ) ;
#34927=ORIENTED_EDGE ( 'NONE', *, *, #24102, .T. ) ;
#34935=VECTOR ( 'NONE', #68955, 1000.000000000000000 ) ;
#34947=VECTOR ( 'NONE', #68228, 1000.000000000000227 ) ;
#34955=DIRECTION ( 'NONE',  ( -1.000000000000000000, 1.901462112903060228E-14, -1.836970198720995175E-16 ) ) ;
#34976=CARTESIAN_POINT ( 'NONE',  ( -11.31351654964670850, 7.793516549646603231, 455.0000000000000568 ) ) ;
#34979=VECTOR ( 'NONE', #8697, 1000.000000000000000 ) ;
#34989=DIRECTION ( 'NONE',  ( -1.000000000000000000, -1.671920889371702657E-15, 0.000000000000000000 ) ) ;
#35012=FACE_OUTER_BOUND ( 'NONE', #66523, .T. ) ;
#35013=DIRECTION ( 'NONE',  ( 0.6414496315691575745, 0.7671651518152999838, 2.587583378555113013E-16 ) ) ;
#35023=VERTEX_POINT ( 'NONE', #44007 ) ;
#35028=CIRCLE ( 'NONE', #24902, 0.1999999999999987899 ) ;
#35032=PLANE ( 'NONE',  #55724 ) ;
#35035=ORIENTED_EDGE ( 'NONE', *, *, #69160, .T. ) ;
#35037=DIRECTION ( 'NONE',  ( -1.836970198721029934E-16, 1.836970198721036344E-16, -1.000000000000000000 ) ) ;
#35044=DIRECTION ( 'NONE',  ( -1.000000000000000000, 8.339399738404101090E-15, -1.836970198721014896E-16 ) ) ;
#35056=CARTESIAN_POINT ( 'NONE',  ( -2.752095193409374030, 9.942044687070435316, 195.0000000000000284 ) ) ;
#35059=PLANE ( 'NONE',  #3961 ) ;
#35063=LINE ( 'NONE', #19162, #43810 ) ;
#35071=EDGE_CURVE ( 'NONE', #40323, #29254, #28103, .T. ) ;
#35072=CARTESIAN_POINT ( 'NONE',  ( 11.12648345035340647, 7.793516549646564151, 455.0000000000000568 ) ) ;
#35076=CARTESIAN_POINT ( 'NONE',  ( 7.616533956692213003, -8.406483450353491094, 455.0000000000000568 ) ) ;
#35094=CARTESIAN_POINT ( 'NONE',  ( 9.247904806590689475, -9.955011587777349291, 455.0000000000000568 ) ) ;
#35098=FACE_OUTER_BOUND ( 'NONE', #41099, .T. ) ;
#35101=VERTEX_POINT ( 'NONE', #17481 ) ;
#35102=AXIS2_PLACEMENT_3D ( 'NONE', #48594, #26682, #64862 ) ;
#35109=ADVANCED_FACE ( 'NONE', ( #60622 ), #12174, .F. ) ;
#35113=ORIENTED_EDGE ( 'NONE', *, *, #50402, .T. ) ;
#35114=VECTOR ( 'NONE', #25970, 1000.000000000000000 ) ;
#35120=EDGE_CURVE ( 'NONE', #64293, #4435, #1814, .T. ) ;
#35123=DIRECTION ( 'NONE',  ( -8.359604446858499085E-15, -1.000000000000000000, 0.000000000000000000 ) ) ;
#35127=ORIENTED_EDGE ( 'NONE', *, *, #55938, .F. ) ;
#35128=ORIENTED_EDGE ( 'NONE', *, *, #38441, .T. ) ;
#35134=ORIENTED_EDGE ( 'NONE', *, *, #23785, .F. ) ;
#35140=VERTEX_POINT ( 'NONE', #28778 ) ;
#35142=DIRECTION ( 'NONE',  ( -1.836970198721029934E-16, 1.836970198721036344E-16, -1.000000000000000000 ) ) ;
#35143=CIRCLE ( 'NONE', #58847, 0.2000000000000005107 ) ;
#35166=FACE_OUTER_BOUND ( 'NONE', #23478, .T. ) ;
#35172=CARTESIAN_POINT ( 'NONE',  ( 7.428221114745003462, -3.006483450353490294, 455.0000000000000568 ) ) ;
#35173=VERTEX_POINT ( 'NONE', #51401 ) ;
#35176=CARTESIAN_POINT ( 'NONE',  ( -9.942044687070568543, 9.234937905883914055, 195.0000000000000284 ) ) ;
#35181=ORIENTED_EDGE ( 'NONE', *, *, #445, .F. ) ;
#35182=VERTEX_POINT ( 'NONE', #60954 ) ;
#35193=ORIENTED_EDGE ( 'NONE', *, *, #39600, .F. ) ;
#35194=VECTOR ( 'NONE', #47221, 1000.000000000000000 ) ;
#35195=AXIS2_PLACEMENT_3D ( 'NONE', #26865, #5976, #53388 ) ;
#35197=CYLINDRICAL_SURFACE ( 'NONE', #12408, 0.1999999999999987899 ) ;
#35199=LINE ( 'NONE', #66353, #66544 ) ;
#35209=DIRECTION ( 'NONE',  ( 0.000000000000000000, 3.673940397442059868E-16, -1.000000000000000000 ) ) ;
#35212=ADVANCED_FACE ( 'NONE', ( #29484 ), #3321, .F. ) ;
#35224=ORIENTED_EDGE ( 'NONE', *, *, #64219, .T. ) ;
#35227=AXIS2_PLACEMENT_3D ( 'NONE', #27511, #49076, #64308 ) ;
#35233=CARTESIAN_POINT ( 'NONE',  ( 8.465062094116069247, -4.255011587777252302, 195.0000000000000284 ) ) ;
#35237=ORIENTED_EDGE ( 'NONE', *, *, #1363, .T. ) ;
#35248=VERTEX_POINT ( 'NONE', #56708 ) ;
#35251=ORIENTED_EDGE ( 'NONE', *, *, #64283, .F. ) ;
#35255=ORIENTED_EDGE ( 'NONE', *, *, #36102, .T. ) ;
#35257=DIRECTION ( 'NONE',  ( -0.5000000000000129896, -0.8660254037844311581, -2.509347957447868930E-16 ) ) ;
#35259=ORIENTED_EDGE ( 'NONE', *, *, #63512, .T. ) ;
#35260=DIRECTION ( 'NONE',  ( 0.7071067811865474617, 0.7071067811865474617, 0.000000000000000000 ) ) ;
#35261=ORIENTED_EDGE ( 'NONE', *, *, #2638, .T. ) ;
#35264=CYLINDRICAL_SURFACE ( 'NONE', #13258, 0.1999999999999987899 ) ;
#35280=CARTESIAN_POINT ( 'NONE',  ( 8.406483450353356091, 6.331612867284063917, 195.0000000000000284 ) ) ;
#35290=DIRECTION ( 'NONE',  ( 0.000000000000000000, -3.673940397442059868E-16, 1.000000000000000000 ) ) ;
#35303=VECTOR ( 'NONE', #51441, 1000.000000000000000 ) ;
#35314=FACE_OUTER_BOUND ( 'NONE', #45400, .T. ) ;
#35317=DIRECTION ( 'NONE',  ( 1.836970198721029934E-16, 1.836970198721010706E-16, -1.000000000000000000 ) ) ;
#35318=AXIS2_PLACEMENT_3D ( 'NONE', #59065, #20188, #26545 ) ;
#35319=EDGE_CURVE ( 'NONE', #19180, #14864, #45928, .T. ) ;
#35322=VERTEX_POINT ( 'NONE', #41140 ) ;
#35330=AXIS2_PLACEMENT_3D ( 'NONE', #66175, #17739, #55912 ) ;
#35332=EDGE_CURVE ( 'NONE', #1311, #7275, #31, .T. ) ;
#35336=VERTEX_POINT ( 'NONE', #5344 ) ;
#35345=CARTESIAN_POINT ( 'NONE',  ( 3.430747519065294071, -7.852485183457023510, 455.0000000000000568 ) ) ;
#35352=DIRECTION ( 'NONE',  ( 1.000000000000000000, -1.952517519553884087E-14, 1.836970198720994435E-16 ) ) ;
#35354=VERTEX_POINT ( 'NONE', #38213 ) ;
#35357=CARTESIAN_POINT ( 'NONE',  ( -11.99351654964671354, 7.813516549646603693, 195.0000000000000284 ) ) ;
#35358=CARTESIAN_POINT ( 'NONE',  ( 4.186483450353337687, -11.78648345035347589, 455.0000000000000568 ) ) ;
#35362=ORIENTED_EDGE ( 'NONE', *, *, #69062, .F. ) ;
#35364=ORIENTED_EDGE ( 'NONE', *, *, #21107, .T. ) ;
#35369=EDGE_CURVE ( 'NONE', #2424, #34152, #4157, .T. ) ;
#35381=VECTOR ( 'NONE', #60830, 999.9999999999998863 ) ;
#35382=VERTEX_POINT ( 'NONE', #38546 ) ;
#35383=EDGE_LOOP ( 'NONE', ( #32294, #30687, #63514, #1016 ) ) ;
#35387=ORIENTED_EDGE ( 'NONE', *, *, #21423, .T. ) ;
#35395=DIRECTION ( 'NONE',  ( 0.000000000000000000, 0.000000000000000000, 1.000000000000000000 ) ) ;
#35401=DIRECTION ( 'NONE',  ( -0.000000000000000000, 1.000000000000000000, -0.000000000000000000 ) ) ;
#35409=VECTOR ( 'NONE', #13284, 1000.000000000000000 ) ;
#35421=AXIS2_PLACEMENT_3D ( 'NONE', #21650, #32948, #432 ) ;
#35422=CARTESIAN_POINT ( 'NONE',  ( 4.740315990920131561, -7.811466277050838514, 455.0000000000000568 ) ) ;
#35429=ORIENTED_EDGE ( 'NONE', *, *, #42670, .F. ) ;
#35432=LINE ( 'NONE', #8567, #22050 ) ;
#35436=LINE ( 'NONE', #2926, #67880 ) ;
#35440=ORIENTED_EDGE ( 'NONE', *, *, #47460, .F. ) ;
#35443=DIRECTION ( 'NONE',  ( -0.7071067811865474617, 0.7071067811865474617, 0.000000000000000000 ) ) ;
#35447=DIRECTION ( 'NONE',  ( 1.836970198721029934E-16, 1.836970198721010706E-16, -1.000000000000000000 ) ) ;
#35453=EDGE_CURVE ( 'NONE', #13195, #67463, #19942, .T. ) ;
#35456=DIRECTION ( 'NONE',  ( 8.673617379884030739E-15, 1.000000000000000000, 0.000000000000000000 ) ) ;
#35458=AXIS2_PLACEMENT_3D ( 'NONE', #65897, #7183, #66256 ) ;
#35459=DIRECTION ( 'NONE',  ( -3.491481338843133355E-15, -1.000000000000000000, -1.836970198721029934E-16 ) ) ;
#35467=VERTEX_POINT ( 'NONE', #33910 ) ;
#35480=VECTOR ( 'NONE', #3417, 1000.000000000000000 ) ;
#35482=DIRECTION ( 'NONE',  ( -1.836970198721029934E-16, -1.836970198721010706E-16, 1.000000000000000000 ) ) ;
#35483=ORIENTED_EDGE ( 'NONE', *, *, #51972, .F. ) ;
#35486=FACE_OUTER_BOUND ( 'NONE', #32660, .T. ) ;
#35491=LINE ( 'NONE', #47177, #53572 ) ;
#35493=ORIENTED_EDGE ( 'NONE', *, *, #2972, .F. ) ;
#35498=CARTESIAN_POINT ( 'NONE',  ( 1.690483450353344352, -10.74648345035345720, 455.0000000000000568 ) ) ;
#35502=AXIS2_PLACEMENT_3D ( 'NONE', #63679, #42091, #51660 ) ;
#35510=FACE_OUTER_BOUND ( 'NONE', #6426, .T. ) ;
#35515=DIRECTION ( 'NONE',  ( -0.000000000000000000, -0.000000000000000000, -1.000000000000000000 ) ) ;
#35519=AXIS2_PLACEMENT_3D ( 'NONE', #2755, #46243, #46944 ) ;
#35527=EDGE_CURVE ( 'NONE', #30476, #53367, #67845, .T. ) ;
#35529=LINE ( 'NONE', #62761, #27844 ) ;
#35536=ORIENTED_EDGE ( 'NONE', *, *, #59508, .T. ) ;
#35541=DIRECTION ( 'NONE',  ( -1.000000000000000000, 0.000000000000000000, 0.000000000000000000 ) ) ;
#35552=LINE ( 'NONE', #30618, #12984 ) ;
#35556=AXIS2_PLACEMENT_3D ( 'NONE', #30119, #40730, #30822 ) ;
#35557=VECTOR ( 'NONE', #52728, 1000.000000000000000 ) ;
#35566=EDGE_CURVE ( 'NONE', #62792, #26698, #68503, .T. ) ;
#35576=VECTOR ( 'NONE', #43944, 1000.000000000000000 ) ;
#35577=CARTESIAN_POINT ( 'NONE',  ( 3.606483450353380249, -4.622483450353491286, 455.0000000000000568 ) ) ;
#35580=PLANE ( 'NONE',  #5436 ) ;
#35582=ORIENTED_EDGE ( 'NONE', *, *, #54951, .F. ) ;
#35593=DIRECTION ( 'NONE',  ( 0.000000000000000000, -1.000000000000000000, 0.000000000000000000 ) ) ;
#35597=CARTESIAN_POINT ( 'NONE',  ( 4.406483450353340103, -11.32648345035347681, 455.0000000000000568 ) ) ;
#35599=CIRCLE ( 'NONE', #26592, 0.1999999999999987899 ) ;
#35605=VECTOR ( 'NONE', #59350, 1000.000000000000000 ) ;
#35607=EDGE_LOOP ( 'NONE', ( #1734, #23216, #3292, #12304 ) ) ;
#35610=PLANE ( 'NONE',  #17532 ) ;
#35612=CARTESIAN_POINT ( 'NONE',  ( 10.09643294401453417, 2.893516549646536262, 455.0000000000000568 ) ) ;
#35615=AXIS2_PLACEMENT_3D ( 'NONE', #69593, #10188, #10882 ) ;
#35616=CARTESIAN_POINT ( 'NONE',  ( 4.255011587777218551, -8.465062094116168723, 455.0000000000000568 ) ) ;
#35621=ORIENTED_EDGE ( 'NONE', *, *, #33886, .T. ) ;
#35625=VECTOR ( 'NONE', #69641, 1000.000000000000000 ) ;
#35637=LINE ( 'NONE', #30354, #11885 ) ;
#35642=ORIENTED_EDGE ( 'NONE', *, *, #35690, .F. ) ;
#35648=VERTEX_POINT ( 'NONE', #32114 ) ;
#35651=DIRECTION ( 'NONE',  ( 1.053224967557347660E-14, 1.000000000000000000, 0.000000000000000000 ) ) ;
#35652=CIRCLE ( 'NONE', #46915, 2.204799999999997429 ) ;
#35653=DIRECTION ( 'NONE',  ( -1.000000000000000000, 0.000000000000000000, 0.000000000000000000 ) ) ;
#35655=CIRCLE ( 'NONE', #41316, 1.399999999999998579 ) ;
#35667=CARTESIAN_POINT ( 'NONE',  ( 10.92648345035337520, -2.906483450353491094, 455.0000000000000568 ) ) ;
#35672=CARTESIAN_POINT ( 'NONE',  ( 8.606483450353380249, -7.616533956692325802, 455.0000000000000568 ) ) ;
#35684=CARTESIAN_POINT ( 'NONE',  ( 7.811466277050774565, 7.259684009079793832, 455.0000000000000568 ) ) ;
#35685=CARTESIAN_POINT ( 'NONE',  ( 8.406483450353398723, 5.655420232009111814, 455.0000000000000568 ) ) ;
#35686=ORIENTED_EDGE ( 'NONE', *, *, #45330, .T. ) ;
#35689=DIRECTION ( 'NONE',  ( -1.671920889371702657E-15, 1.000000000000000000, 3.673940397442059868E-16 ) ) ;
#35690=EDGE_CURVE ( 'NONE', #21517, #44259, #64632, .T. ) ;
#35693=EDGE_CURVE ( 'NONE', #41134, #62844, #4213, .T. ) ;
#35699=VERTEX_POINT ( 'NONE', #48026 ) ;
#35709=EDGE_CURVE ( 'NONE', #50275, #62585, #15517, .T. ) ;
#35711=DIRECTION ( 'NONE',  ( -1.000000000000000000, 0.000000000000000000, 0.000000000000000000 ) ) ;
#35715=CIRCLE ( 'NONE', #32356, 0.5999999999999989786 ) ;
#35728=CARTESIAN_POINT ( 'NONE',  ( -2.277516549646816379, -9.841277389592805847, 455.0000000000000568 ) ) ;
#35729=ORIENTED_EDGE ( 'NONE', *, *, #66010, .F. ) ;
#35739=ORIENTED_EDGE ( 'NONE', *, *, #69529, .F. ) ;
#35742=CYLINDRICAL_SURFACE ( 'NONE', #19871, 1.399999999999998579 ) ;
#35747=ORIENTED_EDGE ( 'NONE', *, *, #18779, .T. ) ;
#35749=DIRECTION ( 'NONE',  ( -1.836970198721029934E-16, 1.836970198721036344E-16, -1.000000000000000000 ) ) ;
#35750=VECTOR ( 'NONE', #41774, 1000.000000000000000 ) ;
#35757=CARTESIAN_POINT ( 'NONE',  ( -7.813516549646711162, 11.99351654964660341, 455.0000000000000568 ) ) ;
#35763=ADVANCED_FACE ( 'NONE', ( #31067 ), #9863, .F. ) ;
#35765=ORIENTED_EDGE ( 'NONE', *, *, #69683, .T. ) ;
#35773=EDGE_CURVE ( 'NONE', #30052, #49314, #20798, .T. ) ;
#35790=ORIENTED_EDGE ( 'NONE', *, *, #24853, .F. ) ;
#35792=CARTESIAN_POINT ( 'NONE',  ( 2.706483450353418085, 10.08346604330775875, 455.0000000000000568 ) ) ;
#35796=ORIENTED_EDGE ( 'NONE', *, *, #30306, .T. ) ;
#35797=EDGE_CURVE ( 'NONE', #59188, #60382, #68900, .T. ) ;
#35803=CARTESIAN_POINT ( 'NONE',  ( -5.993516549646776603, -6.006483450353426790, 455.0000000000000568 ) ) ;
#35805=CARTESIAN_POINT ( 'NONE',  ( 11.12648345035331587, 2.893516549646573566, 195.0000000000000284 ) ) ;
#35806=FACE_BOUND ( 'NONE', #18322, .T. ) ;
#35811=ORIENTED_EDGE ( 'NONE', *, *, #25833, .F. ) ;
#35820=VECTOR ( 'NONE', #41173, 1000.000000000000000 ) ;
#35824=VERTEX_POINT ( 'NONE', #64296 ) ;
#35827=FACE_OUTER_BOUND ( 'NONE', #62500, .T. ) ;
#35833=ORIENTED_EDGE ( 'NONE', *, *, #6154, .T. ) ;
#35844=CARTESIAN_POINT ( 'NONE',  ( -4.393516549646671265, 11.31351654964658771, 455.0000000000000568 ) ) ;
#35852=CARTESIAN_POINT ( 'NONE',  ( 9.306483450353372433, 10.91351654964661044, 195.0000000000000284 ) ) ;
#35853=CARTESIAN_POINT ( 'NONE',  ( 6.006483450353379716, -6.006483450353490738, 455.0000000000000568 ) ) ;
#35854=ADVANCED_FACE ( 'NONE', ( #66368 ), #60349, .F. ) ;
#35855=ORIENTED_EDGE ( 'NONE', *, *, #64139, .F. ) ;
#35856=DIRECTION ( 'NONE',  ( 1.836970198721029934E-16, 1.836970198721010706E-16, -1.000000000000000000 ) ) ;
#35861=LINE ( 'NONE', #8639, #25704 ) ;
#35867=ORIENTED_EDGE ( 'NONE', *, *, #40585, .F. ) ;
#35872=DIRECTION ( 'NONE',  ( 1.000000000000000000, -1.047444401652939849E-14, 0.000000000000000000 ) ) ;
#35876=CARTESIAN_POINT ( 'NONE',  ( -11.31351654964671027, 7.593516549646603941, 455.0000000000000568 ) ) ;
#35879=CARTESIAN_POINT ( 'NONE',  ( -7.793516549646829716, -11.32648345035340576, 455.0000000000000568 ) ) ;
#35881=AXIS2_PLACEMENT_3D ( 'NONE', #7841, #18812, #24822 ) ;
#35892=CARTESIAN_POINT ( 'NONE',  ( -9.093516549646817992, -10.09643294401455904, 455.0000000000000568 ) ) ;
#35893=ADVANCED_FACE ( 'NONE', ( #60011 ), #33141, .T. ) ;
#35896=VERTEX_POINT ( 'NONE', #54725 ) ;
#35906=ORIENTED_EDGE ( 'NONE', *, *, #3430, .F. ) ;
#35910=CARTESIAN_POINT ( 'NONE',  ( -8.393516549646712122, 4.383466043307770121, 455.0000000000000568 ) ) ;
#35921=ORIENTED_EDGE ( 'NONE', *, *, #7935, .F. ) ;
#35925=ORIENTED_EDGE ( 'NONE', *, *, #4415, .F. ) ;
#35940=AXIS2_PLACEMENT_3D ( 'NONE', #47183, #68751, #58504 ) ;
#35953=LINE ( 'NONE', #68486, #60411 ) ;
#35963=DIRECTION ( 'NONE',  ( -1.349135440953254805E-14, -1.000000000000000000, 0.000000000000000000 ) ) ;
#35973=DIRECTION ( 'NONE',  ( 1.000000000000000000, -1.260948829465470062E-14, 0.000000000000000000 ) ) ;
#35975=ORIENTED_EDGE ( 'NONE', *, *, #25001, .F. ) ;
#35986=VERTEX_POINT ( 'NONE', #29210 ) ;
#35987=CYLINDRICAL_SURFACE ( 'NONE', #53106, 0.2000000000000005107 ) ;
#35995=PLANE ( 'NONE',  #24045 ) ;
#36020=CARTESIAN_POINT ( 'NONE',  ( 7.606483450353380249, -11.32648345035348925, 455.0000000000000568 ) ) ;
#36022=VERTEX_POINT ( 'NONE', #2694 ) ;
#36034=CARTESIAN_POINT ( 'NONE',  ( -10.19191654964685689, -10.20488345035338362, 455.0000000000000568 ) ) ;
#36038=ORIENTED_EDGE ( 'NONE', *, *, #23247, .T. ) ;
#36045=VERTEX_POINT ( 'NONE', #8345 ) ;
#36050=ORIENTED_EDGE ( 'NONE', *, *, #50933, .T. ) ;
#36054=ORIENTED_EDGE ( 'NONE', *, *, #65583, .F. ) ;
#36055=ADVANCED_FACE ( 'NONE', ( #25324 ), #24976, .F. ) ;
#36058=EDGE_CURVE ( 'NONE', #2766, #16233, #20998, .T. ) ;
#36063=ORIENTED_EDGE ( 'NONE', *, *, #16110, .F. ) ;
#36066=CIRCLE ( 'NONE', #43988, 0.5999999999999998668 ) ;
#36067=ORIENTED_EDGE ( 'NONE', *, *, #61454, .T. ) ;
#36070=FACE_OUTER_BOUND ( 'NONE', #45693, .T. ) ;
#36075=AXIS2_PLACEMENT_3D ( 'NONE', #13418, #67526, #61488 ) ;
#36078=DIRECTION ( 'NONE',  ( -1.836970198721029934E-16, -1.836970198721010706E-16, 1.000000000000000000 ) ) ;
#36088=ORIENTED_EDGE ( 'NONE', *, *, #18982, .F. ) ;
#36091=DIRECTION ( 'NONE',  ( 0.000000000000000000, 1.000000000000000000, 0.000000000000000000 ) ) ;
#36094=DIRECTION ( 'NONE',  ( 0.000000000000000000, -0.000000000000000000, 1.000000000000000000 ) ) ;
#36095=CARTESIAN_POINT ( 'NONE',  ( -6.331612867284244217, -8.406483450353421816, 455.0000000000000568 ) ) ;
#36097=ADVANCED_FACE ( 'NONE', ( #47592 ), #10803, .F. ) ;
#36101=CARTESIAN_POINT ( 'NONE',  ( -4.193516549646831848, -11.12648345035344377, 455.0000000000000568 ) ) ;
#36102=EDGE_CURVE ( 'NONE', #4470, #62021, #56020, .T. ) ;
#36106=DIRECTION ( 'NONE',  ( -1.000000000000000000, 0.000000000000000000, 0.000000000000000000 ) ) ;
#36114=ORIENTED_EDGE ( 'NONE', *, *, #28905, .F. ) ;
#36116=AXIS2_PLACEMENT_3D ( 'NONE', #3027, #45091, #7255 ) ;
#36121=PLANE ( 'NONE',  #2807 ) ;
#36124=CIRCLE ( 'NONE', #66606, 0.5999999999999989786 ) ;
#36133=ORIENTED_EDGE ( 'NONE', *, *, #48481, .F. ) ;
#36158=DIRECTION ( 'NONE',  ( 1.000000000000000000, 0.000000000000000000, 0.000000000000000000 ) ) ;
#36171=ORIENTED_EDGE ( 'NONE', *, *, #58635, .T. ) ;
#36173=FACE_OUTER_BOUND ( 'NONE', #31356, .T. ) ;
#36176=DIRECTION ( 'NONE',  ( -0.000000000000000000, -0.000000000000000000, -1.000000000000000000 ) ) ;
#36177=EDGE_CURVE ( 'NONE', #39630, #10108, #64560, .T. ) ;
#36178=ORIENTED_EDGE ( 'NONE', *, *, #32201, .F. ) ;
#36181=CARTESIAN_POINT ( 'NONE',  ( 6.619341603356846626, 4.734785091273825408, 455.0000000000000568 ) ) ;
#36189=DIRECTION ( 'NONE',  ( 1.836970198721029934E-16, 1.836970198721010706E-16, -1.000000000000000000 ) ) ;
#36203=PLANE ( 'NONE',  #3900 ) ;
#36206=ORIENTED_EDGE ( 'NONE', *, *, #36878, .T. ) ;
#36207=CARTESIAN_POINT ( 'NONE',  ( 11.08848345035337424, 11.47551654964657608, 195.0000000000000284 ) ) ;
#36208=LINE ( 'NONE', #19950, #35114 ) ;
#36220=CARTESIAN_POINT ( 'NONE',  ( 10.20488345035345468, 10.19191654964656735, 455.0000000000000568 ) ) ;
#36223=CARTESIAN_POINT ( 'NONE',  ( -8.593516549646745162, -4.396432944014545541, 455.0000000000000568 ) ) ;
#36225=ORIENTED_EDGE ( 'NONE', *, *, #4604, .F. ) ;
#36229=CIRCLE ( 'NONE', #45245, 0.1999999999999987899 ) ;
#36233=ORIENTED_EDGE ( 'NONE', *, *, #15147, .T. ) ;
#36234=CARTESIAN_POINT ( 'NONE',  ( -5.380658396643315022, -4.747751991980679875, 455.0000000000000568 ) ) ;
#36235=ORIENTED_EDGE ( 'NONE', *, *, #51031, .T. ) ;
#36237=CARTESIAN_POINT ( 'NONE',  ( 6.006483450353379716, -8.211283450353395352, 195.0000000000000284 ) ) ;
#36243=DIRECTION ( 'NONE',  ( 0.7671651518153006499, -0.6414496315691565753, -2.356647714346250026E-16 ) ) ;
#36251=PLANE ( 'NONE',  #53564 ) ;
#36252=FACE_OUTER_BOUND ( 'NONE', #54132, .T. ) ;
#36253=( NAMED_UNIT ( * ) PLANE_ANGLE_UNIT ( ) SI_UNIT ( $, .RADIAN. ) );
#36255=VERTEX_POINT ( 'NONE', #12523 ) ;
#36259=ADVANCED_FACE ( 'NONE', ( #49675 ), #59934, .F. ) ;
#36260=DIRECTION ( 'NONE',  ( -0.000000000000000000, -0.000000000000000000, -1.000000000000000000 ) ) ;
#36265=EDGE_CURVE ( 'NONE', #11916, #3912, #65592, .T. ) ;
#36275=FACE_OUTER_BOUND ( 'NONE', #66395, .T. ) ;
#36295=LINE ( 'NONE', #14386, #63003 ) ;
#36296=FACE_OUTER_BOUND ( 'NONE', #12998, .T. ) ;
#36297=ORIENTED_EDGE ( 'NONE', *, *, #21066, .F. ) ;
#36300=PLANE ( 'NONE',  #50224 ) ;
#36302=AXIS2_PLACEMENT_3D ( 'NONE', #17143, #11823, #33413 ) ;
#36318=ORIENTED_EDGE ( 'NONE', *, *, #1363, .F. ) ;
#36329=DIRECTION ( 'NONE',  ( 0.7071067811865474617, 0.7071067811865474617, 0.000000000000000000 ) ) ;
#36333=CARTESIAN_POINT ( 'NONE',  ( 1.690483450353418959, 10.73351654964659652, 455.0000000000000568 ) ) ;
#36337=PLANE ( 'NONE',  #34707 ) ;
#36338=CARTESIAN_POINT ( 'NONE',  ( 6.006483450353401921, 5.993516549646582092, 455.0000000000000568 ) ) ;
#36350=LINE ( 'NONE', #19040, #18648 ) ;
#36356=ORIENTED_EDGE ( 'NONE', *, *, #26395, .F. ) ;
#36360=ORIENTED_EDGE ( 'NONE', *, *, #9151, .F. ) ;
#36362=DIRECTION ( 'NONE',  ( -1.000000000000000000, 0.000000000000000000, 0.000000000000000000 ) ) ;
#36363=LINE ( 'NONE', #56532, #43028 ) ;
#36369=LINE ( 'NONE', #30723, #8869 ) ;
#36372=VERTEX_POINT ( 'NONE', #13230 ) ;
#36375=CIRCLE ( 'NONE', #13806, 0.4000000000000010214 ) ;
#36376=DIRECTION ( 'NONE',  ( 0.000000000000000000, 1.000000000000000000, 0.000000000000000000 ) ) ;
#36378=CARTESIAN_POINT ( 'NONE',  ( -9.293516549646827940, -10.92648345035338764, 455.0000000000000568 ) ) ;
#36379=VECTOR ( 'NONE', #7261, 1000.000000000000000 ) ;
#36384=CARTESIAN_POINT ( 'NONE',  ( 4.740315990920173306, 7.798499376343941414, 455.0000000000000568 ) ) ;
#36387=CARTESIAN_POINT ( 'NONE',  ( 2.765062094116041980, -9.955011587777324422, 455.0000000000000568 ) ) ;
#36389=DIRECTION ( 'NONE',  ( 1.000000000000000000, 1.671920889371702854E-15, 6.142537696789956391E-31 ) ) ;
#36391=DIRECTION ( 'NONE',  ( 0.000000000000000000, -1.000000000000000000, 0.000000000000000000 ) ) ;
#36403=DIRECTION ( 'NONE',  ( 8.673617379884087537E-15, 1.000000000000000000, 0.000000000000000000 ) ) ;
#36409=VERTEX_POINT ( 'NONE', #35852 ) ;
#36413=AXIS2_PLACEMENT_3D ( 'NONE', #6581, #65619, #54671 ) ;
#36414=EDGE_CURVE ( 'NONE', #34152, #44259, #7577, .T. ) ;
#36415=DIRECTION ( 'NONE',  ( 0.000000000000000000, 1.000000000000000000, 0.000000000000000000 ) ) ;
#36418=EDGE_CURVE ( 'NONE', #22125, #10176, #41325, .T. ) ;
#36433=ORIENTED_EDGE ( 'NONE', *, *, #17626, .T. ) ;
#36439=VECTOR ( 'NONE', #63118, 1000.000000000000000 ) ;
#36441=ORIENTED_EDGE ( 'NONE', *, *, #9694, .F. ) ;
#36442=VECTOR ( 'NONE', #2643, 999.9999999999998863 ) ;
#36443=VECTOR ( 'NONE', #8557, 1000.000000000000000 ) ;
#36449=VECTOR ( 'NONE', #57600, 1000.000000000000000 ) ;
#36465=LINE ( 'NONE', #69341, #1913 ) ;
#36474=DIRECTION ( 'NONE',  ( -1.000000000000000000, 3.491481338843132961E-15, 1.836970198721036344E-16 ) ) ;
#36476=FACE_OUTER_BOUND ( 'NONE', #61839, .T. ) ;
#36481=CARTESIAN_POINT ( 'NONE',  ( 6.006483450353379716, -6.006483450353394815, 195.0000000000000284 ) ) ;
#36488=CARTESIAN_POINT ( 'NONE',  ( 6.006483450353379716, -6.006483450353394815, 195.0000000000000284 ) ) ;
#36492=DIRECTION ( 'NONE',  ( -3.491481338843133355E-15, -1.000000000000000000, -1.836970198721029934E-16 ) ) ;
#36494=FACE_OUTER_BOUND ( 'NONE', #3853, .T. ) ;
#36498=CARTESIAN_POINT ( 'NONE',  ( 9.306483450353379538, -10.09643294401465852, 455.0000000000000568 ) ) ;
#36501=ADVANCED_FACE ( 'NONE', ( #31276 ), #9691, .T. ) ;
#36507=EDGE_CURVE ( 'NONE', #391, #27141, #14993, .T. ) ;
#36513=ORIENTED_EDGE ( 'NONE', *, *, #26313, .T. ) ;
#36540=CARTESIAN_POINT ( 'NONE',  ( -8.513516549646713116, 11.29351654964659701, 194.9999952000000292 ) ) ;
#36543=ORIENTED_EDGE ( 'NONE', *, *, #18031, .T. ) ;
#36546=DIRECTION ( 'NONE',  ( 4.121462285523434951E-16, 1.000000000000000000, 3.673940397442059868E-16 ) ) ;
#36549=DIRECTION ( 'NONE',  ( -1.836970198721029934E-16, -1.836970198721010706E-16, 1.000000000000000000 ) ) ;
#36561=CYLINDRICAL_SURFACE ( 'NONE', #35940, 0.1999999999999987899 ) ;
#36564=CARTESIAN_POINT ( 'NONE',  ( 11.48848345035334617, -10.20488345035343336, 195.0000000000000284 ) ) ;
#36569=LINE ( 'NONE', #3350, #49047 ) ;
#36572=LINE ( 'NONE', #10748, #53917 ) ;
#36581=DIRECTION ( 'NONE',  ( -1.000000000000000000, 0.000000000000000000, 0.000000000000000000 ) ) ;
#36596=EDGE_CURVE ( 'NONE', #67938, #53770, #25607, .T. ) ;
#36602=EDGE_CURVE ( 'NONE', #28757, #13195, #31955, .T. ) ;
#36610=AXIS2_PLACEMENT_3D ( 'NONE', #25571, #64109, #36158 ) ;
#36614=ORIENTED_EDGE ( 'NONE', *, *, #11194, .F. ) ;
#36627=CIRCLE ( 'NONE', #6147, 0.3999999999999993006 ) ;
#36629=CARTESIAN_POINT ( 'NONE',  ( 10.20488345035345645, 11.07551654964652954, 455.0000000000000568 ) ) ;
#36642=PLANE ( 'NONE',  #37600 ) ;
#36644=FACE_OUTER_BOUND ( 'NONE', #20586, .T. ) ;
#36649=PLANE ( 'NONE',  #51670 ) ;
#36653=ORIENTED_EDGE ( 'NONE', *, *, #7997, .F. ) ;
#36654=AXIS2_PLACEMENT_3D ( 'NONE', #52034, #35395, #36106 ) ;
#36659=EDGE_CURVE ( 'NONE', #14927, #63906, #52661, .T. ) ;
#36664=PLANE ( 'NONE',  #154 ) ;
#36665=EDGE_CURVE ( 'NONE', #33912, #5044, #22391, .T. ) ;
#36668=ADVANCED_FACE ( 'NONE', ( #37958 ), #64828, .T. ) ;
#36672=CARTESIAN_POINT ( 'NONE',  ( 11.08848345035334404, -9.804883450353528929, 455.0000000000000568 ) ) ;
#36677=EDGE_CURVE ( 'NONE', #37252, #26529, #32647, .T. ) ;
#36679=ORIENTED_EDGE ( 'NONE', *, *, #56120, .F. ) ;
#36680=VECTOR ( 'NONE', #58693, 1000.000000000000000 ) ;
#36681=CARTESIAN_POINT ( 'NONE',  ( -11.07551654964683330, -11.48848345035333907, 455.0000000000000568 ) ) ;
#36682=EDGE_CURVE ( 'NONE', #17779, #51662, #59168, .T. ) ;
#36700=CARTESIAN_POINT ( 'NONE',  ( 7.811466277050736373, -7.272650909786632312, 195.0000000000000284 ) ) ;
#36718=ORIENTED_EDGE ( 'NONE', *, *, #43010, .T. ) ;
#36726=ORIENTED_EDGE ( 'NONE', *, *, #41853, .F. ) ;
#36737=EDGE_CURVE ( 'NONE', #4384, #43288, #10903, .T. ) ;
#36741=VECTOR ( 'NONE', #65027, 1000.000000000000000 ) ;
#36743=LINE ( 'NONE', #42037, #36449 ) ;
#36745=CARTESIAN_POINT ( 'NONE',  ( -11.11351654964671098, 7.793516549646603231, 455.0000000000000568 ) ) ;
#36760=ORIENTED_EDGE ( 'NONE', *, *, #37152, .F. ) ;
#36775=ORIENTED_EDGE ( 'NONE', *, *, #16896, .F. ) ;
#36778=ORIENTED_EDGE ( 'NONE', *, *, #34510, .T. ) ;
#36782=CARTESIAN_POINT ( 'NONE',  ( -8.393516549646712122, 6.331612867284047041, 455.0000000000000568 ) ) ;
#36787=ORIENTED_EDGE ( 'NONE', *, *, #69806, .T. ) ;
#36800=ORIENTED_EDGE ( 'NONE', *, *, #51811, .F. ) ;
#36812=VECTOR ( 'NONE', #49896, 1000.000000000000000 ) ;
#36827=CARTESIAN_POINT ( 'NONE',  ( -11.47551654964682122, -10.20488345035336941, 455.0000000000000568 ) ) ;
#36831=DIRECTION ( 'NONE',  ( -1.000000000000000000, 0.000000000000000000, 0.000000000000000000 ) ) ;
#36833=DIRECTION ( 'NONE',  ( -0.7671651518152962090, 0.6414496315691619044, 0.000000000000000000 ) ) ;
#36835=DIRECTION ( 'NONE',  ( 1.000000000000000000, -3.491481338843132961E-15, 0.000000000000000000 ) ) ;
#36840=EDGE_LOOP ( 'NONE', ( #31806, #7351, #31427, #42244 ) ) ;
#36858=CIRCLE ( 'NONE', #17645, 1.399999999999999245 ) ;
#36861=CARTESIAN_POINT ( 'NONE',  ( -10.73351654964671198, 1.077516549646603483, 455.0000000000000568 ) ) ;
#36878=EDGE_CURVE ( 'NONE', #40309, #41587, #24811, .T. ) ;
#36884=CARTESIAN_POINT ( 'NONE',  ( -7.798499376344062206, -4.740315990920112021, 195.0000000000000284 ) ) ;
#36885=LINE ( 'NONE', #14257, #53585 ) ;
#36891=CARTESIAN_POINT ( 'NONE',  ( -5.655420232009250370, 8.393516549646600211, 455.0000000000000568 ) ) ;
#36896=VECTOR ( 'NONE', #65194, 1000.000000000000000 ) ;
#36897=ORIENTED_EDGE ( 'NONE', *, *, #54086, .F. ) ;
#36907=ORIENTED_EDGE ( 'NONE', *, *, #24974, .T. ) ;
#36910=VECTOR ( 'NONE', #38161, 1000.000000000000000 ) ;
#36915=CARTESIAN_POINT ( 'NONE',  ( 5.393625297349900372, -7.265214908726134624, 195.0000000000000284 ) ) ;
#36930=CARTESIAN_POINT ( 'NONE',  ( -3.593516549646742497, -7.428221114745029219, 195.0000000000000284 ) ) ;
#36937=DIRECTION ( 'NONE',  ( 0.7071067811865411334, -0.7071067811865539010, -2.597868168706484541E-16 ) ) ;
#36945=DIRECTION ( 'NONE',  ( -0.7071067811865550112, -0.7071067811865401342, 0.000000000000000000 ) ) ;
#36948=CYLINDRICAL_SURFACE ( 'NONE', #19544, 0.1999999999999987899 ) ;
#36950=CARTESIAN_POINT ( 'NONE',  ( 6.006483450353379716, -6.006483450353490738, 455.0000000000000568 ) ) ;
#36951=CARTESIAN_POINT ( 'NONE',  ( -11.31351654964669784, -4.406483450353282372, 195.0000000000000284 ) ) ;
#36952=AXIS2_PLACEMENT_3D ( 'NONE', #48381, #21503, #21169 ) ;
#36957=DIRECTION ( 'NONE',  ( 0.5000000000000004441, -0.8660254037844382635, 0.000000000000000000 ) ) ;
#36964=DIRECTION ( 'NONE',  ( 1.280238727658158432E-15, 1.000000000000000000, -0.000000000000000000 ) ) ;
#36971=FACE_OUTER_BOUND ( 'NONE', #48898, .T. ) ;
#36972=LINE ( 'NONE', #33383, #62362 ) ;
#36974=EDGE_LOOP ( 'NONE', ( #61019, #24469, #45996, #39464 ) ) ;
#36975=ADVANCED_FACE ( 'NONE', ( #14907 ), #68993, .F. ) ;
#36976=ORIENTED_EDGE ( 'NONE', *, *, #6814, .T. ) ;
#36977=DIRECTION ( 'NONE',  ( 3.717264591378875951E-15, 1.000000000000000000, 0.000000000000000000 ) ) ;
#36981=ORIENTED_EDGE ( 'NONE', *, *, #56592, .F. ) ;
#36983=CARTESIAN_POINT ( 'NONE',  ( -7.793516549646781755, -11.12648345035335851, 195.0000000000000284 ) ) ;
#36992=DIRECTION ( 'NONE',  ( 0.7071067811865474617, -0.7071067811865474617, 0.000000000000000000 ) ) ;
#37001=VERTEX_POINT ( 'NONE', #47082 ) ;
#37007=DIRECTION ( 'NONE',  ( 0.000000000000000000, 0.000000000000000000, 1.000000000000000000 ) ) ;
#37008=EDGE_CURVE ( 'NONE', #40597, #29083, #36465, .T. ) ;
#37012=DIRECTION ( 'NONE',  ( 0.000000000000000000, -1.000000000000000000, 0.000000000000000000 ) ) ;
#37013=DIRECTION ( 'NONE',  ( 0.7671651518153029814, 0.6414496315691537998, 0.000000000000000000 ) ) ;
#37020=ADVANCED_FACE ( 'NONE', ( #15259 ), #52755, .F. ) ;
#37032=VERTEX_POINT ( 'NONE', #54137 ) ;
#37039=EDGE_LOOP ( 'NONE', ( #1618, #65512, #46822, #66286 ) ) ;
#37049=VERTEX_POINT ( 'NONE', #387 ) ;
#37051=DIRECTION ( 'NONE',  ( 0.000000000000000000, -1.000000000000000000, 0.000000000000000000 ) ) ;
#37054=PLANE ( 'NONE',  #49693 ) ;
#37057=EDGE_LOOP ( 'NONE', ( #38688, #23006, #69913, #37339 ) ) ;
#37058=EDGE_LOOP ( 'NONE', ( #60494, #20882, #69304, #23907 ) ) ;
#37061=CIRCLE ( 'NONE', #6410, 0.1999999999999996503 ) ;
#37062=DIRECTION ( 'NONE',  ( 8.673617379884051249E-15, 1.000000000000000000, 0.000000000000000000 ) ) ;
#37063=DIRECTION ( 'NONE',  ( -0.7071067811865391350, 0.7071067811865560104, 1.750285133459120294E-30 ) ) ;
#37064=EDGE_CURVE ( 'NONE', #40926, #35986, #56114, .T. ) ;
#37074=CARTESIAN_POINT ( 'NONE',  ( 11.48848345035334617, -11.08848345035349148, 455.0000000000000568 ) ) ;
#37076=EDGE_LOOP ( 'NONE', ( #27722, #57133, #35255, #52208 ) ) ;
#37078=EDGE_LOOP ( 'NONE', ( #28826, #3459, #32437, #18188 ) ) ;
#37081=ORIENTED_EDGE ( 'NONE', *, *, #60929, .F. ) ;
#37092=ORIENTED_EDGE ( 'NONE', *, *, #19130, .F. ) ;
#37095=CARTESIAN_POINT ( 'NONE',  ( -11.47551654964667733, 10.19191654964664018, 195.0000000000000284 ) ) ;
#37100=CARTESIAN_POINT ( 'NONE',  ( -10.19191654964671301, 11.47551654964660450, 455.0000000000000568 ) ) ;
#37105=DIRECTION ( 'NONE',  ( 1.000000000000000000, 0.000000000000000000, 0.000000000000000000 ) ) ;
#37111=LINE ( 'NONE', #4238, #6213 ) ;
#37119=CARTESIAN_POINT ( 'NONE',  ( 8.406483450353379183, -6.344579767990935260, 455.0000000000000568 ) ) ;
#37125=FACE_OUTER_BOUND ( 'NONE', #10679, .T. ) ;
#37145=CARTESIAN_POINT ( 'NONE',  ( -8.393516549646722780, -5.668387132715892562, 195.0000000000000284 ) ) ;
#37149=ORIENTED_EDGE ( 'NONE', *, *, #33297, .T. ) ;
#37152=EDGE_CURVE ( 'NONE', #14703, #38244, #59082, .T. ) ;
#37157=EDGE_CURVE ( 'NONE', #26529, #56381, #17324, .T. ) ;
#37159=VECTOR ( 'NONE', #58834, 1000.000000000000000 ) ;
#37160=DIRECTION ( 'NONE',  ( 1.000000000000000000, 0.000000000000000000, 0.000000000000000000 ) ) ;
#37167=CIRCLE ( 'NONE', #6652, 0.5999999999999998668 ) ;
#37177=VERTEX_POINT ( 'NONE', #8724 ) ;
#37185=LINE ( 'NONE', #5362, #31673 ) ;
#37186=CARTESIAN_POINT ( 'NONE',  ( -9.942044687070527687, -2.765062094115999347, 195.0000000000000284 ) ) ;
#37190=( LENGTH_UNIT ( ) NAMED_UNIT ( * ) SI_UNIT ( .MILLI., .METRE. ) );
#37200=CIRCLE ( 'NONE', #22501, 0.3999999999999993006 ) ;
#37201=DIRECTION ( 'NONE',  ( -1.000000000000000000, 0.000000000000000000, 0.000000000000000000 ) ) ;
#37204=LINE ( 'NONE', #50131, #64832 ) ;
#37206=LINE ( 'NONE', #48158, #13518 ) ;
#37207=VERTEX_POINT ( 'NONE', #46190 ) ;
#37210=LINE ( 'NONE', #9277, #66356 ) ;
#37216=ORIENTED_EDGE ( 'NONE', *, *, #55114, .F. ) ;
#37220=EDGE_CURVE ( 'NONE', #34688, #391, #46893, .T. ) ;
#37221=DIRECTION ( 'NONE',  ( 1.836970198721029934E-16, 1.836970198721010706E-16, -1.000000000000000000 ) ) ;
#37225=CYLINDRICAL_SURFACE ( 'NONE', #5162, 0.1999999999999996503 ) ;
#37245=DIRECTION ( 'NONE',  ( -1.047444401652940007E-14, -1.000000000000000000, -1.836970198721029934E-16 ) ) ;
#37250=CARTESIAN_POINT ( 'NONE',  ( -11.11351654964680336, -9.106483450353373144, 455.0000000000000568 ) ) ;
#37252=VERTEX_POINT ( 'NONE', #25336 ) ;
#37254=ORIENTED_EDGE ( 'NONE', *, *, #27325, .F. ) ;
#37255=DIRECTION ( 'NONE',  ( -0.000000000000000000, -0.000000000000000000, 1.000000000000000000 ) ) ;
#37257=ORIENTED_EDGE ( 'NONE', *, *, #19561, .F. ) ;
#37260=CARTESIAN_POINT ( 'NONE',  ( -11.07551654964678711, -11.48848345035328933, 195.0000000000000284 ) ) ;
#37264=VECTOR ( 'NONE', #50222, 1000.000000000000000 ) ;
#37268=FACE_BOUND ( 'NONE', #23085, .T. ) ;
#37269=VECTOR ( 'NONE', #9274, 1000.000000000000000 ) ;
#37272=DIRECTION ( 'NONE',  ( -0.000000000000000000, -0.000000000000000000, -1.000000000000000000 ) ) ;
#37276=CARTESIAN_POINT ( 'NONE',  ( 4.206483450353341702, -11.32648345035347504, 455.0000000000000568 ) ) ;
#37285=CARTESIAN_POINT ( 'NONE',  ( 1.690483450353351458, -9.841277389592800517, 455.0000000000000568 ) ) ;
#37289=ORIENTED_EDGE ( 'NONE', *, *, #48084, .F. ) ;
#37290=PLANE ( 'NONE',  #7326 ) ;
#37298=ORIENTED_EDGE ( 'NONE', *, *, #52172, .F. ) ;
#37299=EDGE_CURVE ( 'NONE', #32112, #16139, #43760, .T. ) ;
#37301=DIRECTION ( 'NONE',  ( -0.000000000000000000, 3.673940397442059868E-16, -1.000000000000000000 ) ) ;
#37302=DIRECTION ( 'NONE',  ( -0.8660254037844510311, -0.4999999999999785727, 0.000000000000000000 ) ) ;
#37313=ORIENTED_EDGE ( 'NONE', *, *, #49079, .F. ) ;
#37326=AXIS2_PLACEMENT_3D ( 'NONE', #24614, #56425, #2338 ) ;
#37328=ORIENTED_EDGE ( 'NONE', *, *, #10872, .T. ) ;
#37329=ORIENTED_EDGE ( 'NONE', *, *, #43353, .T. ) ;
#37337=AXIS2_PLACEMENT_3D ( 'NONE', #48196, #28600, #5055 ) ;
#37339=ORIENTED_EDGE ( 'NONE', *, *, #25741, .T. ) ;
#37341=DIRECTION ( 'NONE',  ( 3.491481338843132961E-15, 1.000000000000000000, 1.836970198721029934E-16 ) ) ;
#37346=CARTESIAN_POINT ( 'NONE',  ( 12.00648345035340903, 7.813516549646560172, 455.0000000000000568 ) ) ;
#37347=DIRECTION ( 'NONE',  ( 0.7071067811865451302, -0.7071067811865500152, -2.597868168706484048E-16 ) ) ;
#37349=EDGE_CURVE ( 'NONE', #54143, #28681, #31320, .T. ) ;
#37353=FACE_OUTER_BOUND ( 'NONE', #54513, .T. ) ;
#37355=EDGE_CURVE ( 'NONE', #54387, #50275, #63871, .T. ) ;
#37360=DIRECTION ( 'NONE',  ( -0.000000000000000000, -0.000000000000000000, -1.000000000000000000 ) ) ;
#37361=DIRECTION ( 'NONE',  ( 1.000000000000000000, -2.990116172375847553E-15, -1.836970198721035357E-16 ) ) ;
#37363=DIRECTION ( 'NONE',  ( 1.000000000000000000, 0.000000000000000000, 0.000000000000000000 ) ) ;
#37373=DIRECTION ( 'NONE',  ( -2.135044278125299371E-15, 1.000000000000000000, -0.000000000000000000 ) ) ;
#37386=CARTESIAN_POINT ( 'NONE',  ( -3.593516549646712299, 4.609516549646604844, 195.0000000000000284 ) ) ;
#37388=ORIENTED_EDGE ( 'NONE', *, *, #29459, .F. ) ;
#37395=CARTESIAN_POINT ( 'NONE',  ( -5.993516549646711766, 5.993516549646603409, 195.0000000000000284 ) ) ;
#37397=ADVANCED_FACE ( 'NONE', ( #53965 ), #47602, .T. ) ;
#37403=CARTESIAN_POINT ( 'NONE',  ( 11.78648345035337819, -7.606483450353493936, 455.0000000000000568 ) ) ;
#37406=ORIENTED_EDGE ( 'NONE', *, *, #41654, .F. ) ;
#37407=CIRCLE ( 'NONE', #15955, 1.399999999999998579 ) ;
#37414=ORIENTED_EDGE ( 'NONE', *, *, #41599, .F. ) ;
#37423=ORIENTED_EDGE ( 'NONE', *, *, #21992, .F. ) ;
#37428=FACE_OUTER_BOUND ( 'NONE', #40150, .T. ) ;
#37431=CARTESIAN_POINT ( 'NONE',  ( 2.906483450353420928, 11.11351654964658842, 455.0000000000000568 ) ) ;
#37435=DIRECTION ( 'NONE',  ( -2.891205793294683355E-15, -1.000000000000000000, 0.000000000000000000 ) ) ;
#37437=DIRECTION ( 'NONE',  ( 0.000000000000000000, -1.000000000000000000, 0.000000000000000000 ) ) ;
#37439=CARTESIAN_POINT ( 'NONE',  ( 11.32648345035337911, 4.193516549646524538, 455.0000000000000568 ) ) ;
#37442=DIRECTION ( 'NONE',  ( 0.000000000000000000, -3.673940397442059868E-16, 1.000000000000000000 ) ) ;
#37446=EDGE_LOOP ( 'NONE', ( #52051, #53560, #44157, #38179 ) ) ;
#37448=AXIS2_PLACEMENT_3D ( 'NONE', #55159, #7391, #6703 ) ;
#37452=EDGE_CURVE ( 'NONE', #61368, #51358, #21158, .T. ) ;
#37457=EDGE_LOOP ( 'NONE', ( #58355, #32972, #23891, #52890 ) ) ;
#37461=LINE ( 'NONE', #54418, #3025 ) ;
#37471=CARTESIAN_POINT ( 'NONE',  ( -9.942044687070573872, -2.765062094116046865, 455.0000000000000568 ) ) ;
#37472=CIRCLE ( 'NONE', #25043, 0.1999999999999992339 ) ;
#37478=ORIENTED_EDGE ( 'NONE', *, *, #7030, .F. ) ;
#37481=DIRECTION ( 'NONE',  ( 1.047444401652939849E-14, 1.000000000000000000, 1.836970198721029934E-16 ) ) ;
#37485=ADVANCED_FACE ( 'NONE', ( #64568 ), #53615, .F. ) ;
#37489=CARTESIAN_POINT ( 'NONE',  ( 10.20488345035340849, 11.47551654964657786, 195.0000000000000284 ) ) ;
#37495=VERTEX_POINT ( 'NONE', #6207 ) ;
#37497=EDGE_CURVE ( 'NONE', #30184, #43815, #11494, .T. ) ;
#37507=ORIENTED_EDGE ( 'NONE', *, *, #31773, .F. ) ;
#37509=DIRECTION ( 'NONE',  ( -1.836970198721029934E-16, 1.836970198721036344E-16, -1.000000000000000000 ) ) ;
#37512=VECTOR ( 'NONE', #41636, 1000.000000000000000 ) ;
#37513=PLANE ( 'NONE',  #24466 ) ;
#37527=DIRECTION ( 'NONE',  ( -1.000000000000000000, 0.000000000000000000, 0.000000000000000000 ) ) ;
#37533=LINE ( 'NONE', #32223, #63801 ) ;
#37538=DIRECTION ( 'NONE',  ( -1.000000000000000000, 0.000000000000000000, 0.000000000000000000 ) ) ;
#37540=ORIENTED_EDGE ( 'NONE', *, *, #987, .F. ) ;
#37550=ORIENTED_EDGE ( 'NONE', *, *, #2890, .T. ) ;
#37563=ORIENTED_EDGE ( 'NONE', *, *, #10739, .F. ) ;
#37588=CARTESIAN_POINT ( 'NONE',  ( -11.07551654964667520, 11.07551654964660237, 455.0000000000000568 ) ) ;
#37589=VERTEX_POINT ( 'NONE', #2630 ) ;
#37594=CARTESIAN_POINT ( 'NONE',  ( 3.606483450353397568, 4.609516549646590633, 455.0000000000000568 ) ) ;
#37600=AXIS2_PLACEMENT_3D ( 'NONE', #41950, #9784, #47604 ) ;
#37615=DIRECTION ( 'NONE',  ( 0.000000000000000000, -1.000000000000000000, 0.000000000000000000 ) ) ;
#37628=ORIENTED_EDGE ( 'NONE', *, *, #60101, .T. ) ;
#37631=EDGE_CURVE ( 'NONE', #30523, #32112, #35861, .T. ) ;
#37633=ORIENTED_EDGE ( 'NONE', *, *, #33939, .T. ) ;
#37634=LINE ( 'NONE', #26670, #9029 ) ;
#37655=CARTESIAN_POINT ( 'NONE',  ( -11.77351654964670935, 4.393516549646602876, 195.0000000000000284 ) ) ;
#37656=ORIENTED_EDGE ( 'NONE', *, *, #47137, .F. ) ;
#37657=ORIENTED_EDGE ( 'NONE', *, *, #21505, .T. ) ;
#37660=FACE_OUTER_BOUND ( 'NONE', #21019, .T. ) ;
#37666=ORIENTED_EDGE ( 'NONE', *, *, #24267, .T. ) ;
#37668=VECTOR ( 'NONE', #55533, 1000.000000000000000 ) ;
#37673=ORIENTED_EDGE ( 'NONE', *, *, #16110, .T. ) ;
#37685=EDGE_LOOP ( 'NONE', ( #25955, #51317, #56344, #9662 ) ) ;
#37688=CARTESIAN_POINT ( 'NONE',  ( 11.32648345035333293, 4.193516549646572500, 195.0000000000000284 ) ) ;
#37691=AXIS2_PLACEMENT_3D ( 'NONE', #28463, #7939, #39423 ) ;
#37693=ADVANCED_FACE ( 'NONE', ( #19949 ), #45408, .T. ) ;
#37720=VECTOR ( 'NONE', #44574, 1000.000000000000000 ) ;
#37723=DIRECTION ( 'NONE',  ( -0.7071067811865474617, -0.7071067811865474617, 0.000000000000000000 ) ) ;
#37729=CARTESIAN_POINT ( 'NONE',  ( -6.606374702650169795, 4.734785091273855606, 455.0000000000000568 ) ) ;
#37743=AXIS2_PLACEMENT_3D ( 'NONE', #35879, #41878, #13951 ) ;
#37745=ADVANCED_FACE ( 'NONE', ( #58129 ), #69439, .F. ) ;
#37751=CIRCLE ( 'NONE', #7229, 0.3999999999999993006 ) ;
#37754=ORIENTED_EDGE ( 'NONE', *, *, #60274, .F. ) ;
#37762=VERTEX_POINT ( 'NONE', #36207 ) ;
#37764=AXIS2_PLACEMENT_3D ( 'NONE', #12658, #39540, #21910 ) ;
#37765=AXIS2_PLACEMENT_3D ( 'NONE', #10674, #32242, #11027 ) ;
#37779=DIRECTION ( 'NONE',  ( -0.000000000000000000, 3.673940397442059868E-16, -1.000000000000000000 ) ) ;
#37789=CARTESIAN_POINT ( 'NONE',  ( 7.606483450353376696, 11.77351654964662053, 195.0000000000000284 ) ) ;
#37791=VERTEX_POINT ( 'NONE', #41517 ) ;
#37792=FACE_OUTER_BOUND ( 'NONE', #47979, .T. ) ;
#37793=EDGE_CURVE ( 'NONE', #33976, #55193, #32312, .T. ) ;
#37794=CARTESIAN_POINT ( 'NONE',  ( -2.693516549646675529, 10.91351654964657314, 455.0000000000000568 ) ) ;
#37801=AXIS2_PLACEMENT_3D ( 'NONE', #29954, #3099, #4503 ) ;
#37804=CARTESIAN_POINT ( 'NONE',  ( 6.344579767990823349, -8.406483450353491094, 455.0000000000000568 ) ) ;
#37812=PLANE ( 'NONE',  #31812 ) ;
#37822=CARTESIAN_POINT ( 'NONE',  ( 3.606483450353350051, 4.609516549646638595, 195.0000000000000284 ) ) ;
#37825=DIRECTION ( 'NONE',  ( -3.491481338843133355E-15, -1.000000000000000000, -1.836970198721029934E-16 ) ) ;
#37829=ORIENTED_EDGE ( 'NONE', *, *, #10525, .T. ) ;
#37838=VERTEX_POINT ( 'NONE', #21354 ) ;
#37846=EDGE_LOOP ( 'NONE', ( #36614, #25855, #27979, #41447 ) ) ;
#37848=DIRECTION ( 'NONE',  ( 0.000000000000000000, 3.673940397442059868E-16, -1.000000000000000000 ) ) ;
#37854=EDGE_CURVE ( 'NONE', #56381, #41426, #17809, .T. ) ;
#37875=EDGE_CURVE ( 'NONE', #68313, #15525, #848, .T. ) ;
#37877=ORIENTED_EDGE ( 'NONE', *, *, #36507, .T. ) ;
#37881=CARTESIAN_POINT ( 'NONE',  ( -4.383466043307859827, 8.393516549646589553, 455.0000000000000568 ) ) ;
#37888=CARTESIAN_POINT ( 'NONE',  ( -4.193516549646833624, -11.32648345035344128, 455.0000000000000568 ) ) ;
#37889=CARTESIAN_POINT ( 'NONE',  ( -7.839518282750262301, 3.417780618358531530, 455.0000000000000568 ) ) ;
#37893=CARTESIAN_POINT ( 'NONE',  ( -9.293516549646710700, 10.91351654964659801, 455.0000000000000568 ) ) ;
#37901=VERTEX_POINT ( 'NONE', #54578 ) ;
#37902=LINE ( 'NONE', #23010, #22314 ) ;
#37914=AXIS2_PLACEMENT_3D ( 'NONE', #34976, #26483, #5615 ) ;
#37920=VECTOR ( 'NONE', #20455, 1000.000000000000000 ) ;
#37921=VECTOR ( 'NONE', #47991, 1000.000000000000000 ) ;
#37935=ORIENTED_EDGE ( 'NONE', *, *, #33168, .T. ) ;
#37940=CARTESIAN_POINT ( 'NONE',  ( 9.955011587777235604, -2.765062094116086833, 195.0000000000000284 ) ) ;
#37942=ORIENTED_EDGE ( 'NONE', *, *, #10973, .T. ) ;
#37943=ORIENTED_EDGE ( 'NONE', *, *, #31010, .F. ) ;
#37944=DIRECTION ( 'NONE',  ( 0.000000000000000000, 1.000000000000000000, 0.000000000000000000 ) ) ;
#37953=ORIENTED_EDGE ( 'NONE', *, *, #38752, .F. ) ;
#37956=DIRECTION ( 'NONE',  ( -0.6414496315691494699, 0.7671651518153064231, 2.818519042764025305E-16 ) ) ;
#37958=FACE_OUTER_BOUND ( 'NONE', #59227, .T. ) ;
#37963=EDGE_LOOP ( 'NONE', ( #64100, #16212, #64200, #16324 ) ) ;
#37964=AXIS2_PLACEMENT_3D ( 'NONE', #49920, #17392, #29048 ) ;
#37985=CYLINDRICAL_SURFACE ( 'NONE', #63745, 0.1999999999999996503 ) ;
#37988=LINE ( 'NONE', #31986, #12712 ) ;
#37992=LINE ( 'NONE', #54252, #2960 ) ;
#38001=VERTEX_POINT ( 'NONE', #2204 ) ;
#38007=ORIENTED_EDGE ( 'NONE', *, *, #6254, .F. ) ;
#38010=VECTOR ( 'NONE', #22294, 1000.000000000000000 ) ;
#38013=ADVANCED_FACE ( 'NONE', ( #56297 ), #34721, .F. ) ;
#38021=EDGE_CURVE ( 'NONE', #35023, #8790, #35063, .T. ) ;
#38027=ORIENTED_EDGE ( 'NONE', *, *, #2562, .F. ) ;
#38031=CARTESIAN_POINT ( 'NONE',  ( -5.655420232009311654, -8.406483450353382736, 195.0000000000000284 ) ) ;
#38050=LINE ( 'NONE', #43690, #51460 ) ;
#38054=CARTESIAN_POINT ( 'NONE',  ( -11.77351654964670935, 4.173516549646604901, 455.0000000000000568 ) ) ;
#38059=AXIS2_PLACEMENT_3D ( 'NONE', #48032, #10898, #64993 ) ;
#38064=DIRECTION ( 'NONE',  ( 2.990116172375847553E-15, 1.000000000000000000, 0.000000000000000000 ) ) ;
#38067=AXIS2_PLACEMENT_3D ( 'NONE', #5881, #28465, #33778 ) ;
#38082=FACE_OUTER_BOUND ( 'NONE', #21553, .T. ) ;
#38084=ORIENTED_EDGE ( 'NONE', *, *, #28225, .F. ) ;
#38085=VECTOR ( 'NONE', #42379, 1000.000000000000000 ) ;
#38089=ORIENTED_EDGE ( 'NONE', *, *, #45409, .F. ) ;
#38100=CYLINDRICAL_SURFACE ( 'NONE', #58471, 0.5999999999999998668 ) ;
#38103=EDGE_CURVE ( 'NONE', #3732, #8019, #55488, .T. ) ;
#38105=CARTESIAN_POINT ( 'NONE',  ( 7.272650909786644746, 7.798499376343933420, 455.0000000000000568 ) ) ;
#38109=ORIENTED_EDGE ( 'NONE', *, *, #44894, .F. ) ;
#38113=VECTOR ( 'NONE', #57165, 1000.000000000000000 ) ;
#38114=VECTOR ( 'NONE', #45840, 1000.000000000000000 ) ;
#38116=EDGE_CURVE ( 'NONE', #40247, #39974, #60425, .T. ) ;
#38125=ORIENTED_EDGE ( 'NONE', *, *, #23078, .F. ) ;
#38128=DIRECTION ( 'NONE',  ( 8.359604446858500663E-15, 1.000000000000000000, 3.673940397442059868E-16 ) ) ;
#38136=ORIENTED_EDGE ( 'NONE', *, *, #15164, .F. ) ;
#38137=ORIENTED_EDGE ( 'NONE', *, *, #12904, .T. ) ;
#38139=LINE ( 'NONE', #59690, #60087 ) ;
#38141=CARTESIAN_POINT ( 'NONE',  ( -2.893516549646780511, -10.92648345035340895, 195.0000000000000284 ) ) ;
#38147=CARTESIAN_POINT ( 'NONE',  ( 7.806483450353418618, 11.11351654964657421, 455.0000000000000568 ) ) ;
#38148=ORIENTED_EDGE ( 'NONE', *, *, #24968, .F. ) ;
#38152=DIRECTION ( 'NONE',  ( -1.836970198721029934E-16, -1.836970198721010706E-16, 1.000000000000000000 ) ) ;
#38153=EDGE_CURVE ( 'NONE', #11172, #45635, #17856, .T. ) ;
#38161=DIRECTION ( 'NONE',  ( -0.000000000000000000, -0.000000000000000000, -1.000000000000000000 ) ) ;
#38169=CARTESIAN_POINT ( 'NONE',  ( -1.677516549646676625, 10.73351654964656987, 455.0000000000000568 ) ) ;
#38175=CARTESIAN_POINT ( 'NONE',  ( -11.11351654964671098, 4.193516549646605363, 455.0000000000000568 ) ) ;
#38179=ORIENTED_EDGE ( 'NONE', *, *, #52161, .T. ) ;
#38182=DIRECTION ( 'NONE',  ( -1.000000000000000000, 0.000000000000000000, 0.000000000000000000 ) ) ;
#38187=LINE ( 'NONE', #33881, #42839 ) ;
#38188=DIRECTION ( 'NONE',  ( 0.7671651518153106419, -0.6414496315691445849, 0.000000000000000000 ) ) ;
#38193=CARTESIAN_POINT ( 'NONE',  ( 2.706483450353343478, -10.92648345035346225, 455.0000000000000568 ) ) ;
#38207=VERTEX_POINT ( 'NONE', #6359 ) ;
#38209=DIRECTION ( 'NONE',  ( -0.7071067811865500152, -0.7071067811865451302, 4.361490581750786694E-31 ) ) ;
#38213=CARTESIAN_POINT ( 'NONE',  ( 11.12648345035338160, 4.193516549646526315, 455.0000000000000568 ) ) ;
#38216=VECTOR ( 'NONE', #57981, 1000.000000000000000 ) ;
#38219=DIRECTION ( 'NONE',  ( -1.000000000000000000, 0.000000000000000000, 0.000000000000000000 ) ) ;
#38229=DIRECTION ( 'NONE',  ( -0.000000000000000000, -0.000000000000000000, -1.000000000000000000 ) ) ;
#38231=DIRECTION ( 'NONE',  ( -0.7071067811865474617, 0.7071067811865474617, -0.000000000000000000 ) ) ;
#38237=EDGE_CURVE ( 'NONE', #30268, #17336, #6689, .T. ) ;
#38238=CARTESIAN_POINT ( 'NONE',  ( -7.798499376344067535, 4.727349090213367688, 455.0000000000000568 ) ) ;
#38244=VERTEX_POINT ( 'NONE', #6008 ) ;
#38249=ORIENTED_EDGE ( 'NONE', *, *, #7935, .T. ) ;
#38264=CARTESIAN_POINT ( 'NONE',  ( 11.08848345035334404, -9.804883450353528929, 455.0000000000000568 ) ) ;
#38266=CYLINDRICAL_SURFACE ( 'NONE', #43254, 0.2000000000000005107 ) ;
#38274=ORIENTED_EDGE ( 'NONE', *, *, #36177, .F. ) ;
#38281=CARTESIAN_POINT ( 'NONE',  ( 11.78648345035337819, -4.406483450353490205, 455.0000000000000568 ) ) ;
#38288=LINE ( 'NONE', #37594, #51227 ) ;
#38295=DIRECTION ( 'NONE',  ( 3.717264591378875951E-15, 1.000000000000000000, 0.000000000000000000 ) ) ;
#38303=DIRECTION ( 'NONE',  ( -1.000000000000000000, 1.047444401652940007E-14, -1.836970198721010706E-16 ) ) ;
#38307=PLANE ( 'NONE',  #10156 ) ;
#38308=VERTEX_POINT ( 'NONE', #56181 ) ;
#38315=CARTESIAN_POINT ( 'NONE',  ( -8.593516549646711411, 4.383466043307770121, 195.0000000000000284 ) ) ;
#38317=CARTESIAN_POINT ( 'NONE',  ( 7.265214908726123078, -6.619341603356865278, 195.0000000000000284 ) ) ;
#38318=EDGE_CURVE ( 'NONE', #20859, #40401, #43855, .T. ) ;
#38328=EDGE_LOOP ( 'NONE', ( #8838, #27282, #6205, #1730, #10309, #10886, #18388, #36171 ) ) ;
#38337=ADVANCED_FACE ( 'NONE', ( #45204 ), #24347, .F. ) ;
#38352=LINE ( 'NONE', #6170, #8415 ) ;
#38358=ORIENTED_EDGE ( 'NONE', *, *, #32377, .T. ) ;
#38361=DIRECTION ( 'NONE',  ( 3.491481338843132961E-15, 1.000000000000000000, 1.836970198721029934E-16 ) ) ;
#38363=EDGE_CURVE ( 'NONE', #43836, #66768, #23989, .T. ) ;
#38367=ORIENTED_EDGE ( 'NONE', *, *, #14636, .F. ) ;
#38370=CARTESIAN_POINT ( 'NONE',  ( 10.09643294401448621, 2.893516549646583780, 195.0000000000000284 ) ) ;
#38373=VECTOR ( 'NONE', #49014, 1000.000000000000000 ) ;
#38377=EDGE_LOOP ( 'NONE', ( #12167, #36775, #43331, #31400 ) ) ;
#38383=DIRECTION ( 'NONE',  ( -1.000000000000000000, 3.491481338843133355E-15, 1.836970198721036344E-16 ) ) ;
#38393=LINE ( 'NONE', #64923, #60695 ) ;
#38394=DIRECTION ( 'NONE',  ( 1.000000000000000000, -8.359604446858499085E-15, 0.000000000000000000 ) ) ;
#38395=AXIS2_PLACEMENT_3D ( 'NONE', #28075, #49632, #22761 ) ;
#38398=EDGE_CURVE ( 'NONE', #2080, #48487, #67145, .T. ) ;
#38403=LINE ( 'NONE', #27788, #19524 ) ;
#38418=ORIENTED_EDGE ( 'NONE', *, *, #60101, .F. ) ;
#38420=CARTESIAN_POINT ( 'NONE',  ( -5.380658396643234198, 4.734785091273867152, 455.0000000000000568 ) ) ;
#38421=ADVANCED_FACE ( 'NONE', ( #51943 ), #8434, .F. ) ;
#38426=FACE_OUTER_BOUND ( 'NONE', #26032, .T. ) ;
#38429=EDGE_CURVE ( 'NONE', #47767, #24680, #62531, .T. ) ;
#38434=DIRECTION ( 'NONE',  ( 0.7071067811865447972, -0.7071067811865502373, 0.000000000000000000 ) ) ;
#38436=DIRECTION ( 'NONE',  ( 1.000000000000000000, -8.612436249475772606E-15, -1.836970198721045958E-16 ) ) ;
#38438=CARTESIAN_POINT ( 'NONE',  ( 11.78648345035337996, 4.173516549646518747, 455.0000000000000568 ) ) ;
#38441=EDGE_CURVE ( 'NONE', #10108, #38244, #45568, .T. ) ;
#38444=FACE_OUTER_BOUND ( 'NONE', #61903, .T. ) ;
#38462=EDGE_CURVE ( 'NONE', #56867, #6649, #45933, .T. ) ;
#38465=CARTESIAN_POINT ( 'NONE',  ( -4.193516549646785663, -11.32648345035339510, 195.0000000000000284 ) ) ;
#38475=AXIS2_PLACEMENT_3D ( 'NONE', #49329, #22447, #16095 ) ;
#38478=CARTESIAN_POINT ( 'NONE',  ( -2.993516549646701108, 7.415254214038204061, 195.0000000000000284 ) ) ;
#38487=CARTESIAN_POINT ( 'NONE',  ( -4.734785091274035018, -6.619341603356897252, 455.0000000000000568 ) ) ;
#38499=DIRECTION ( 'NONE',  ( 1.836970198721029934E-16, 1.836970198721010706E-16, -1.000000000000000000 ) ) ;
#38510=CIRCLE ( 'NONE', #33991, 1.399999999999998579 ) ;
#38519=AXIS2_PLACEMENT_3D ( 'NONE', #61970, #23094, #61612 ) ;
#38525=DIRECTION ( 'NONE',  ( 1.836970198721029934E-16, 1.836970198721010706E-16, -1.000000000000000000 ) ) ;
#38528=CARTESIAN_POINT ( 'NONE',  ( -7.839518282750262301, 3.417780618358531530, 195.0000000000000284 ) ) ;
#38529=ORIENTED_EDGE ( 'NONE', *, *, #30829, .T. ) ;
#38538=AXIS2_PLACEMENT_3D ( 'NONE', #10110, #59240, #4118 ) ;
#38546=CARTESIAN_POINT ( 'NONE',  ( -9.293516549646710700, 10.08346604330776941, 455.0000000000000568 ) ) ;
#38561=CIRCLE ( 'NONE', #27316, 0.1999999999999987899 ) ;
#38579=EDGE_CURVE ( 'NONE', #43775, #20610, #36369, .T. ) ;
#38581=DIRECTION ( 'NONE',  ( -1.000000000000000000, 3.491481338843133355E-15, 1.836970198721036344E-16 ) ) ;
#38582=CARTESIAN_POINT ( 'NONE',  ( -11.31351654964671027, 7.593516549646603941, 195.0000000000000284 ) ) ;
#38586=LINE ( 'NONE', #49193, #37264 ) ;
#38596=CARTESIAN_POINT ( 'NONE',  ( 10.20488345035338007, -11.48848345035349361, 455.0000000000000568 ) ) ;
#38597=VERTEX_POINT ( 'NONE', #26732 ) ;
#38599=CIRCLE ( 'NONE', #2441, 0.5999999999999998668 ) ;
#38622=ORIENTED_EDGE ( 'NONE', *, *, #58314, .F. ) ;
#38623=ORIENTED_EDGE ( 'NONE', *, *, #25503, .F. ) ;
#38624=EDGE_CURVE ( 'NONE', #43288, #64892, #921, .T. ) ;
#38647=DIRECTION ( 'NONE',  ( -1.000000000000000000, 0.000000000000000000, 0.000000000000000000 ) ) ;
#38665=ORIENTED_EDGE ( 'NONE', *, *, #6641, .F. ) ;
#38669=AXIS2_PLACEMENT_3D ( 'NONE', #40551, #7675, #45502 ) ;
#38676=CARTESIAN_POINT ( 'NONE',  ( 10.92648345035337520, -2.906483450353491094, 455.0000000000000568 ) ) ;
#38677=ORIENTED_EDGE ( 'NONE', *, *, #16153, .T. ) ;
#38688=ORIENTED_EDGE ( 'NONE', *, *, #19561, .T. ) ;
#38689=DIRECTION ( 'NONE',  ( -1.836970198721029934E-16, 1.836970198721036344E-16, -1.000000000000000000 ) ) ;
#38694=ORIENTED_EDGE ( 'NONE', *, *, #1441, .F. ) ;
#38695=ORIENTED_EDGE ( 'NONE', *, *, #8200, .F. ) ;
#38698=DIRECTION ( 'NONE',  ( -0.000000000000000000, -0.000000000000000000, -1.000000000000000000 ) ) ;
#38704=CARTESIAN_POINT ( 'NONE',  ( 10.74648345035329911, 1.077516549646576616, 195.0000000000000284 ) ) ;
#38705=DIRECTION ( 'NONE',  ( -1.836970198721029934E-16, 1.836970198721036344E-16, -1.000000000000000000 ) ) ;
#38706=ORIENTED_EDGE ( 'NONE', *, *, #45193, .T. ) ;
#38709=CARTESIAN_POINT ( 'NONE',  ( -11.47551654964682122, -10.20488345035336941, 455.0000000000000568 ) ) ;
#38733=ADVANCED_FACE ( 'NONE', ( #7220 ), #1246, .F. ) ;
#38737=CARTESIAN_POINT ( 'NONE',  ( -11.77351654964670935, 7.593516549646604830, 455.0000000000000568 ) ) ;
#38741=VERTEX_POINT ( 'NONE', #33753 ) ;
#38750=CARTESIAN_POINT ( 'NONE',  ( -4.173516549646790530, -11.78648345035339595, 195.0000000000000284 ) ) ;
#38752=EDGE_CURVE ( 'NONE', #46347, #52260, #23501, .T. ) ;
#38759=VECTOR ( 'NONE', #55109, 1000.000000000000000 ) ;
#38764=AXIS2_PLACEMENT_3D ( 'NONE', #3852, #20117, #63251 ) ;
#38768=FACE_OUTER_BOUND ( 'NONE', #21401, .T. ) ;
#38771=PLANE ( 'NONE',  #15784 ) ;
#38778=ORIENTED_EDGE ( 'NONE', *, *, #22041, .T. ) ;
#38783=CARTESIAN_POINT ( 'NONE',  ( 7.428221114744993692, 2.993516549646566105, 455.0000000000000568 ) ) ;
#38793=VECTOR ( 'NONE', #57698, 1000.000000000000000 ) ;
#38795=CARTESIAN_POINT ( 'NONE',  ( -3.417780618358626565, 7.839518282750134404, 195.0000000000000284 ) ) ;
#38805=EDGE_CURVE ( 'NONE', #39788, #37177, #14527, .T. ) ;
#38807=EDGE_CURVE ( 'NONE', #24754, #49618, #30908, .T. ) ;
#38818=CARTESIAN_POINT ( 'NONE',  ( 7.811466277050697293, 4.727349090213374794, 195.0000000000000284 ) ) ;
#38826=CARTESIAN_POINT ( 'NONE',  ( -7.813516549646791098, -12.00648345035336284, 195.0000000000000284 ) ) ;
#38839=LINE ( 'NONE', #60065, #17484 ) ;
#38841=ORIENTED_EDGE ( 'NONE', *, *, #62602, .T. ) ;
#38843=ORIENTED_EDGE ( 'NONE', *, *, #35773, .T. ) ;
#38848=VECTOR ( 'NONE', #7678, 1000.000000000000000 ) ;
#38859=LINE ( 'NONE', #2074, #32004 ) ;
#38861=ORIENTED_EDGE ( 'NONE', *, *, #51134, .T. ) ;
#38863=EDGE_CURVE ( 'NONE', #11813, #23831, #47176, .T. ) ;
#38886=ORIENTED_EDGE ( 'NONE', *, *, #30576, .F. ) ;
#38891=CARTESIAN_POINT ( 'NONE',  ( 11.12648345035337627, -2.906483450353395614, 195.0000000000000284 ) ) ;
#38895=EDGE_CURVE ( 'NONE', #17706, #52264, #14300, .T. ) ;
#38896=EDGE_CURVE ( 'NONE', #64033, #62061, #13936, .T. ) ;
#38900=LINE ( 'NONE', #33927, #6692 ) ;
#38905=AXIS2_PLACEMENT_3D ( 'NONE', #50736, #4071, #51446 ) ;
#38912=LINE ( 'NONE', #22658, #67011 ) ;
#38915=DIRECTION ( 'NONE',  ( 0.000000000000000000, 0.000000000000000000, 1.000000000000000000 ) ) ;
#38921=LINE ( 'NONE', #66820, #24064 ) ;
#38928=CARTESIAN_POINT ( 'NONE',  ( 8.406483450353379183, -4.396432944014657451, 455.0000000000000568 ) ) ;
#38937=DIRECTION ( 'NONE',  ( -0.000000000000000000, 3.673940397442059868E-16, -1.000000000000000000 ) ) ;
#38941=DIRECTION ( 'NONE',  ( -3.491481338843133355E-15, -1.000000000000000000, -1.836970198721029934E-16 ) ) ;
#38948=VERTEX_POINT ( 'NONE', #36930 ) ;
#38952=PLANE ( 'NONE',  #44393 ) ;
#38956=EDGE_CURVE ( 'NONE', #20214, #26006, #49606, .T. ) ;
#38966=EDGE_CURVE ( 'NONE', #17214, #4035, #48917, .T. ) ;
#38972=LINE ( 'NONE', #18427, #61079 ) ;
#38977=CARTESIAN_POINT ( 'NONE',  ( 2.906483450353349429, -10.09643294401463365, 455.0000000000000568 ) ) ;
#38978=CARTESIAN_POINT ( 'NONE',  ( -10.08346604330787777, 2.693516549646604918, 195.0000000000000284 ) ) ;
#38980=CARTESIAN_POINT ( 'NONE',  ( 11.19368345035336532, -11.19368345035338308, 195.0000000000000284 ) ) ;
#38992=ORIENTED_EDGE ( 'NONE', *, *, #51941, .F. ) ;
#38993=ORIENTED_EDGE ( 'NONE', *, *, #38429, .F. ) ;
#38994=VECTOR ( 'NONE', #33527, 1000.000000000000114 ) ;
#38997=ADVANCED_FACE ( 'NONE', ( #47863, #48569, #63789, #53193, #69435, #37268, #64154, #20989, #22040, #32306 ), #43602, .F. ) ;
#38998=AXIS2_PLACEMENT_3D ( 'NONE', #38370, #38705, #64897 ) ;
#39004=EDGE_CURVE ( 'NONE', #39722, #47486, #21348, .T. ) ;
#39006=DIRECTION ( 'NONE',  ( 8.673617379884087537E-15, 1.000000000000000000, 0.000000000000000000 ) ) ;
#39009=VECTOR ( 'NONE', #28079, 1000.000000000000114 ) ;
#39014=FACE_OUTER_BOUND ( 'NONE', #37685, .T. ) ;
#39021=DIRECTION ( 'NONE',  ( -0.000000000000000000, -0.000000000000000000, -1.000000000000000000 ) ) ;
#39022=DIRECTION ( 'NONE',  ( 1.000000000000000000, -1.115702204244422993E-14, -1.836970198721050395E-16 ) ) ;
#39029=EDGE_LOOP ( 'NONE', ( #50476, #46580, #17469, #16887 ) ) ;
#39033=CARTESIAN_POINT ( 'NONE',  ( 7.826483450353380000, -12.00648345035349251, 455.0000000000000568 ) ) ;
#39035=ORIENTED_EDGE ( 'NONE', *, *, #35453, .F. ) ;
#39037=CIRCLE ( 'NONE', #6281, 0.1999999999999987899 ) ;
#39040=ORIENTED_EDGE ( 'NONE', *, *, #15769, .F. ) ;
#39043=ORIENTED_EDGE ( 'NONE', *, *, #11513, .F. ) ;
#39044=ORIENTED_EDGE ( 'NONE', *, *, #41853, .T. ) ;
#39045=VECTOR ( 'NONE', #54677, 1000.000000000000000 ) ;
#39047=EDGE_CURVE ( 'NONE', #39228, #68196, #26652, .T. ) ;
#39049=CARTESIAN_POINT ( 'NONE',  ( -8.393516549646744096, -7.616533956692189022, 195.0000000000000284 ) ) ;
#39054=VECTOR ( 'NONE', #55232, 1000.000000000000000 ) ;
#39055=LINE ( 'NONE', #16808, #10376 ) ;
#39077=DIRECTION ( 'NONE',  ( 1.000000000000000000, 0.000000000000000000, 0.000000000000000000 ) ) ;
#39079=CARTESIAN_POINT ( 'NONE',  ( 11.32648345035337911, 4.193516549646524538, 455.0000000000000568 ) ) ;
#39083=DIRECTION ( 'NONE',  ( -1.000000000000000000, 0.000000000000000000, 0.000000000000000000 ) ) ;
#39092=CARTESIAN_POINT ( 'NONE',  ( -4.188533722949335569, 4.727349090213398775, 455.0000000000000568 ) ) ;
#39101=VECTOR ( 'NONE', #65516, 1000.000000000000000 ) ;
#39102=VECTOR ( 'NONE', #67172, 1000.000000000000114 ) ;
#39107=AXIS2_PLACEMENT_3D ( 'NONE', #56970, #8183, #67948 ) ;
#39111=VECTOR ( 'NONE', #36362, 1000.000000000000000 ) ;
#39126=EDGE_LOOP ( 'NONE', ( #53336, #11200, #10856, #22170 ) ) ;
#39149=VECTOR ( 'NONE', #65416, 1000.000000000000000 ) ;
#39158=DIRECTION ( 'NONE',  ( 0.7671651518153083105, -0.6414496315691473605, -2.587583378555127804E-16 ) ) ;
#39159=DIRECTION ( 'NONE',  ( -1.836970198721029934E-16, -1.836970198721010706E-16, 1.000000000000000000 ) ) ;
#39172=CARTESIAN_POINT ( 'NONE',  ( 7.606483450353380249, -11.78648345035349010, 455.0000000000000568 ) ) ;
#39173=VERTEX_POINT ( 'NONE', #12108 ) ;
#39179=CARTESIAN_POINT ( 'NONE',  ( -5.993516549646776603, -6.006483450353426790, 455.0000000000000568 ) ) ;
#39181=CARTESIAN_POINT ( 'NONE',  ( -1.077516549646676092, 10.73351654964656454, 455.0000000000000568 ) ) ;
#39182=ORIENTED_EDGE ( 'NONE', *, *, #22187, .T. ) ;
#39188=DIRECTION ( 'NONE',  ( 1.000000000000000000, 0.000000000000000000, 0.000000000000000000 ) ) ;
#39192=ADVANCED_FACE ( 'NONE', ( #66206 ), #12439, .F. ) ;
#39198=ORIENTED_EDGE ( 'NONE', *, *, #18864, .T. ) ;
#39204=ORIENTED_EDGE ( 'NONE', *, *, #12726, .T. ) ;
#39207=VECTOR ( 'NONE', #66061, 1000.000000000000000 ) ;
#39214=ADVANCED_FACE ( 'NONE', ( #39331 ), #49936, .F. ) ;
#39219=EDGE_LOOP ( 'NONE', ( #45164, #68430, #52670, #18000 ) ) ;
#39221=CARTESIAN_POINT ( 'NONE',  ( 7.606483450353380249, -11.78648345035339418, 195.0000000000000284 ) ) ;
#39228=VERTEX_POINT ( 'NONE', #55598 ) ;
#39244=EDGE_LOOP ( 'NONE', ( #25505, #34192, #63626, #41253 ) ) ;
#39246=DIRECTION ( 'NONE',  ( -1.836970198721029934E-16, 1.836970198721036344E-16, -1.000000000000000000 ) ) ;
#39253=PLANE ( 'NONE',  #4762 ) ;
#39254=AXIS2_PLACEMENT_3D ( 'NONE', #59180, #6131, #27694 ) ;
#39255=CIRCLE ( 'NONE', #48307, 1.399999999999999245 ) ;
#39259=ORIENTED_EDGE ( 'NONE', *, *, #8700, .T. ) ;
#39268=ORIENTED_EDGE ( 'NONE', *, *, #3862, .T. ) ;
#39270=ORIENTED_EDGE ( 'NONE', *, *, #29782, .T. ) ;
#39272=EDGE_LOOP ( 'NONE', ( #54834, #61204, #24170, #23239 ) ) ;
#39280=EDGE_LOOP ( 'NONE', ( #12817, #46096, #28602, #16935 ) ) ;
#39285=DIRECTION ( 'NONE',  ( 0.000000000000000000, 1.000000000000000000, 0.000000000000000000 ) ) ;
#39289=CARTESIAN_POINT ( 'NONE',  ( 6.006483450353401921, 5.993516549646582092, 455.0000000000000568 ) ) ;
#39293=VERTEX_POINT ( 'NONE', #56291 ) ;
#39294=EDGE_CURVE ( 'NONE', #65043, #20060, #62999, .T. ) ;
#39296=ORIENTED_EDGE ( 'NONE', *, *, #48414, .T. ) ;
#39306=ORIENTED_EDGE ( 'NONE', *, *, #9939, .F. ) ;
#39310=DIRECTION ( 'NONE',  ( 1.836970198721029934E-16, 1.836970198721010706E-16, -1.000000000000000000 ) ) ;
#39313=ORIENTED_EDGE ( 'NONE', *, *, #40585, .T. ) ;
#39323=ORIENTED_EDGE ( 'NONE', *, *, #7818, .F. ) ;
#39331=FACE_OUTER_BOUND ( 'NONE', #10894, .T. ) ;
#39335=DIRECTION ( 'NONE',  ( -1.000000000000000000, 0.000000000000000000, 0.000000000000000000 ) ) ;
#39341=DIRECTION ( 'NONE',  ( 1.000000000000000000, -1.047444401652939849E-14, 1.836970198721010706E-16 ) ) ;
#39344=EDGE_CURVE ( 'NONE', #20182, #39844, #67954, .T. ) ;
#39346=ORIENTED_EDGE ( 'NONE', *, *, #20279, .T. ) ;
#39347=LINE ( 'NONE', #34734, #19174 ) ;
#39350=ORIENTED_EDGE ( 'NONE', *, *, #6641, .T. ) ;
#39354=ORIENTED_EDGE ( 'NONE', *, *, #67090, .T. ) ;
#39358=EDGE_CURVE ( 'NONE', #35896, #11814, #41767, .T. ) ;
#39361=CARTESIAN_POINT ( 'NONE',  ( 11.78648345035337819, -4.186483450353492231, 455.0000000000000568 ) ) ;
#39364=CARTESIAN_POINT ( 'NONE',  ( 7.806483450353372433, 11.31351654964661968, 195.0000000000000284 ) ) ;
#39389=DIRECTION ( 'NONE',  ( 3.491481338843133355E-15, 1.000000000000000000, 1.836970198721029934E-16 ) ) ;
#39390=EDGE_LOOP ( 'NONE', ( #23548, #43757, #68867, #33030 ) ) ;
#39407=AXIS2_PLACEMENT_3D ( 'NONE', #18254, #67050, #39817 ) ;
#39421=ORIENTED_EDGE ( 'NONE', *, *, #25668, .F. ) ;
#39423=DIRECTION ( 'NONE',  ( -1.084202172485501594E-14, -1.000000000000000000, 0.000000000000000000 ) ) ;
#39426=CARTESIAN_POINT ( 'NONE',  ( -4.173516549646790530, -11.78648345035339595, 195.0000000000000284 ) ) ;
#39433=CARTESIAN_POINT ( 'NONE',  ( 5.393625297349950110, 4.734785091273829849, 455.0000000000000568 ) ) ;
#39440=AXIS2_PLACEMENT_3D ( 'NONE', #49030, #55044, #17184 ) ;
#39445=CYLINDRICAL_SURFACE ( 'NONE', #61642, 0.2000000000000005107 ) ;
#39448=ORIENTED_EDGE ( 'NONE', *, *, #44326, .T. ) ;
#39449=VECTOR ( 'NONE', #12432, 1000.000000000000000 ) ;
#39450=DIRECTION ( 'NONE',  ( -1.836970198721029934E-16, 1.836970198721036344E-16, -1.000000000000000000 ) ) ;
#39451=ORIENTED_EDGE ( 'NONE', *, *, #21775, .T. ) ;
#39452=ORIENTED_EDGE ( 'NONE', *, *, #21340, .F. ) ;
#39456=CARTESIAN_POINT ( 'NONE',  ( -1.077516549646676092, 10.73351654964656454, 195.0000000000000284 ) ) ;
#39459=ORIENTED_EDGE ( 'NONE', *, *, #9003, .F. ) ;
#39462=CARTESIAN_POINT ( 'NONE',  ( -2.893516549646830249, -11.12648345035345621, 455.0000000000000568 ) ) ;
#39464=ORIENTED_EDGE ( 'NONE', *, *, #42317, .T. ) ;
#39483=CARTESIAN_POINT ( 'NONE',  ( -1.677516549646683730, 9.828310488885911411, 455.0000000000000568 ) ) ;
#39491=LINE ( 'NONE', #56456, #61835 ) ;
#39492=FACE_OUTER_BOUND ( 'NONE', #51786, .T. ) ;
#39507=CARTESIAN_POINT ( 'NONE',  ( 7.616533956692244089, 8.393516549646575342, 455.0000000000000568 ) ) ;
#39508=CARTESIAN_POINT ( 'NONE',  ( 7.826483450353380000, -12.00648345035349251, 455.0000000000000568 ) ) ;
#39509=VERTEX_POINT ( 'NONE', #32219 ) ;
#39513=LINE ( 'NONE', #61074, #7099 ) ;
#39515=ADVANCED_FACE ( 'NONE', ( #53796 ), #26922, .T. ) ;
#39516=VERTEX_POINT ( 'NONE', #17329 ) ;
#39522=ORIENTED_EDGE ( 'NONE', *, *, #56164, .T. ) ;
#39528=CARTESIAN_POINT ( 'NONE',  ( 12.00648345035340903, 7.813516549646560172, 455.0000000000000568 ) ) ;
#39537=ORIENTED_EDGE ( 'NONE', *, *, #62192, .T. ) ;
#39540=DIRECTION ( 'NONE',  ( 0.000000000000000000, 0.000000000000000000, 1.000000000000000000 ) ) ;
#39555=AXIS2_PLACEMENT_3D ( 'NONE', #53939, #189, #21748 ) ;
#39563=VERTEX_POINT ( 'NONE', #49858 ) ;
#39564=DIRECTION ( 'NONE',  ( 1.836970198721029934E-16, 1.836970198721010706E-16, -1.000000000000000000 ) ) ;
#39569=CARTESIAN_POINT ( 'NONE',  ( 7.272650909786598561, -7.811466277050764795, 195.0000000000000284 ) ) ;
#39572=EDGE_CURVE ( 'NONE', #24415, #22946, #65096, .T. ) ;
#39592=ORIENTED_EDGE ( 'NONE', *, *, #34073, .F. ) ;
#39595=CARTESIAN_POINT ( 'NONE',  ( 4.396432944014529554, 8.393516549646633962, 195.0000000000000284 ) ) ;
#39600=EDGE_CURVE ( 'NONE', #40737, #25493, #43862, .T. ) ;
#39612=CARTESIAN_POINT ( 'NONE',  ( -9.234937905884020637, 9.942044687070460185, 455.0000000000000568 ) ) ;
#39615=EDGE_CURVE ( 'NONE', #41426, #48554, #38900, .T. ) ;
#39624=DIRECTION ( 'NONE',  ( -3.540573132209561620E-15, -1.000000000000000000, 0.000000000000000000 ) ) ;
#39628=ORIENTED_EDGE ( 'NONE', *, *, #1156, .T. ) ;
#39630=VERTEX_POINT ( 'NONE', #17683 ) ;
#39639=CARTESIAN_POINT ( 'NONE',  ( -8.393516549646712122, 5.655420232009161552, 455.0000000000000568 ) ) ;
#39642=AXIS2_PLACEMENT_3D ( 'NONE', #22756, #10756, #65218 ) ;
#39646=CARTESIAN_POINT ( 'NONE',  ( 7.272650909786644746, 7.798499376343933420, 455.0000000000000568 ) ) ;
#39647=CARTESIAN_POINT ( 'NONE',  ( -11.99351654964671354, 7.813516549646603693, 195.0000000000000284 ) ) ;
#39652=CARTESIAN_POINT ( 'NONE',  ( 9.306483450353415066, 10.08346604330773744, 455.0000000000000568 ) ) ;
#39662=EDGE_CURVE ( 'NONE', #29102, #27000, #27051, .T. ) ;
#39667=ORIENTED_EDGE ( 'NONE', *, *, #63656, .F. ) ;
#39671=ADVANCED_FACE ( 'NONE', ( #24381 ), #45945, .F. ) ;
#39674=FACE_OUTER_BOUND ( 'NONE', #30594, .T. ) ;
#39696=DIRECTION ( 'NONE',  ( 0.000000000000000000, -3.673940397442059868E-16, 1.000000000000000000 ) ) ;
#39708=DIRECTION ( 'NONE',  ( -1.000000000000000000, 0.000000000000000000, 0.000000000000000000 ) ) ;
#39722=VERTEX_POINT ( 'NONE', #3169 ) ;
#39729=CIRCLE ( 'NONE', #57816, 0.2000000000000005107 ) ;
#39732=EDGE_CURVE ( 'NONE', #38207, #58876, #67719, .T. ) ;
#39737=DIRECTION ( 'NONE',  ( -0.7671651518152985405, -0.6414496315691592399, 0.000000000000000000 ) ) ;
#39738=ORIENTED_EDGE ( 'NONE', *, *, #41865, .F. ) ;
#39753=EDGE_CURVE ( 'NONE', #30052, #46347, #6742, .T. ) ;
#39758=ORIENTED_EDGE ( 'NONE', *, *, #28183, .F. ) ;
#39770=FACE_OUTER_BOUND ( 'NONE', #66012, .T. ) ;
#39777=EDGE_CURVE ( 'NONE', #56924, #7012, #47436, .T. ) ;
#39784=ORIENTED_EDGE ( 'NONE', *, *, #16397, .T. ) ;
#39788=VERTEX_POINT ( 'NONE', #68919 ) ;
#39801=VECTOR ( 'NONE', #24490, 1000.000000000000000 ) ;
#39802=ORIENTED_EDGE ( 'NONE', *, *, #34081, .T. ) ;
#39803=ORIENTED_EDGE ( 'NONE', *, *, #20888, .T. ) ;
#39805=AXIS2_PLACEMENT_3D ( 'NONE', #31451, #53016, #41333 ) ;
#39807=ORIENTED_EDGE ( 'NONE', *, *, #58924, .F. ) ;
#39808=EDGE_CURVE ( 'NONE', #55579, #67623, #42736, .T. ) ;
#39817=DIRECTION ( 'NONE',  ( -1.000000000000000000, 0.000000000000000000, 0.000000000000000000 ) ) ;
#39822=LINE ( 'NONE', #1649, #57480 ) ;
#39830=DIRECTION ( 'NONE',  ( 0.5000000000000038858, 0.8660254037844363761, 3.181725716174712609E-16 ) ) ;
#39844=VERTEX_POINT ( 'NONE', #16214 ) ;
#39845=CARTESIAN_POINT ( 'NONE',  ( -7.798499376344109280, -4.740315990920159095, 455.0000000000000568 ) ) ;
#39846=CARTESIAN_POINT ( 'NONE',  ( -9.404046420174124066, 1.853252480934674873, 195.0000000000000284 ) ) ;
#39850=DIRECTION ( 'NONE',  ( -0.7671651518153043137, 0.6414496315691521344, 2.587583378555129776E-16 ) ) ;
#39851=VECTOR ( 'NONE', #19059, 1000.000000000000000 ) ;
#39859=ORIENTED_EDGE ( 'NONE', *, *, #62513, .T. ) ;
#39874=CARTESIAN_POINT ( 'NONE',  ( -2.277516549646682709, 9.828310488885916740, 195.0000000000000284 ) ) ;
#39886=DIRECTION ( 'NONE',  ( -0.000000000000000000, 3.673940397442059868E-16, -1.000000000000000000 ) ) ;
#39888=ADVANCED_FACE ( 'NONE', ( #41687 ), #58663, .T. ) ;
#39897=DIRECTION ( 'NONE',  ( 0.000000000000000000, -3.673940397442059868E-16, 1.000000000000000000 ) ) ;
#39906=EDGE_CURVE ( 'NONE', #16863, #40309, #31659, .T. ) ;
#39910=CARTESIAN_POINT ( 'NONE',  ( 10.92648345035335922, 2.693516549646528091, 455.0000000000000568 ) ) ;
#39913=CARTESIAN_POINT ( 'NONE',  ( -9.234937905884127218, -9.955011587777249815, 455.0000000000000568 ) ) ;
#39919=DIRECTION ( 'NONE',  ( 1.836970198721029934E-16, 1.836970198721010706E-16, -1.000000000000000000 ) ) ;
#39922=DIRECTION ( 'NONE',  ( -1.084202172485511060E-14, -1.000000000000000000, 0.000000000000000000 ) ) ;
#39925=ORIENTED_EDGE ( 'NONE', *, *, #52802, .T. ) ;
#39931=EDGE_LOOP ( 'NONE', ( #19564, #6412, #44036, #59472 ) ) ;
#39938=VECTOR ( 'NONE', #60936, 1000.000000000000000 ) ;
#39942=ORIENTED_EDGE ( 'NONE', *, *, #24158, .T. ) ;
#39944=ADVANCED_FACE ( 'NONE', ( #33166 ), #27869, .F. ) ;
#39946=EDGE_CURVE ( 'NONE', #50762, #22220, #36124, .T. ) ;
#39951=LINE ( 'NONE', #24409, #7244 ) ;
#39952=VECTOR ( 'NONE', #7790, 1000.000000000000000 ) ;
#39959=DIRECTION ( 'NONE',  ( -1.836970198721029934E-16, -1.836970198721010706E-16, 1.000000000000000000 ) ) ;
#39960=PLANE ( 'NONE',  #1561 ) ;
#39965=LINE ( 'NONE', #14157, #17498 ) ;
#39971=CARTESIAN_POINT ( 'NONE',  ( 7.272650909786602114, 4.188533722949199678, 455.0000000000000568 ) ) ;
#39974=VERTEX_POINT ( 'NONE', #5612 ) ;
#39977=CARTESIAN_POINT ( 'NONE',  ( -10.73351654964671020, 1.677516549646603794, 195.0000000000000284 ) ) ;
#39981=FACE_OUTER_BOUND ( 'NONE', #54258, .T. ) ;
#39984=ADVANCED_FACE ( 'NONE', ( #27519 ), #1007, .F. ) ;
#39990=ADVANCED_FACE ( 'NONE', ( #22562 ), #17932, .F. ) ;
#39993=ORIENTED_EDGE ( 'NONE', *, *, #59025, .T. ) ;
#40008=ADVANCED_FACE ( 'NONE', ( #65009 ), #17589, .F. ) ;
#40027=CARTESIAN_POINT ( 'NONE',  ( 8.406483450353382736, 4.383466043307721272, 455.0000000000000568 ) ) ;
#40030=DIRECTION ( 'NONE',  ( -1.000000000000000000, 0.000000000000000000, 0.000000000000000000 ) ) ;
#40033=CARTESIAN_POINT ( 'NONE',  ( -4.193516549646675529, 11.11351654964658664, 195.0000000000000284 ) ) ;
#40054=EDGE_CURVE ( 'NONE', #33046, #51738, #56463, .T. ) ;
#40056=CARTESIAN_POINT ( 'NONE',  ( -11.77351654964674132, -4.186483450353323477, 455.0000000000000568 ) ) ;
#40064=VECTOR ( 'NONE', #24639, 1000.000000000000000 ) ;
#40069=ORIENTED_EDGE ( 'NONE', *, *, #52223, .F. ) ;
#40070=ORIENTED_EDGE ( 'NONE', *, *, #12415, .F. ) ;
#40075=DIRECTION ( 'NONE',  ( -8.673617379884013384E-15, -1.000000000000000000, 0.000000000000000000 ) ) ;
#40082=AXIS2_PLACEMENT_3D ( 'NONE', #36950, #16765, #59886 ) ;
#40083=CARTESIAN_POINT ( 'NONE',  ( 6.006483450353353959, 5.993516549646629166, 195.0000000000000284 ) ) ;
#40088=ORIENTED_EDGE ( 'NONE', *, *, #24205, .T. ) ;
#40100=AXIS2_PLACEMENT_3D ( 'NONE', #45014, #11457, #60591 ) ;
#40105=VECTOR ( 'NONE', #25218, 1000.000000000000000 ) ;
#40116=DIRECTION ( 'NONE',  ( 1.836970198721029934E-16, 1.836970198721010706E-16, -1.000000000000000000 ) ) ;
#40126=ORIENTED_EDGE ( 'NONE', *, *, #14393, .F. ) ;
#40128=DIRECTION ( 'NONE',  ( 0.8660254037844358210, -0.5000000000000049960, 0.000000000000000000 ) ) ;
#40130=ORIENTED_EDGE ( 'NONE', *, *, #16132, .F. ) ;
#40137=AXIS2_PLACEMENT_3D ( 'NONE', #1603, #49023, #23175 ) ;
#40138=CARTESIAN_POINT ( 'NONE',  ( 2.765062094116107705, 9.942044687070449527, 455.0000000000000568 ) ) ;
#40142=CARTESIAN_POINT ( 'NONE',  ( -7.252248008019455128, 6.606374702650072983, 455.0000000000000568 ) ) ;
#40143=DIRECTION ( 'NONE',  ( 1.671920889371702657E-15, 1.000000000000000000, -0.000000000000000000 ) ) ;
#40145=FACE_OUTER_BOUND ( 'NONE', #5651, .T. ) ;
#40148=ORIENTED_EDGE ( 'NONE', *, *, #15280, .F. ) ;
#40149=ADVANCED_FACE ( 'NONE', ( #46198 ), #67772, .F. ) ;
#40150=EDGE_LOOP ( 'NONE', ( #8494, #64712, #12506, #17961 ) ) ;
#40175=EDGE_CURVE ( 'NONE', #35648, #5476, #68833, .T. ) ;
#40176=DIRECTION ( 'NONE',  ( -0.7671651518153105309, -0.6414496315691445849, 0.000000000000000000 ) ) ;
#40184=CARTESIAN_POINT ( 'NONE',  ( 10.09643294401453062, 2.693516549646537417, 455.0000000000000568 ) ) ;
#40189=AXIS2_PLACEMENT_3D ( 'NONE', #67003, #61694, #40834 ) ;
#40192=CARTESIAN_POINT ( 'NONE',  ( 4.406483450353420928, 11.31351654964658593, 455.0000000000000568 ) ) ;
#40218=CIRCLE ( 'NONE', #4117, 0.1999999999999987899 ) ;
#40219=VERTEX_POINT ( 'NONE', #9080 ) ;
#40221=ORIENTED_EDGE ( 'NONE', *, *, #14564, .F. ) ;
#40223=LINE ( 'NONE', #6998, #59654 ) ;
#40225=ORIENTED_EDGE ( 'NONE', *, *, #14975, .T. ) ;
#40227=PLANE ( 'NONE',  #13048 ) ;
#40230=ORIENTED_EDGE ( 'NONE', *, *, #37064, .F. ) ;
#40231=DIRECTION ( 'NONE',  ( -1.000000000000000000, -0.000000000000000000, -0.000000000000000000 ) ) ;
#40235=CARTESIAN_POINT ( 'NONE',  ( 9.841277389592693936, 1.677516549646539623, 455.0000000000000568 ) ) ;
#40242=CARTESIAN_POINT ( 'NONE',  ( -7.798499376344067535, 4.727349090213367688, 455.0000000000000568 ) ) ;
#40247=VERTEX_POINT ( 'NONE', #48314 ) ;
#40248=ADVANCED_FACE ( 'NONE', ( #63535 ), #64575, .T. ) ;
#40251=VECTOR ( 'NONE', #61209, 1000.000000000000000 ) ;
#40255=VECTOR ( 'NONE', #45871, 1000.000000000000000 ) ;
#40265=ORIENTED_EDGE ( 'NONE', *, *, #4432, .T. ) ;
#40273=VECTOR ( 'NONE', #3596, 1000.000000000000000 ) ;
#40278=ORIENTED_EDGE ( 'NONE', *, *, #41956, .F. ) ;
#40280=ORIENTED_EDGE ( 'NONE', *, *, #24048, .F. ) ;
#40285=CARTESIAN_POINT ( 'NONE',  ( -11.99351654964678282, -11.19368345035330314, 195.0000000000000284 ) ) ;
#40286=ORIENTED_EDGE ( 'NONE', *, *, #64014, .T. ) ;
#40309=VERTEX_POINT ( 'NONE', #47961 ) ;
#40314=CARTESIAN_POINT ( 'NONE',  ( -11.77351654964670935, 7.813516549646603693, 195.0000000000000284 ) ) ;
#40317=EDGE_CURVE ( 'NONE', #2273, #65266, #15782, .T. ) ;
#40319=ADVANCED_FACE ( 'NONE', ( #60289 ), #5874, .F. ) ;
#40323=VERTEX_POINT ( 'NONE', #22136 ) ;
#40328=ORIENTED_EDGE ( 'NONE', *, *, #51941, .T. ) ;
#40337=CARTESIAN_POINT ( 'NONE',  ( 2.706483450353419862, 10.91351654964658735, 455.0000000000000568 ) ) ;
#40339=VERTEX_POINT ( 'NONE', #16828 ) ;
#40341=VERTEX_POINT ( 'NONE', #934 ) ;
#40346=ORIENTED_EDGE ( 'NONE', *, *, #2230, .F. ) ;
#40349=CARTESIAN_POINT ( 'NONE',  ( -11.99351654964674374, -4.186483450353318148, 455.0000000000000568 ) ) ;
#40352=VECTOR ( 'NONE', #2904, 1000.000000000000000 ) ;
#40353=VECTOR ( 'NONE', #58912, 1000.000000000000000 ) ;
#40375=EDGE_CURVE ( 'NONE', #5297, #30586, #44715, .T. ) ;
#40383=DIRECTION ( 'NONE',  ( -3.491481338843132961E-15, -1.000000000000000000, 0.000000000000000000 ) ) ;
#40388=EDGE_LOOP ( 'NONE', ( #36038, #17911, #695, #4003 ) ) ;
#40389=DIRECTION ( 'NONE',  ( 1.000000000000000000, -8.540177112501197482E-15, 0.000000000000000000 ) ) ;
#40401=VERTEX_POINT ( 'NONE', #23157 ) ;
#40402=DIRECTION ( 'NONE',  ( 1.000000000000000000, -1.883404846338789915E-14, 1.836970198720995421E-16 ) ) ;
#40413=CARTESIAN_POINT ( 'NONE',  ( 4.406483450353335662, -11.78648345035347766, 455.0000000000000568 ) ) ;
#40425=ORIENTED_EDGE ( 'NONE', *, *, #28877, .T. ) ;
#40427=DIRECTION ( 'NONE',  ( -5.163402228214836012E-15, -1.000000000000000000, -1.836970198721026976E-16 ) ) ;
#40438=ORIENTED_EDGE ( 'NONE', *, *, #8202, .F. ) ;
#40441=VERTEX_POINT ( 'NONE', #14215 ) ;
#40443=PLANE ( 'NONE',  #64421 ) ;
#40445=ORIENTED_EDGE ( 'NONE', *, *, #26934, .T. ) ;
#40462=ORIENTED_EDGE ( 'NONE', *, *, #15980, .T. ) ;
#40464=VECTOR ( 'NONE', #13040, 1000.000000000000000 ) ;
#40465=ADVANCED_FACE ( 'NONE', ( #28804 ), #62295, .F. ) ;
#40478=VERTEX_POINT ( 'NONE', #41080 ) ;
#40486=EDGE_LOOP ( 'NONE', ( #16753, #58258, #48812, #14541 ) ) ;
#40491=VERTEX_POINT ( 'NONE', #19168 ) ;
#40492=ADVANCED_FACE ( 'NONE', ( #63364 ), #55688, .T. ) ;
#40493=DIRECTION ( 'NONE',  ( -7.808916176531286882E-15, -1.000000000000000000, 0.000000000000000000 ) ) ;
#40511=CARTESIAN_POINT ( 'NONE',  ( -11.07551654964681731, -9.804883450353372609, 455.0000000000000568 ) ) ;
#40517=DIRECTION ( 'NONE',  ( 0.000000000000000000, 1.000000000000000000, 0.000000000000000000 ) ) ;
#40521=DIRECTION ( 'NONE',  ( -0.000000000000000000, 3.673940397442059868E-16, -1.000000000000000000 ) ) ;
#40524=ORIENTED_EDGE ( 'NONE', *, *, #38318, .T. ) ;
#40526=EDGE_CURVE ( 'NONE', #11040, #3811, #24872, .T. ) ;
#40527=FACE_OUTER_BOUND ( 'NONE', #45506, .T. ) ;
#40532=LINE ( 'NONE', #24280, #38114 ) ;
#40536=EDGE_CURVE ( 'NONE', #11215, #24412, #26229, .T. ) ;
#40544=ORIENTED_EDGE ( 'NONE', *, *, #10064, .F. ) ;
#40549=CARTESIAN_POINT ( 'NONE',  ( 10.92648345035335922, 2.693516549646528091, 455.0000000000000568 ) ) ;
#40551=CARTESIAN_POINT ( 'NONE',  ( -11.07551654964682797, -11.08848345035333693, 455.0000000000000568 ) ) ;
#40565=DIRECTION ( 'NONE',  ( 0.000000000000000000, -3.673940397442059868E-16, 1.000000000000000000 ) ) ;
#40566=CARTESIAN_POINT ( 'NONE',  ( -7.798499376344067535, 4.727349090213368576, 195.0000000000000284 ) ) ;
#40576=EDGE_LOOP ( 'NONE', ( #12505, #25529, #52341, #40789 ) ) ;
#40584=CARTESIAN_POINT ( 'NONE',  ( 5.393625297349901260, -4.747751991980754482, 455.0000000000000568 ) ) ;
#40585=EDGE_CURVE ( 'NONE', #61368, #4952, #16676, .T. ) ;
#40596=FACE_OUTER_BOUND ( 'NONE', #41652, .T. ) ;
#40597=VERTEX_POINT ( 'NONE', #59098 ) ;
#40599=ORIENTED_EDGE ( 'NONE', *, *, #58008, .T. ) ;
#40616=DIRECTION ( 'NONE',  ( 1.836970198721029934E-16, 1.836970198721010706E-16, -1.000000000000000000 ) ) ;
#40628=EDGE_CURVE ( 'NONE', #22525, #6513, #43175, .T. ) ;
#40633=CARTESIAN_POINT ( 'NONE',  ( -2.893516549646681035, 10.08346604330774632, 455.0000000000000568 ) ) ;
#40641=VERTEX_POINT ( 'NONE', #12360 ) ;
#40645=ORIENTED_EDGE ( 'NONE', *, *, #21881, .F. ) ;
#40655=CIRCLE ( 'NONE', #2249, 2.204799999999997429 ) ;
#40659=ORIENTED_EDGE ( 'NONE', *, *, #13272, .F. ) ;
#40667=FACE_OUTER_BOUND ( 'NONE', #52095, .T. ) ;
#40679=DIRECTION ( 'NONE',  ( 7.665540703601094997E-15, 1.000000000000000000, 0.000000000000000000 ) ) ;
#40680=PLANE ( 'NONE',  #24110 ) ;
#40682=DIRECTION ( 'NONE',  ( -0.7671651518153105309, 0.6414496315691445849, 2.356647714346206145E-16 ) ) ;
#40686=DIRECTION ( 'NONE',  ( -0.000000000000000000, -0.000000000000000000, -1.000000000000000000 ) ) ;
#40690=EDGE_LOOP ( 'NONE', ( #54097, #8167, #5142, #60676, #7507, #52337, #45956, #23917, #49390, #48365, #69168, #60320, #26193, #25466, #40524, #41496, #67093 ) ) ;
#40694=AXIS2_PLACEMENT_3D ( 'NONE', #46605, #13021, #29284 ) ;
#40695=EDGE_LOOP ( 'NONE', ( #24326, #16831, #8825, #57908 ) ) ;
#40702=VECTOR ( 'NONE', #21261, 1000.000000000000000 ) ;
#40708=FACE_OUTER_BOUND ( 'NONE', #15690, .T. ) ;
#40711=ORIENTED_EDGE ( 'NONE', *, *, #33238, .F. ) ;
#40712=VERTEX_POINT ( 'NONE', #17694 ) ;
#40724=ADVANCED_FACE ( 'NONE', ( #55867 ), #60128, .F. ) ;
#40730=DIRECTION ( 'NONE',  ( 1.836970198721029934E-16, 1.836970198721010706E-16, -1.000000000000000000 ) ) ;
#40736=FACE_OUTER_BOUND ( 'NONE', #21724, .T. ) ;
#40737=VERTEX_POINT ( 'NONE', #55527 ) ;
#40741=FACE_OUTER_BOUND ( 'NONE', #5299, .T. ) ;
#40747=EDGE_LOOP ( 'NONE', ( #29951, #56795, #58496, #17130 ) ) ;
#40749=CARTESIAN_POINT ( 'NONE',  ( -9.828310488886053520, 2.277516549646603661, 455.0000000000000568 ) ) ;
#40750=PLANE ( 'NONE',  #12973 ) ;
#40759=EDGE_CURVE ( 'NONE', #1592, #35824, #66698, .T. ) ;
#40770=LINE ( 'NONE', #28755, #61235 ) ;
#40772=ORIENTED_EDGE ( 'NONE', *, *, #13187, .T. ) ;
#40775=AXIS2_PLACEMENT_3D ( 'NONE', #17440, #60230, #11784 ) ;
#40779=CARTESIAN_POINT ( 'NONE',  ( 8.406483450353379183, -7.616533956692230767, 195.0000000000000284 ) ) ;
#40789=ORIENTED_EDGE ( 'NONE', *, *, #65008, .T. ) ;
#40798=EDGE_CURVE ( 'NONE', #67879, #43669, #51617, .T. ) ;
#40822=LINE ( 'NONE', #35498, #58448 ) ;
#40823=LINE ( 'NONE', #51788, #29980 ) ;
#40834=DIRECTION ( 'NONE',  ( -1.000000000000000000, 0.000000000000000000, 0.000000000000000000 ) ) ;
#40838=FACE_OUTER_BOUND ( 'NONE', #3555, .T. ) ;
#40841=DIRECTION ( 'NONE',  ( 1.000000000000000000, -3.491481338843133355E-15, -1.836970198721036344E-16 ) ) ;
#40842=DIRECTION ( 'NONE',  ( -0.000000000000000000, 3.673940397442059868E-16, -1.000000000000000000 ) ) ;
#40847=EDGE_CURVE ( 'NONE', #3246, #40441, #45958, .T. ) ;
#40852=CARTESIAN_POINT ( 'NONE',  ( 4.201500623655991085, 7.259684009079854228, 195.0000000000000284 ) ) ;
#40853=CARTESIAN_POINT ( 'NONE',  ( 11.12648345035333186, 4.193516549646575164, 195.0000000000000284 ) ) ;
#40872=ORIENTED_EDGE ( 'NONE', *, *, #48389, .T. ) ;
#40885=ORIENTED_EDGE ( 'NONE', *, *, #5068, .F. ) ;
#40894=ADVANCED_FACE ( 'NONE', ( #50901 ), #52317, .F. ) ;
#40897=DIRECTION ( 'NONE',  ( -6.308085367188446447E-15, -1.000000000000000000, 0.000000000000000000 ) ) ;
#40906=CYLINDRICAL_SURFACE ( 'NONE', #29339, 0.1999999999999987899 ) ;
#40910=DIRECTION ( 'NONE',  ( -1.836970198721029934E-16, -1.836970198721010706E-16, 1.000000000000000000 ) ) ;
#40917=ORIENTED_EDGE ( 'NONE', *, *, #35332, .T. ) ;
#40920=ORIENTED_EDGE ( 'NONE', *, *, #27451, .F. ) ;
#40923=VECTOR ( 'NONE', #19517, 1000.000000000000000 ) ;
#40924=ORIENTED_EDGE ( 'NONE', *, *, #53426, .F. ) ;
#40926=VERTEX_POINT ( 'NONE', #19771 ) ;
#40927=VECTOR ( 'NONE', #34623, 1000.000000000000000 ) ;
#40940=EDGE_CURVE ( 'NONE', #46798, #7898, #62922, .T. ) ;
#40962=FACE_OUTER_BOUND ( 'NONE', #51939, .T. ) ;
#40965=CARTESIAN_POINT ( 'NONE',  ( 11.12648345035333364, 4.193516549646575164, 195.0000000000000284 ) ) ;
#40977=DIRECTION ( 'NONE',  ( 1.203165845134433242E-14, 1.000000000000000000, 0.000000000000000000 ) ) ;
#40978=EDGE_CURVE ( 'NONE', #43112, #6826, #48755, .T. ) ;
#40980=DIRECTION ( 'NONE',  ( 4.336808689942006692E-15, 1.000000000000000000, 0.000000000000000000 ) ) ;
#40988=DIRECTION ( 'NONE',  ( -0.000000000000000000, -0.000000000000000000, -1.000000000000000000 ) ) ;
#40993=CIRCLE ( 'NONE', #15020, 0.5999999999999998668 ) ;
#41004=VERTEX_POINT ( 'NONE', #53377 ) ;
#41010=ORIENTED_EDGE ( 'NONE', *, *, #69463, .F. ) ;
#41018=VECTOR ( 'NONE', #24423, 1000.000000000000000 ) ;
#41021=EDGE_LOOP ( 'NONE', ( #60146, #42962, #26386, #40462 ) ) ;
#41023=VECTOR ( 'NONE', #26321, 1000.000000000000114 ) ;
#41027=CIRCLE ( 'NONE', #22957, 0.2000000000000000944 ) ;
#41049=VERTEX_POINT ( 'NONE', #52683 ) ;
#41065=EDGE_CURVE ( 'NONE', #60260, #4452, #55443, .T. ) ;
#41068=LINE ( 'NONE', #69346, #20963 ) ;
#41078=VERTEX_POINT ( 'NONE', #39508 ) ;
#41080=CARTESIAN_POINT ( 'NONE',  ( 10.74648345035335240, 1.677516549646529409, 455.0000000000000568 ) ) ;
#41082=VECTOR ( 'NONE', #1452, 1000.000000000000000 ) ;
#41085=CYLINDRICAL_SURFACE ( 'NONE', #12694, 0.5999999999999998668 ) ;
#41089=ORIENTED_EDGE ( 'NONE', *, *, #33839, .F. ) ;
#41099=EDGE_LOOP ( 'NONE', ( #58356, #27018, #63597, #39313 ) ) ;
#41105=CARTESIAN_POINT ( 'NONE',  ( 11.78648345035337819, -4.186483450353396307, 195.0000000000000284 ) ) ;
#41112=VECTOR ( 'NONE', #21536, 1000.000000000000000 ) ;
#41120=LINE ( 'NONE', #19205, #41123 ) ;
#41123=VECTOR ( 'NONE', #69048, 1000.000000000000000 ) ;
#41134=VERTEX_POINT ( 'NONE', #28217 ) ;
#41140=CARTESIAN_POINT ( 'NONE',  ( 11.78648345035337819, -7.606483450353398013, 195.0000000000000284 ) ) ;
#41142=LINE ( 'NONE', #36540, #58462 ) ;
#41145=AXIS2_PLACEMENT_3D ( 'NONE', #33299, #64789, #27309 ) ;
#41150=LINE ( 'NONE', #8629, #28166 ) ;
#41151=ORIENTED_EDGE ( 'NONE', *, *, #29619, .T. ) ;
#41155=LINE ( 'NONE', #63792, #63941 ) ;
#41173=DIRECTION ( 'NONE',  ( 0.000000000000000000, 1.000000000000000000, 3.673940397442059868E-16 ) ) ;
#41178=DIRECTION ( 'NONE',  ( -1.836970198721029934E-16, 1.836970198721036344E-16, -1.000000000000000000 ) ) ;
#41180=AXIS2_PLACEMENT_3D ( 'NONE', #14778, #30694, #52619 ) ;
#41186=ADVANCED_FACE ( 'NONE', ( #66033 ), #50478, .F. ) ;
#41189=CARTESIAN_POINT ( 'NONE',  ( -11.11351654964671098, 7.793516549646603231, 195.0000000000000284 ) ) ;
#41190=CARTESIAN_POINT ( 'NONE',  ( 4.747751991980608821, 6.606374702650090747, 195.0000000000000284 ) ) ;
#41197=VERTEX_POINT ( 'NONE', #17603 ) ;
#41220=FACE_OUTER_BOUND ( 'NONE', #10430, .T. ) ;
#41221=VECTOR ( 'NONE', #40686, 1000.000000000000000 ) ;
#41222=ORIENTED_EDGE ( 'NONE', *, *, #59598, .T. ) ;
#41223=EDGE_LOOP ( 'NONE', ( #14359, #2174, #51246, #17878 ) ) ;
#41229=AXIS2_PLACEMENT_3D ( 'NONE', #39079, #22489, #1588 ) ;
#41239=ADVANCED_FACE ( 'NONE', ( #18998 ), #14035, .F. ) ;
#41253=ORIENTED_EDGE ( 'NONE', *, *, #55797, .T. ) ;
#41254=CARTESIAN_POINT ( 'NONE',  ( -11.47551654964682122, -10.20488345035336941, 455.0000000000000568 ) ) ;
#41272=VERTEX_POINT ( 'NONE', #46557 ) ;
#41283=CARTESIAN_POINT ( 'NONE',  ( 7.806483450353418618, 11.11351654964657421, 455.0000000000000568 ) ) ;
#41294=DIRECTION ( 'NONE',  ( 0.7071067811865391350, -0.7071067811865560104, 0.000000000000000000 ) ) ;
#41295=EDGE_CURVE ( 'NONE', #25935, #4952, #61413, .T. ) ;
#41299=EDGE_CURVE ( 'NONE', #9367, #4940, #63229, .T. ) ;
#41305=CARTESIAN_POINT ( 'NONE',  ( 7.606483450353380249, -11.78648345035349010, 455.0000000000000568 ) ) ;
#41306=ORIENTED_EDGE ( 'NONE', *, *, #9502, .T. ) ;
#41309=VECTOR ( 'NONE', #36964, 1000.000000000000000 ) ;
#41314=LINE ( 'NONE', #9500, #63327 ) ;
#41316=AXIS2_PLACEMENT_3D ( 'NONE', #5434, #461, #38295 ) ;
#41319=DIRECTION ( 'NONE',  ( 1.047444401652939849E-14, 1.000000000000000000, 0.000000000000000000 ) ) ;
#41320=CARTESIAN_POINT ( 'NONE',  ( 12.00648345035333620, 4.173516549646563156, 195.0000000000000284 ) ) ;
#41321=ORIENTED_EDGE ( 'NONE', *, *, #23235, .T. ) ;
#41324=CARTESIAN_POINT ( 'NONE',  ( 3.606483450353397568, 4.609516549646590633, 455.0000000000000568 ) ) ;
#41325=CIRCLE ( 'NONE', #53825, 0.1999999999999987899 ) ;
#41328=DIRECTION ( 'NONE',  ( 1.000000000000000000, 0.000000000000000000, 0.000000000000000000 ) ) ;
#41333=DIRECTION ( 'NONE',  ( 0.000000000000000000, 1.000000000000000000, 0.000000000000000000 ) ) ;
#41334=VERTEX_POINT ( 'NONE', #29949 ) ;
#41337=DIRECTION ( 'NONE',  ( 5.163402228214835223E-15, 1.000000000000000000, 0.000000000000000000 ) ) ;
#41341=CARTESIAN_POINT ( 'NONE',  ( 5.668387132715918320, -8.406483450353487541, 455.0000000000000568 ) ) ;
#41350=EDGE_CURVE ( 'NONE', #20840, #17214, #30625, .T. ) ;
#41362=DIRECTION ( 'NONE',  ( -1.836970198721029934E-16, 1.836970198721036344E-16, -1.000000000000000000 ) ) ;
#41367=ORIENTED_EDGE ( 'NONE', *, *, #38398, .T. ) ;
#41377=ADVANCED_FACE ( 'NONE', ( #30660 ), #40906, .F. ) ;
#41379=ORIENTED_EDGE ( 'NONE', *, *, #1949, .T. ) ;
#41381=VECTOR ( 'NONE', #43597, 1000.000000000000000 ) ;
#41382=VECTOR ( 'NONE', #51654, 999.9999999999998863 ) ;
#41383=VECTOR ( 'NONE', #54098, 1000.000000000000000 ) ;
#41397=ORIENTED_EDGE ( 'NONE', *, *, #52161, .F. ) ;
#41407=CARTESIAN_POINT ( 'NONE',  ( 10.92648345035340895, 9.293516549646565039, 455.0000000000000568 ) ) ;
#41417=ADVANCED_FACE ( 'NONE', ( #42665 ), #36664, .T. ) ;
#41426=VERTEX_POINT ( 'NONE', #20051 ) ;
#41436=ORIENTED_EDGE ( 'NONE', *, *, #23703, .T. ) ;
#41447=ORIENTED_EDGE ( 'NONE', *, *, #24857, .T. ) ;
#41449=ORIENTED_EDGE ( 'NONE', *, *, #35797, .F. ) ;
#41453=CARTESIAN_POINT ( 'NONE',  ( 10.92648345035337343, -9.306483450353493225, 455.0000000000000568 ) ) ;
#41477=VECTOR ( 'NONE', #3413, 1000.000000000000000 ) ;
#41483=EDGE_CURVE ( 'NONE', #39722, #27985, #21490, .T. ) ;
#41486=CARTESIAN_POINT ( 'NONE',  ( -11.99351654964674374, -4.186483450353318148, 455.0000000000000568 ) ) ;
#41489=ORIENTED_EDGE ( 'NONE', *, *, #53528, .T. ) ;
#41490=DIRECTION ( 'NONE',  ( -1.000000000000000000, 0.000000000000000000, 0.000000000000000000 ) ) ;
#41495=CARTESIAN_POINT ( 'NONE',  ( 7.428221114745003462, -3.606483450353489939, 455.0000000000000568 ) ) ;
#41496=ORIENTED_EDGE ( 'NONE', *, *, #55932, .T. ) ;
#41497=ORIENTED_EDGE ( 'NONE', *, *, #39344, .T. ) ;
#41498=DIRECTION ( 'NONE',  ( 1.000000000000000000, 0.000000000000000000, 0.000000000000000000 ) ) ;
#41503=CARTESIAN_POINT ( 'NONE',  ( 8.465062094116072799, 4.242044687070411157, 455.0000000000000568 ) ) ;
#41514=DIRECTION ( 'NONE',  ( 0.8660254037844363761, -0.5000000000000038858, 0.000000000000000000 ) ) ;
#41517=CARTESIAN_POINT ( 'NONE',  ( 4.186483450353423841, 11.99351654964658742, 455.0000000000000568 ) ) ;
#41518=EDGE_CURVE ( 'NONE', #34655, #15827, #57, .T. ) ;
#41522=ORIENTED_EDGE ( 'NONE', *, *, #9681, .F. ) ;
#41528=VECTOR ( 'NONE', #18889, 1000.000000000000000 ) ;
#41532=AXIS2_PLACEMENT_3D ( 'NONE', #1410, #50548, #43854 ) ;
#41548=ORIENTED_EDGE ( 'NONE', *, *, #26781, .F. ) ;
#41550=CARTESIAN_POINT ( 'NONE',  ( -10.91351654964670814, 2.893516549646604208, 195.0000000000000284 ) ) ;
#41555=LINE ( 'NONE', #58170, #57828 ) ;
#41556=ORIENTED_EDGE ( 'NONE', *, *, #3376, .T. ) ;
#41560=EDGE_CURVE ( 'NONE', #64638, #25131, #34119, .T. ) ;
#41572=ORIENTED_EDGE ( 'NONE', *, *, #9041, .T. ) ;
#41573=VERTEX_POINT ( 'NONE', #43351 ) ;
#41583=ORIENTED_EDGE ( 'NONE', *, *, #62602, .F. ) ;
#41587=VERTEX_POINT ( 'NONE', #17175 ) ;
#41593=EDGE_LOOP ( 'NONE', ( #15846, #28235, #56302, #58820 ) ) ;
#41594=DIRECTION ( 'NONE',  ( -1.836970198721029934E-16, 1.836970198721036344E-16, -1.000000000000000000 ) ) ;
#41595=CARTESIAN_POINT ( 'NONE',  ( -10.19191654964671301, 10.19191654964664018, 195.0000000000000284 ) ) ;
#41599=EDGE_CURVE ( 'NONE', #2177, #22188, #49381, .T. ) ;
#41608=LINE ( 'NONE', #63174, #34538 ) ;
#41609=EDGE_CURVE ( 'NONE', #65753, #27294, #12209, .T. ) ;
#41613=CARTESIAN_POINT ( 'NONE',  ( 4.740315990920191958, 4.188533722949208560, 455.0000000000000568 ) ) ;
#41623=EDGE_LOOP ( 'NONE', ( #48484, #66229, #63384, #40445 ) ) ;
#41625=ORIENTED_EDGE ( 'NONE', *, *, #57857, .F. ) ;
#41636=DIRECTION ( 'NONE',  ( -0.000000000000000000, 3.673940397442059868E-16, -1.000000000000000000 ) ) ;
#41637=VERTEX_POINT ( 'NONE', #33782 ) ;
#41641=DIRECTION ( 'NONE',  ( 0.000000000000000000, -0.000000000000000000, -1.000000000000000000 ) ) ;
#41651=DIRECTION ( 'NONE',  ( 0.000000000000000000, -1.000000000000000000, -3.673940397442059868E-16 ) ) ;
#41652=EDGE_LOOP ( 'NONE', ( #65469, #20763, #30612, #24984 ) ) ;
#41654=EDGE_CURVE ( 'NONE', #32917, #51761, #28815, .T. ) ;
#41656=CARTESIAN_POINT ( 'NONE',  ( 9.106483450353417552, 10.91351654964656603, 455.0000000000000568 ) ) ;
#41660=CARTESIAN_POINT ( 'NONE',  ( -10.73351654964664981, -1.690483450353293948, 195.0000000000000284 ) ) ;
#41670=VECTOR ( 'NONE', #65475, 1000.000000000000000 ) ;
#41683=DIRECTION ( 'NONE',  ( -1.000000000000000000, 3.491481338843132961E-15, 1.836970198721036344E-16 ) ) ;
#41687=FACE_OUTER_BOUND ( 'NONE', #26175, .T. ) ;
#41702=CARTESIAN_POINT ( 'NONE',  ( -7.603567055985586798, -8.406483450353363196, 195.0000000000000284 ) ) ;
#41706=ADVANCED_FACE ( 'NONE', ( #35166 ), #51447, .F. ) ;
#41722=VECTOR ( 'NONE', #67818, 1000.000000000000000 ) ;
#41723=ORIENTED_EDGE ( 'NONE', *, *, #33297, .F. ) ;
#41726=DIRECTION ( 'NONE',  ( 9.799566706031580591E-15, 1.000000000000000000, 1.836970198721018348E-16 ) ) ;
#41732=ORIENTED_EDGE ( 'NONE', *, *, #48720, .F. ) ;
#41735=ORIENTED_EDGE ( 'NONE', *, *, #3710, .T. ) ;
#41757=EDGE_LOOP ( 'NONE', ( #21197, #46163, #43474, #1564 ) ) ;
#41758=EDGE_LOOP ( 'NONE', ( #68880, #32166, #59244, #6738 ) ) ;
#41759=DIRECTION ( 'NONE',  ( 1.836970198721029934E-16, 1.836970198721010706E-16, -1.000000000000000000 ) ) ;
#41767=LINE ( 'NONE', #43512, #53010 ) ;
#41770=ADVANCED_FACE ( 'NONE', ( #51799 ), #62748, .T. ) ;
#41774=DIRECTION ( 'NONE',  ( -0.000000000000000000, 3.673940397442059868E-16, -1.000000000000000000 ) ) ;
#41791=DIRECTION ( 'NONE',  ( -0.000000000000000000, -0.000000000000000000, -1.000000000000000000 ) ) ;
#41798=DIRECTION ( 'NONE',  ( -1.000000000000000000, 0.000000000000000000, 0.000000000000000000 ) ) ;
#41803=ORIENTED_EDGE ( 'NONE', *, *, #32603, .T. ) ;
#41811=EDGE_CURVE ( 'NONE', #65753, #59053, #61337, .T. ) ;
#41815=CARTESIAN_POINT ( 'NONE',  ( -11.77351654964670935, 4.173516549646604901, 455.0000000000000568 ) ) ;
#41818=ORIENTED_EDGE ( 'NONE', *, *, #17557, .F. ) ;
#41828=VERTEX_POINT ( 'NONE', #36951 ) ;
#41836=ORIENTED_EDGE ( 'NONE', *, *, #26779, .T. ) ;
#41837=CARTESIAN_POINT ( 'NONE',  ( 11.48848345035342078, 11.07551654964652599, 455.0000000000000568 ) ) ;
#41846=ORIENTED_EDGE ( 'NONE', *, *, #62111, .T. ) ;
#41852=CARTESIAN_POINT ( 'NONE',  ( -5.993516549646728642, -6.006483450353378828, 195.0000000000000284 ) ) ;
#41853=EDGE_CURVE ( 'NONE', #30539, #2766, #30930, .T. ) ;
#41865=EDGE_CURVE ( 'NONE', #8459, #21517, #47545, .T. ) ;
#41871=AXIS2_PLACEMENT_3D ( 'NONE', #40083, #55670, #56023 ) ;
#41875=DIRECTION ( 'NONE',  ( -0.000000000000000000, -0.000000000000000000, -1.000000000000000000 ) ) ;
#41878=DIRECTION ( 'NONE',  ( 1.836970198721029934E-16, 1.836970198721010706E-16, -1.000000000000000000 ) ) ;
#41879=CYLINDRICAL_SURFACE ( 'NONE', #10549, 0.5999999999999989786 ) ;
#41895=DIRECTION ( 'NONE',  ( -1.000000000000000000, 0.000000000000000000, 0.000000000000000000 ) ) ;
#41896=DIRECTION ( 'NONE',  ( 2.135044278125299371E-15, 1.000000000000000000, 0.000000000000000000 ) ) ;
#41917=EDGE_CURVE ( 'NONE', #60141, #13479, #24801, .T. ) ;
#41922=EDGE_CURVE ( 'NONE', #5458, #33631, #8174, .T. ) ;
#41923=AXIS2_PLACEMENT_3D ( 'NONE', #28032, #31954, #11415 ) ;
#41927=VECTOR ( 'NONE', #32638, 1000.000000000000000 ) ;
#41934=VECTOR ( 'NONE', #3275, 1000.000000000000000 ) ;
#41936=EDGE_CURVE ( 'NONE', #14411, #30184, #45301, .T. ) ;
#41937=VECTOR ( 'NONE', #37051, 1000.000000000000000 ) ;
#41946=ORIENTED_EDGE ( 'NONE', *, *, #10739, .T. ) ;
#41950=CARTESIAN_POINT ( 'NONE',  ( -5.655420232009250370, 8.393516549646600211, 455.0000000000000568 ) ) ;
#41952=LINE ( 'NONE', #51515, #12751 ) ;
#41956=EDGE_CURVE ( 'NONE', #20447, #46212, #61561, .T. ) ;
#41958=CARTESIAN_POINT ( 'NONE',  ( -8.393516549646744096, -4.396432944014549093, 455.0000000000000568 ) ) ;
#41961=CARTESIAN_POINT ( 'NONE',  ( -11.11351654964671098, 4.193516549646605363, 455.0000000000000568 ) ) ;
#41970=LINE ( 'NONE', #62840, #27651 ) ;
#41992=LINE ( 'NONE', #10166, #57571 ) ;
#41993=DIRECTION ( 'NONE',  ( -1.000000000000000000, 8.728482790395504563E-15, 0.000000000000000000 ) ) ;
#41994=CARTESIAN_POINT ( 'NONE',  ( -4.383466043307968185, -8.406483450353443132, 455.0000000000000568 ) ) ;
#41995=VERTEX_POINT ( 'NONE', #56961 ) ;
#42005=EDGE_CURVE ( 'NONE', #59475, #35467, #61924, .T. ) ;
#42016=ORIENTED_EDGE ( 'NONE', *, *, #21423, .F. ) ;
#42023=VECTOR ( 'NONE', #31789, 1000.000000000000000 ) ;
#42036=CARTESIAN_POINT ( 'NONE',  ( 7.616533956692198792, 8.593516549646622593, 195.0000000000000284 ) ) ;
#42037=CARTESIAN_POINT ( 'NONE',  ( 4.406483450353335662, -11.78648345035337996, 195.0000000000000284 ) ) ;
#42038=ORIENTED_EDGE ( 'NONE', *, *, #55981, .T. ) ;
#42039=CARTESIAN_POINT ( 'NONE',  ( -11.47551654964683010, -11.08848345035333338, 455.0000000000000568 ) ) ;
#42062=ORIENTED_EDGE ( 'NONE', *, *, #52223, .T. ) ;
#42063=DIRECTION ( 'NONE',  ( -7.665540703601094997E-15, -1.000000000000000000, 0.000000000000000000 ) ) ;
#42073=DIRECTION ( 'NONE',  ( -0.000000000000000000, -0.000000000000000000, -1.000000000000000000 ) ) ;
#42075=ORIENTED_EDGE ( 'NONE', *, *, #6233, .F. ) ;
#42079=CARTESIAN_POINT ( 'NONE',  ( 4.206483450353343478, -11.12648345035347575, 455.0000000000000568 ) ) ;
#42080=ORIENTED_EDGE ( 'NONE', *, *, #36737, .T. ) ;
#42087=ORIENTED_EDGE ( 'NONE', *, *, #1712, .T. ) ;
#42091=DIRECTION ( 'NONE',  ( 1.836970198721029934E-16, -1.836970198721036344E-16, 1.000000000000000000 ) ) ;
#42098=CARTESIAN_POINT ( 'NONE',  ( 7.606483450353420217, 11.31351654964657349, 455.0000000000000568 ) ) ;
#42105=ORIENTED_EDGE ( 'NONE', *, *, #5492, .F. ) ;
#42106=VECTOR ( 'NONE', #35037, 1000.000000000000000 ) ;
#42116=DIRECTION ( 'NONE',  ( 0.000000000000000000, -3.673940397442059868E-16, 1.000000000000000000 ) ) ;
#42120=FILL_AREA_STYLE ('',( #20560 ) ) ;
#42127=LINE ( 'NONE', #38238, #11495 ) ;
#42140=DIRECTION ( 'NONE',  ( 0.000000000000000000, -3.673940397442059868E-16, 1.000000000000000000 ) ) ;
#42145=DIRECTION ( 'NONE',  ( -0.000000000000000000, -0.000000000000000000, -1.000000000000000000 ) ) ;
#42150=VECTOR ( 'NONE', #67060, 1000.000000000000114 ) ;
#42159=CARTESIAN_POINT ( 'NONE',  ( 9.417013320880768035, 1.853252480934615809, 455.0000000000000568 ) ) ;
#42160=CARTESIAN_POINT ( 'NONE',  ( -9.791916549646867196, -11.08848345035335115, 455.0000000000000568 ) ) ;
#42169=LINE ( 'NONE', #40779, #17396 ) ;
#42170=EDGE_CURVE ( 'NONE', #19296, #6331, #54474, .T. ) ;
#42178=DIRECTION ( 'NONE',  ( 1.836970198721029934E-16, 1.836970198721010706E-16, -1.000000000000000000 ) ) ;
#42181=LINE ( 'NONE', #14274, #14170 ) ;
#42184=VERTEX_POINT ( 'NONE', #12001 ) ;
#42189=EDGE_CURVE ( 'NONE', #22125, #21000, #733, .T. ) ;
#42194=DIRECTION ( 'NONE',  ( -1.062171939662868249E-14, -1.000000000000000000, 0.000000000000000000 ) ) ;
#42198=ORIENTED_EDGE ( 'NONE', *, *, #42746, .T. ) ;
#42200=DIRECTION ( 'NONE',  ( -0.000000000000000000, 3.673940397442059868E-16, -1.000000000000000000 ) ) ;
#42201=AXIS2_PLACEMENT_3D ( 'NONE', #16714, #49240, #28684 ) ;
#42205=AXIS2_PLACEMENT_3D ( 'NONE', #25786, #37779, #36376 ) ;
#42207=VECTOR ( 'NONE', #39310, 1000.000000000000000 ) ;
#42211=CARTESIAN_POINT ( 'NONE',  ( -10.91351654964670992, -2.706483450353338593, 455.0000000000000568 ) ) ;
#42212=PLANE ( 'NONE',  #60535 ) ;
#42222=PLANE ( 'NONE',  #8289 ) ;
#42225=CARTESIAN_POINT ( 'NONE',  ( 12.00648345035338060, -7.826483450353491023, 455.0000000000000568 ) ) ;
#42227=ADVANCED_FACE ( 'NONE', ( #17313 ), #27587, .T. ) ;
#42231=AXIS2_PLACEMENT_3D ( 'NONE', #21205, #16589, #65028 ) ;
#42233=DIRECTION ( 'NONE',  ( 0.7071067811865401342, -0.7071067811865550112, -1.355854680848614216E-30 ) ) ;
#42234=EDGE_CURVE ( 'NONE', #23727, #25048, #63330, .T. ) ;
#42244=ORIENTED_EDGE ( 'NONE', *, *, #10733, .T. ) ;
#42261=VECTOR ( 'NONE', #66504, 1000.000000000000000 ) ;
#42292=VECTOR ( 'NONE', #18442, 1000.000000000000000 ) ;
#42293=CARTESIAN_POINT ( 'NONE',  ( -7.793516549646712477, 11.11351654964660085, 455.0000000000000568 ) ) ;
#42306=ADVANCED_FACE ( 'NONE', ( #44880 ), #44519, .F. ) ;
#42312=EDGE_CURVE ( 'NONE', #7744, #62134, #43589, .T. ) ;
#42317=EDGE_CURVE ( 'NONE', #2837, #20689, #65845, .T. ) ;
#42319=ORIENTED_EDGE ( 'NONE', *, *, #37854, .T. ) ;
#42329=EDGE_CURVE ( 'NONE', #22525, #9315, #35143, .T. ) ;
#42331=ORIENTED_EDGE ( 'NONE', *, *, #46875, .T. ) ;
#42337=CARTESIAN_POINT ( 'NONE',  ( 4.255011587777269177, 8.452095193409277840, 455.0000000000000568 ) ) ;
#42338=ORIENTED_EDGE ( 'NONE', *, *, #49985, .F. ) ;
#42347=FACE_OUTER_BOUND ( 'NONE', #28476, .T. ) ;
#42350=VECTOR ( 'NONE', #36243, 1000.000000000000000 ) ;
#42372=LINE ( 'NONE', #65343, #44831 ) ;
#42377=CARTESIAN_POINT ( 'NONE',  ( 1.866219381641437636, 9.404046420174054788, 195.0000000000000284 ) ) ;
#42379=DIRECTION ( 'NONE',  ( 1.836970198721029934E-16, 1.836970198721010706E-16, -1.000000000000000000 ) ) ;
#42392=VECTOR ( 'NONE', #43048, 1000.000000000000000 ) ;
#42394=DIRECTION ( 'NONE',  ( -4.336808689942025625E-15, -1.000000000000000000, 0.000000000000000000 ) ) ;
#42395=CARTESIAN_POINT ( 'NONE',  ( -2.752095193409374030, 9.942044687070435316, 455.0000000000000568 ) ) ;
#42406=CARTESIAN_POINT ( 'NONE',  ( 7.806483450353379538, -11.12648345035348996, 455.0000000000000568 ) ) ;
#42408=CARTESIAN_POINT ( 'NONE',  ( -4.727349090213463612, 7.798499376343949407, 455.0000000000000568 ) ) ;
#42413=ORIENTED_EDGE ( 'NONE', *, *, #3371, .F. ) ;
#42419=DIRECTION ( 'NONE',  ( 0.6414496315691494699, -0.7671651518153064231, 0.000000000000000000 ) ) ;
#42427=ORIENTED_EDGE ( 'NONE', *, *, #14626, .F. ) ;
#42428=DIRECTION ( 'NONE',  ( -0.000000000000000000, -0.000000000000000000, -1.000000000000000000 ) ) ;
#42439=ORIENTED_EDGE ( 'NONE', *, *, #25528, .T. ) ;
#42452=CARTESIAN_POINT ( 'NONE',  ( 8.406483450353405829, 7.603567055985406498, 455.0000000000000568 ) ) ;
#42456=LINE ( 'NONE', #64044, #31978 ) ;
#42472=DIRECTION ( 'NONE',  ( -3.491481338843132961E-15, -1.000000000000000000, -1.836970198721029934E-16 ) ) ;
#42488=EDGE_CURVE ( 'NONE', #8621, #61820, #38972, .T. ) ;
#42493=EDGE_CURVE ( 'NONE', #43288, #36372, #7479, .T. ) ;
#42496=EDGE_CURVE ( 'NONE', #61169, #9593, #27253, .T. ) ;
#42499=ORIENTED_EDGE ( 'NONE', *, *, #1740, .T. ) ;
#42500=ORIENTED_EDGE ( 'NONE', *, *, #27489, .T. ) ;
#42502=AXIS2_PLACEMENT_3D ( 'NONE', #4734, #64149, #26297 ) ;
#42505=AXIS2_PLACEMENT_3D ( 'NONE', #69305, #9926, #25835 ) ;
#42506=AXIS2_PLACEMENT_3D ( 'NONE', #46793, #64384, #19572 ) ;
#42508=CARTESIAN_POINT ( 'NONE',  ( 7.757955312929553315, 8.452095193409265406, 455.0000000000000568 ) ) ;
#42511=LINE ( 'NONE', #64099, #52091 ) ;
#42520=LINE ( 'NONE', #64790, #13105 ) ;
#42523=ORIENTED_EDGE ( 'NONE', *, *, #11393, .T. ) ;
#42524=VERTEX_POINT ( 'NONE', #60536 ) ;
#42528=VERTEX_POINT ( 'NONE', #39652 ) ;
#42532=EDGE_CURVE ( 'NONE', #57915, #10108, #12096, .T. ) ;
#42540=ORIENTED_EDGE ( 'NONE', *, *, #37349, .T. ) ;
#42543=DIRECTION ( 'NONE',  ( -1.836970198721029934E-16, 1.836970198721036344E-16, -1.000000000000000000 ) ) ;
#42546=ORIENTED_EDGE ( 'NONE', *, *, #25476, .F. ) ;
#42551=PLANE ( 'NONE',  #14248 ) ;
#42563=CARTESIAN_POINT ( 'NONE',  ( 9.106483450353417552, 10.91351654964656603, 455.0000000000000568 ) ) ;
#42567=DIRECTION ( 'NONE',  ( 0.7071067811865474617, -0.7071067811865474617, -2.597868168706479611E-16 ) ) ;
#42570=DIRECTION ( 'NONE',  ( -8.359604446858500663E-15, -1.000000000000000000, 0.000000000000000000 ) ) ;
#42572=EDGE_CURVE ( 'NONE', #26427, #61169, #56275, .T. ) ;
#42588=AXIS2_PLACEMENT_3D ( 'NONE', #55422, #60713, #44104 ) ;
#42601=VERTEX_POINT ( 'NONE', #20194 ) ;
#42612=AXIS2_PLACEMENT_3D ( 'NONE', #45, #1412, #22976 ) ;
#42621=CARTESIAN_POINT ( 'NONE',  ( -8.393516549646712122, 4.383466043307770121, 455.0000000000000568 ) ) ;
#42631=CIRCLE ( 'NONE', #69708, 1.399999999999998579 ) ;
#42633=AXIS2_PLACEMENT_3D ( 'NONE', #2535, #34712, #56289 ) ;
#42634=EDGE_CURVE ( 'NONE', #48721, #3757, #30456, .T. ) ;
#42637=VECTOR ( 'NONE', #34657, 1000.000000000000000 ) ;
#42638=CIRCLE ( 'NONE', #30228, 0.1999999999999996503 ) ;
#42641=LINE ( 'NONE', #32393, #61806 ) ;
#42642=CARTESIAN_POINT ( 'NONE',  ( -1.677516549646777877, -10.74648345035342167, 195.0000000000000284 ) ) ;
#42646=AXIS2_PLACEMENT_3D ( 'NONE', #56727, #34439, #18540 ) ;
#42658=DIRECTION ( 'NONE',  ( 3.491481338843133355E-15, 1.000000000000000000, 1.836970198721029934E-16 ) ) ;
#42662=DIRECTION ( 'NONE',  ( -1.836970198721029934E-16, 1.836970198721036344E-16, -1.000000000000000000 ) ) ;
#42665=FACE_OUTER_BOUND ( 'NONE', #19705, .T. ) ;
#42670=EDGE_CURVE ( 'NONE', #62883, #21000, #46360, .T. ) ;
#42675=CARTESIAN_POINT ( 'NONE',  ( -10.19191654964671301, 9.791916549646639822, 195.0000000000000284 ) ) ;
#42677=AXIS2_PLACEMENT_3D ( 'NONE', #12119, #39341, #60900 ) ;
#42678=VERTEX_POINT ( 'NONE', #47074 ) ;
#42682=FACE_OUTER_BOUND ( 'NONE', #63373, .T. ) ;
#42684=ORIENTED_EDGE ( 'NONE', *, *, #9616, .F. ) ;
#42689=DIRECTION ( 'NONE',  ( -1.836970198721029934E-16, 1.836970198721036344E-16, -1.000000000000000000 ) ) ;
#42695=VECTOR ( 'NONE', #3503, 1000.000000000000114 ) ;
#42707=EDGE_CURVE ( 'NONE', #52260, #34851, #48124, .T. ) ;
#42708=VECTOR ( 'NONE', #26664, 1000.000000000000000 ) ;
#42720=CARTESIAN_POINT ( 'NONE',  ( -10.91351654964671525, -2.906483450353338771, 455.0000000000000568 ) ) ;
#42726=LINE ( 'NONE', #58654, #16264 ) ;
#42727=DIRECTION ( 'NONE',  ( -1.836970198721029934E-16, 1.836970198721036344E-16, -1.000000000000000000 ) ) ;
#42728=EDGE_CURVE ( 'NONE', #52264, #64997, #15610, .T. ) ;
#42734=ORIENTED_EDGE ( 'NONE', *, *, #47551, .F. ) ;
#42736=LINE ( 'NONE', #4918, #16957 ) ;
#42743=ADVANCED_FACE ( 'NONE', ( #64392 ), #65085, .F. ) ;
#42744=DIRECTION ( 'NONE',  ( -1.000000000000000000, 1.047444401652940007E-14, -1.836970198721010706E-16 ) ) ;
#42746=EDGE_CURVE ( 'NONE', #6513, #35140, #30671, .T. ) ;
#42750=LINE ( 'NONE', #35684, #10646 ) ;
#42753=CARTESIAN_POINT ( 'NONE',  ( 11.78648345035337996, 4.173516549646518747, 455.0000000000000568 ) ) ;
#42755=FACE_OUTER_BOUND ( 'NONE', #3075, .T. ) ;
#42766=LINE ( 'NONE', #46666, #38216 ) ;
#42781=DIRECTION ( 'NONE',  ( -4.745709458399858621E-16, -1.000000000000000000, 0.000000000000000000 ) ) ;
#42794=PLANE ( 'NONE',  #12034 ) ;
#42799=AXIS2_PLACEMENT_3D ( 'NONE', #66706, #2357, #17915 ) ;
#42806=CARTESIAN_POINT ( 'NONE',  ( -4.193516549646675529, 11.11351654964658664, 455.0000000000000568 ) ) ;
#42813=DIRECTION ( 'NONE',  ( -1.836970198721029934E-16, 1.836970198721036344E-16, -1.000000000000000000 ) ) ;
#42816=LINE ( 'NONE', #59081, #45931 ) ;
#42817=CARTESIAN_POINT ( 'NONE',  ( -7.603567055985545942, 8.393516549646601987, 195.0000000000000284 ) ) ;
#42819=CARTESIAN_POINT ( 'NONE',  ( -7.603567055985634759, -8.406483450353409381, 455.0000000000000568 ) ) ;
#42821=ORIENTED_EDGE ( 'NONE', *, *, #52172, .T. ) ;
#42823=( NAMED_UNIT ( * ) PLANE_ANGLE_UNIT ( ) SI_UNIT ( $, .RADIAN. ) );
#42839=VECTOR ( 'NONE', #37825, 1000.000000000000000 ) ;
#42840=ADVANCED_FACE ( 'NONE', ( #45220 ), #66789, .F. ) ;
#42848=AXIS2_PLACEMENT_3D ( 'NONE', #26730, #48297, #17406 ) ;
#42850=FACE_OUTER_BOUND ( 'NONE', #12016, .T. ) ;
#42859=CARTESIAN_POINT ( 'NONE',  ( -8.393516549646697911, -4.396432944014502020, 195.0000000000000284 ) ) ;
#42868=CARTESIAN_POINT ( 'NONE',  ( -7.593516549646791347, -11.78648345035336042, 195.0000000000000284 ) ) ;
#42871=CARTESIAN_POINT ( 'NONE',  ( -4.727349090213512461, -7.811466277050747919, 195.0000000000000284 ) ) ;
#42873=ORIENTED_EDGE ( 'NONE', *, *, #58215, .F. ) ;
#42876=EDGE_CURVE ( 'NONE', #46850, #24181, #67921, .T. ) ;
#42888=CARTESIAN_POINT ( 'NONE',  ( -4.188533722949335569, 4.727349090213398775, 195.0000000000000284 ) ) ;
#42894=LINE ( 'NONE', #60534, #24572 ) ;
#42895=DIRECTION ( 'NONE',  ( 0.7671651518153105309, 0.6414496315691445849, 2.356647714346206145E-16 ) ) ;
#42922=AXIS2_PLACEMENT_3D ( 'NONE', #57482, #3395, #30967 ) ;
#42928=DIRECTION ( 'NONE',  ( -0.000000000000000000, -0.000000000000000000, -1.000000000000000000 ) ) ;
#42931=CARTESIAN_POINT ( 'NONE',  ( 4.201500623656003519, -7.272650909786698037, 455.0000000000000568 ) ) ;
#42941=LINE ( 'NONE', #11452, #27084 ) ;
#42948=ORIENTED_EDGE ( 'NONE', *, *, #47864, .F. ) ;
#42960=CARTESIAN_POINT ( 'NONE',  ( 4.186483450353335023, -12.00648345035338238, 195.0000000000000284 ) ) ;
#42962=ORIENTED_EDGE ( 'NONE', *, *, #38363, .F. ) ;
#42968=EDGE_CURVE ( 'NONE', #13563, #29083, #25070, .T. ) ;
#42978=DIRECTION ( 'NONE',  ( -0.000000000000000000, 3.673940397442059868E-16, -1.000000000000000000 ) ) ;
#42979=AXIS2_PLACEMENT_3D ( 'NONE', #58398, #26914, #63340 ) ;
#42986=CARTESIAN_POINT ( 'NONE',  ( -11.18071654964669825, 11.99351654964660341, 195.0000000000000284 ) ) ;
#42987=ORIENTED_EDGE ( 'NONE', *, *, #55410, .T. ) ;
#42989=DIRECTION ( 'NONE',  ( -1.000000000000000000, 0.000000000000000000, 0.000000000000000000 ) ) ;
#42995=DIRECTION ( 'NONE',  ( 0.000000000000000000, 0.000000000000000000, 1.000000000000000000 ) ) ;
#42999=ORIENTED_EDGE ( 'NONE', *, *, #16058, .T. ) ;
#43010=EDGE_CURVE ( 'NONE', #22374, #36022, #29724, .T. ) ;
#43024=CARTESIAN_POINT ( 'NONE',  ( -2.693516549646780334, -10.92648345035340895, 195.0000000000000284 ) ) ;
#43025=VERTEX_POINT ( 'NONE', #15167 ) ;
#43028=VECTOR ( 'NONE', #20111, 1000.000000000000000 ) ;
#43034=AXIS2_PLACEMENT_3D ( 'NONE', #66452, #17670, #27255 ) ;
#43045=VECTOR ( 'NONE', #5905, 1000.000000000000000 ) ;
#43048=DIRECTION ( 'NONE',  ( -0.000000000000000000, 3.673940397442059868E-16, -1.000000000000000000 ) ) ;
#43058=ADVANCED_FACE ( 'NONE', ( #65344 ), #5597, .F. ) ;
#43061=EDGE_CURVE ( 'NONE', #29674, #40641, #10546, .T. ) ;
#43069=EDGE_CURVE ( 'NONE', #27985, #31340, #4562, .T. ) ;
#43072=DIRECTION ( 'NONE',  ( 0.7071067811865441310, -0.7071067811865510144, -2.597868168706485034E-16 ) ) ;
#43075=DIRECTION ( 'NONE',  ( -0.000000000000000000, 3.673940397442059868E-16, -1.000000000000000000 ) ) ;
#43078=DIRECTION ( 'NONE',  ( 8.673617379884051249E-15, 1.000000000000000000, 0.000000000000000000 ) ) ;
#43103=CARTESIAN_POINT ( 'NONE',  ( -10.91351654964670814, 2.893516549646604208, 455.0000000000000568 ) ) ;
#43104=ORIENTED_EDGE ( 'NONE', *, *, #3490, .T. ) ;
#43106=CARTESIAN_POINT ( 'NONE',  ( 11.78648345035337996, 4.393516549646516722, 455.0000000000000568 ) ) ;
#43112=VERTEX_POINT ( 'NONE', #58650 ) ;
#43132=DIRECTION ( 'NONE',  ( 0.000000000000000000, -3.673940397442059868E-16, 1.000000000000000000 ) ) ;
#43136=ORIENTED_EDGE ( 'NONE', *, *, #68111, .T. ) ;
#43146=CARTESIAN_POINT ( 'NONE',  ( 12.00648345035340903, 7.813516549646560172, 455.0000000000000568 ) ) ;
#43149=EDGE_CURVE ( 'NONE', #14943, #48678, #33148, .T. ) ;
#43150=DIRECTION ( 'NONE',  ( 1.000000000000000000, -1.047444401652939849E-14, 0.000000000000000000 ) ) ;
#43158=DIRECTION ( 'NONE',  ( -1.836970198721029934E-16, -1.836970198721010706E-16, 1.000000000000000000 ) ) ;
#43163=DIRECTION ( 'NONE',  ( 1.000000000000000000, 1.570596175624152290E-15, 5.770276737693577136E-31 ) ) ;
#43167=CARTESIAN_POINT ( 'NONE',  ( 4.622483450353380263, -3.606483450353491271, 455.0000000000000568 ) ) ;
#43171=LINE ( 'NONE', #49182, #7536 ) ;
#43175=LINE ( 'NONE', #54501, #50898 ) ;
#43186=ORIENTED_EDGE ( 'NONE', *, *, #6953, .T. ) ;
#43190=CARTESIAN_POINT ( 'NONE',  ( 8.211283450353379365, -6.006483450353490738, 455.0000000000000568 ) ) ;
#43193=VECTOR ( 'NONE', #51737, 1000.000000000000000 ) ;
#43198=ORIENTED_EDGE ( 'NONE', *, *, #65542, .F. ) ;
#43211=LINE ( 'NONE', #31577, #34544 ) ;
#43221=VECTOR ( 'NONE', #45942, 1000.000000000000000 ) ;
#43223=EDGE_CURVE ( 'NONE', #45713, #8019, #34869, .T. ) ;
#43225=DIRECTION ( 'NONE',  ( -1.000000000000000000, 0.000000000000000000, 0.000000000000000000 ) ) ;
#43232=DIRECTION ( 'NONE',  ( -0.000000000000000000, -0.000000000000000000, -1.000000000000000000 ) ) ;
#43245=DIRECTION ( 'NONE',  ( -1.000000000000000000, 8.728482790395504563E-15, 0.000000000000000000 ) ) ;
#43246=LINE ( 'NONE', #65849, #21045 ) ;
#43251=DIRECTION ( 'NONE',  ( -1.000000000000000000, 0.000000000000000000, 0.000000000000000000 ) ) ;
#43254=AXIS2_PLACEMENT_3D ( 'NONE', #60156, #1125, #39285 ) ;
#43258=CARTESIAN_POINT ( 'NONE',  ( -1.677516549646816291, -9.841277389592811176, 455.0000000000000568 ) ) ;
#43260=LINE ( 'NONE', #16393, #43819 ) ;
#43261=VERTEX_POINT ( 'NONE', #62809 ) ;
#43279=EDGE_CURVE ( 'NONE', #5119, #54829, #52565, .T. ) ;
#43282=EDGE_CURVE ( 'NONE', #43722, #54865, #6478, .T. ) ;
#43286=ORIENTED_EDGE ( 'NONE', *, *, #6029, .F. ) ;
#43288=VERTEX_POINT ( 'NONE', #26042 ) ;
#43291=PLANE ( 'NONE',  #55612 ) ;
#43299=CARTESIAN_POINT ( 'NONE',  ( 1.690483450353344352, -10.74648345035336128, 195.0000000000000284 ) ) ;
#43301=SHAPE_REPRESENTATION_RELATIONSHIP ( 'NONE' , 'NONE' ,  #35, #21682 ) ;
#43302=VECTOR ( 'NONE', #15968, 1000.000000000000114 ) ;
#43305=ORIENTED_EDGE ( 'NONE', *, *, #50785, .T. ) ;
#43306=VERTEX_POINT ( 'NONE', #47948 ) ;
#43318=ORIENTED_EDGE ( 'NONE', *, *, #27055, .T. ) ;
#43319=CARTESIAN_POINT ( 'NONE',  ( -7.878491296477273309, 5.098491296477203782, 195.0000000000000284 ) ) ;
#43323=EDGE_CURVE ( 'NONE', #32671, #52471, #842, .T. ) ;
#43331=ORIENTED_EDGE ( 'NONE', *, *, #53138, .F. ) ;
#43341=VECTOR ( 'NONE', #53578, 1000.000000000000000 ) ;
#43344=CARTESIAN_POINT ( 'NONE',  ( -1.677516549646676625, 10.73351654964656987, 195.0000000000000284 ) ) ;
#43345=CARTESIAN_POINT ( 'NONE',  ( 8.606483450353380249, -4.396432944014657451, 455.0000000000000568 ) ) ;
#43351=CARTESIAN_POINT ( 'NONE',  ( -4.393516549646667713, 11.77351654964658856, 195.0000000000000284 ) ) ;
#43353=EDGE_CURVE ( 'NONE', #10322, #20182, #69516, .T. ) ;
#43362=ORIENTED_EDGE ( 'NONE', *, *, #25202, .T. ) ;
#43364=EDGE_CURVE ( 'NONE', #9367, #40219, #49599, .T. ) ;
#43369=VECTOR ( 'NONE', #11713, 1000.000000000000000 ) ;
#43371=VERTEX_POINT ( 'NONE', #10121 ) ;
#43386=ORIENTED_EDGE ( 'NONE', *, *, #3609, .F. ) ;
#43388=ORIENTED_EDGE ( 'NONE', *, *, #63743, .F. ) ;
#43391=CARTESIAN_POINT ( 'NONE',  ( 7.265214908726153276, 6.606374702650035680, 455.0000000000000568 ) ) ;
#43393=ORIENTED_EDGE ( 'NONE', *, *, #69806, .F. ) ;
#43403=DIRECTION ( 'NONE',  ( -0.000000000000000000, -0.000000000000000000, -1.000000000000000000 ) ) ;
#43404=EDGE_LOOP ( 'NONE', ( #65724, #36054, #51605, #41946 ) ) ;
#43410=PLANE ( 'NONE',  #16607 ) ;
#43413=ORIENTED_EDGE ( 'NONE', *, *, #15986, .T. ) ;
#43422=CARTESIAN_POINT ( 'NONE',  ( 4.186483450353335023, -12.00648345035347830, 455.0000000000000568 ) ) ;
#43424=DIRECTION ( 'NONE',  ( -1.000000000000000000, 0.000000000000000000, 0.000000000000000000 ) ) ;
#43425=VERTEX_POINT ( 'NONE', #56639 ) ;
#43428=AXIS2_PLACEMENT_3D ( 'NONE', #63296, #64681, #57983 ) ;
#43435=ORIENTED_EDGE ( 'NONE', *, *, #27244, .T. ) ;
#43444=ORIENTED_EDGE ( 'NONE', *, *, #42329, .F. ) ;
#43447=CARTESIAN_POINT ( 'NONE',  ( -11.77351654964669514, -4.406483450353273490, 195.0000000000000284 ) ) ;
#43452=LINE ( 'NONE', #37471, #46065 ) ;
#43453=CIRCLE ( 'NONE', #2814, 0.2000000000000000944 ) ;
#43460=VERTEX_POINT ( 'NONE', #12440 ) ;
#43461=CARTESIAN_POINT ( 'NONE',  ( -8.393516549646733438, -6.344579767990798480, 195.0000000000000284 ) ) ;
#43472=LINE ( 'NONE', #49485, #45656 ) ;
#43474=ORIENTED_EDGE ( 'NONE', *, *, #41922, .F. ) ;
#43476=ORIENTED_EDGE ( 'NONE', *, *, #60399, .T. ) ;
#43482=CARTESIAN_POINT ( 'NONE',  ( -11.11351654964668612, 8.693516549646636449, 195.0000000000000284 ) ) ;
#43485=ADVANCED_FACE ( 'NONE', ( #2891 ), #35059, .F. ) ;
#43488=AXIS2_PLACEMENT_3D ( 'NONE', #5630, #26854, #64666 ) ;
#43498=LINE ( 'NONE', #65087, #43653 ) ;
#43506=CARTESIAN_POINT ( 'NONE',  ( 7.806483450353379538, -11.32648345035339155, 195.0000000000000284 ) ) ;
#43512=CARTESIAN_POINT ( 'NONE',  ( -11.11351654964669322, -4.206483450353289300, 195.0000000000000284 ) ) ;
#43514=ORIENTED_EDGE ( 'NONE', *, *, #16406, .F. ) ;
#43520=ORIENTED_EDGE ( 'NONE', *, *, #68122, .T. ) ;
#43521=DIRECTION ( 'NONE',  ( -1.261617073437657735E-14, -1.000000000000000000, 0.000000000000000000 ) ) ;
#43526=CARTESIAN_POINT ( 'NONE',  ( -10.73351654964671020, 1.677516549646604016, 455.0000000000000568 ) ) ;
#43528=FACE_OUTER_BOUND ( 'NONE', #53178, .T. ) ;
#43532=ORIENTED_EDGE ( 'NONE', *, *, #55410, .F. ) ;
#43539=DIRECTION ( 'NONE',  ( -1.356437060717832013E-15, -1.000000000000000000, -1.836970198721033878E-16 ) ) ;
#43544=ORIENTED_EDGE ( 'NONE', *, *, #44237, .T. ) ;
#43554=FACE_OUTER_BOUND ( 'NONE', #38377, .T. ) ;
#43558=CARTESIAN_POINT ( 'NONE',  ( 6.006483450353401921, 5.993516549646582092, 455.0000000000000568 ) ) ;
#43559=CARTESIAN_POINT ( 'NONE',  ( 11.32648345035337734, -7.806483450353490561, 455.0000000000000568 ) ) ;
#43578=DIRECTION ( 'NONE',  ( 1.836970198721029934E-16, -1.836970198721036344E-16, 1.000000000000000000 ) ) ;
#43581=ORIENTED_EDGE ( 'NONE', *, *, #23703, .F. ) ;
#43589=LINE ( 'NONE', #21333, #65650 ) ;
#43593=DIRECTION ( 'NONE',  ( -0.7071067811865514585, -0.7071067811865435759, -2.597868168706465806E-16 ) ) ;
#43597=DIRECTION ( 'NONE',  ( -8.612436249475772606E-15, -1.000000000000000000, -1.836970198721020566E-16 ) ) ;
#43599=CIRCLE ( 'NONE', #40189, 0.3999999999999993006 ) ;
#43602=PLANE ( 'NONE',  #6644 ) ;
#43612=CIRCLE ( 'NONE', #67334, 2.204799999999996540 ) ;
#43622=EDGE_CURVE ( 'NONE', #38244, #68597, #41068, .T. ) ;
#43625=MANIFOLD_SOLID_BREP ( 'Scale1', #55513 ) ;
#43635=CARTESIAN_POINT ( 'NONE',  ( -10.91351654964670637, 2.693516549646604030, 195.0000000000000284 ) ) ;
#43637=CARTESIAN_POINT ( 'NONE',  ( -11.99351654964671354, 4.173516549646604901, 455.0000000000000568 ) ) ;
#43646=ORIENTED_EDGE ( 'NONE', *, *, #50732, .F. ) ;
#43648=CARTESIAN_POINT ( 'NONE',  ( 8.465062094116053260, 7.744988412222763685, 195.0000000000000284 ) ) ;
#43653=VECTOR ( 'NONE', #60106, 1000.000000000000000 ) ;
#43666=CARTESIAN_POINT ( 'NONE',  ( 4.186483450353422953, 11.77351654964658501, 455.0000000000000568 ) ) ;
#43669=VERTEX_POINT ( 'NONE', #16299 ) ;
#43680=DIRECTION ( 'NONE',  ( -0.000000000000000000, -0.000000000000000000, -1.000000000000000000 ) ) ;
#43682=ADVANCED_FACE ( 'NONE', ( #5707 ), #21617, .F. ) ;
#43684=EDGE_CURVE ( 'NONE', #22317, #21676, #33258, .T. ) ;
#43690=CARTESIAN_POINT ( 'NONE',  ( 7.826483450353421745, 11.77351654964657257, 455.0000000000000568 ) ) ;
#43696=CARTESIAN_POINT ( 'NONE',  ( 8.406483450353398723, 5.655420232009111814, 455.0000000000000568 ) ) ;
#43706=VERTEX_POINT ( 'NONE', #32914 ) ;
#43715=DIRECTION ( 'NONE',  ( 0.000000000000000000, -3.673940397442059868E-16, 1.000000000000000000 ) ) ;
#43716=DIRECTION ( 'NONE',  ( 1.062171939662868407E-14, 1.000000000000000000, 0.000000000000000000 ) ) ;
#43720=CARTESIAN_POINT ( 'NONE',  ( 5.668387132715968058, 8.393516549646582448, 455.0000000000000568 ) ) ;
#43722=VERTEX_POINT ( 'NONE', #48838 ) ;
#43734=VERTEX_POINT ( 'NONE', #17330 ) ;
#43735=DIRECTION ( 'NONE',  ( -3.614007241618349165E-15, -1.000000000000000000, 0.000000000000000000 ) ) ;
#43736=VERTEX_POINT ( 'NONE', #59785 ) ;
#43752=VECTOR ( 'NONE', #58518, 1000.000000000000000 ) ;
#43757=ORIENTED_EDGE ( 'NONE', *, *, #69227, .F. ) ;
#43760=CIRCLE ( 'NONE', #55027, 0.3999999999999993006 ) ;
#43775=VERTEX_POINT ( 'NONE', #2804 ) ;
#43781=ORIENTED_EDGE ( 'NONE', *, *, #11513, .T. ) ;
#43791=CARTESIAN_POINT ( 'NONE',  ( 4.186483450353375879, 11.77351654964663119, 195.0000000000000284 ) ) ;
#43797=CARTESIAN_POINT ( 'NONE',  ( -6.606374702650169795, 7.252248008019352099, 455.0000000000000568 ) ) ;
#43808=DIRECTION ( 'NONE',  ( -1.000000000000000000, 1.254221251785257731E-14, 1.836970198721053107E-16 ) ) ;
#43810=VECTOR ( 'NONE', #1860, 1000.000000000000000 ) ;
#43814=ORIENTED_EDGE ( 'NONE', *, *, #38624, .T. ) ;
#43815=VERTEX_POINT ( 'NONE', #18357 ) ;
#43819=VECTOR ( 'NONE', #59874, 1000.000000000000000 ) ;
#43820=LINE ( 'NONE', #54438, #53054 ) ;
#43821=PLANE ( 'NONE',  #34659 ) ;
#43822=PLANE ( 'NONE',  #6121 ) ;
#43833=ADVANCED_FACE ( 'NONE', ( #45583 ), #44898, .F. ) ;
#43834=DIRECTION ( 'NONE',  ( -0.000000000000000000, -0.000000000000000000, -1.000000000000000000 ) ) ;
#43836=VERTEX_POINT ( 'NONE', #22983 ) ;
#43839=ORIENTED_EDGE ( 'NONE', *, *, #63227, .T. ) ;
#43851=ORIENTED_EDGE ( 'NONE', *, *, #35566, .T. ) ;
#43853=ORIENTED_EDGE ( 'NONE', *, *, #12214, .T. ) ;
#43854=DIRECTION ( 'NONE',  ( 1.067128122525083795E-14, 1.000000000000000000, 0.000000000000000000 ) ) ;
#43855=CIRCLE ( 'NONE', #19015, 2.204799999999997429 ) ;
#43861=ORIENTED_EDGE ( 'NONE', *, *, #36665, .F. ) ;
#43862=LINE ( 'NONE', #66464, #22554 ) ;
#43868=PLANE ( 'NONE',  #4181 ) ;
#43873=VERTEX_POINT ( 'NONE', #24732 ) ;
#43874=LINE ( 'NONE', #65452, #16557 ) ;
#43883=ADVANCED_FACE ( 'NONE', ( #31455 ), #68574, .F. ) ;
#43894=EDGE_LOOP ( 'NONE', ( #30676, #3256, #45977, #43781 ) ) ;
#43909=ADVANCED_FACE ( 'NONE', ( #25795 ), #25087, .F. ) ;
#43917=VECTOR ( 'NONE', #4319, 1000.000000000000000 ) ;
#43924=ORIENTED_EDGE ( 'NONE', *, *, #55234, .T. ) ;
#43925=EDGE_CURVE ( 'NONE', #48692, #41078, #51608, .T. ) ;
#43931=ORIENTED_EDGE ( 'NONE', *, *, #2117, .F. ) ;
#43933=DIRECTION ( 'NONE',  ( 0.000000000000000000, 1.000000000000000000, 0.000000000000000000 ) ) ;
#43934=ADVANCED_FACE ( 'NONE', ( #35314 ), #68214, .F. ) ;
#43937=VECTOR ( 'NONE', #66691, 1000.000000000000000 ) ;
#43943=AXIS2_PLACEMENT_3D ( 'NONE', #30856, #21301, #48518 ) ;
#43944=DIRECTION ( 'NONE',  ( -1.836970198721029934E-16, 1.836970198721036344E-16, -1.000000000000000000 ) ) ;
#43947=CARTESIAN_POINT ( 'NONE',  ( 9.306483450353379538, -10.92648345035348534, 455.0000000000000568 ) ) ;
#43949=DIRECTION ( 'NONE',  ( -0.000000000000000000, 3.673940397442059868E-16, -1.000000000000000000 ) ) ;
#43957=AXIS2_PLACEMENT_3D ( 'NONE', #55693, #17867, #34112 ) ;
#43961=EDGE_CURVE ( 'NONE', #49212, #4106, #64651, .T. ) ;
#43967=EDGE_LOOP ( 'NONE', ( #17553, #66552, #17066, #50314 ) ) ;
#43968=CYLINDRICAL_SURFACE ( 'NONE', #40082, 1.399999999999998579 ) ;
#43969=CARTESIAN_POINT ( 'NONE',  ( 11.08848345035334404, -9.804883450353528929, 455.0000000000000568 ) ) ;
#43975=CARTESIAN_POINT ( 'NONE',  ( -1.677516549646778099, -10.74648345035342167, 195.0000000000000284 ) ) ;
#43980=CARTESIAN_POINT ( 'NONE',  ( -4.173516549646669738, 11.77351654964658678, 455.0000000000000568 ) ) ;
#43982=ORIENTED_EDGE ( 'NONE', *, *, #51300, .F. ) ;
#43986=CARTESIAN_POINT ( 'NONE',  ( 5.668387132715918320, -8.406483450353487541, 455.0000000000000568 ) ) ;
#43988=AXIS2_PLACEMENT_3D ( 'NONE', #953, #50051, #1609 ) ;
#43990=DIRECTION ( 'NONE',  ( -0.7071067811865398012, 0.7071067811865552333, 2.597868168706484541E-16 ) ) ;
#43991=ORIENTED_EDGE ( 'NONE', *, *, #20304, .T. ) ;
#44003=EDGE_LOOP ( 'NONE', ( #50850, #65507, #47788, #39198 ) ) ;
#44007=CARTESIAN_POINT ( 'NONE',  ( -11.77351654964674310, -7.606483450353318965, 195.0000000000000284 ) ) ;
#44009=ADVANCED_FACE ( 'NONE', ( #15541 ), #49084, .F. ) ;
#44023=CARTESIAN_POINT ( 'NONE',  ( 5.668387132715920096, 8.393516549646628633, 195.0000000000000284 ) ) ;
#44026=ADVANCED_FACE ( 'NONE', ( #32133 ), #53706, .F. ) ;
#44033=VECTOR ( 'NONE', #60325, 1000.000000000000000 ) ;
#44034=DIRECTION ( 'NONE',  ( -0.7671651518152962090, -0.6414496315691619044, 0.000000000000000000 ) ) ;
#44036=ORIENTED_EDGE ( 'NONE', *, *, #23559, .T. ) ;
#44041=CARTESIAN_POINT ( 'NONE',  ( 11.32648345035335780, 7.793516549646610336, 195.0000000000000284 ) ) ;
#44048=DIRECTION ( 'NONE',  ( 1.819560449471430698E-15, 1.000000000000000000, 1.836970198721032892E-16 ) ) ;
#44049=CARTESIAN_POINT ( 'NONE',  ( -11.77351654964670935, 7.593516549646604830, 195.0000000000000284 ) ) ;
#44060=CIRCLE ( 'NONE', #64375, 1.399999999999999245 ) ;
#44067=ORIENTED_EDGE ( 'NONE', *, *, #40536, .T. ) ;
#44068=DIRECTION ( 'NONE',  ( 1.836970198721029934E-16, -1.836970198721036344E-16, 1.000000000000000000 ) ) ;
#44083=EDGE_CURVE ( 'NONE', #7898, #23630, #2376, .T. ) ;
#44088=CARTESIAN_POINT ( 'NONE',  ( 8.465062094116069247, -7.757955312929635028, 455.0000000000000568 ) ) ;
#44096=AXIS2_PLACEMENT_3D ( 'NONE', #36481, #58051, #9622 ) ;
#44097=VECTOR ( 'NONE', #29878, 1000.000000000000000 ) ;
#44101=EDGE_LOOP ( 'NONE', ( #352, #35193, #22552, #2113 ) ) ;
#44104=DIRECTION ( 'NONE',  ( 0.000000000000000000, 1.000000000000000000, 0.000000000000000000 ) ) ;
#44122=ORIENTED_EDGE ( 'NONE', *, *, #19176, .F. ) ;
#44124=DIRECTION ( 'NONE',  ( 0.000000000000000000, 3.673940397442059868E-16, -1.000000000000000000 ) ) ;
#44130=DIRECTION ( 'NONE',  ( -0.000000000000000000, -0.000000000000000000, -1.000000000000000000 ) ) ;
#44136=ORIENTED_EDGE ( 'NONE', *, *, #37793, .T. ) ;
#44143=VECTOR ( 'NONE', #34839, 1000.000000000000000 ) ;
#44144=DIRECTION ( 'NONE',  ( 1.000000000000000000, 0.000000000000000000, 0.000000000000000000 ) ) ;
#44150=DIRECTION ( 'NONE',  ( 1.000000000000000000, -3.491481338843133355E-15, -1.836970198721036344E-16 ) ) ;
#44153=VERTEX_POINT ( 'NONE', #33515 ) ;
#44155=DIRECTION ( 'NONE',  ( -0.6414496315691445849, -0.7671651518153106419, -2.818519042764040096E-16 ) ) ;
#44157=ORIENTED_EDGE ( 'NONE', *, *, #55234, .F. ) ;
#44161=CARTESIAN_POINT ( 'NONE',  ( -7.813516549646836395, -11.78648345035340661, 455.0000000000000568 ) ) ;
#44162=EDGE_LOOP ( 'NONE', ( #47571, #16801, #44337, #15674, #59109, #9314, #51266, #11493, #31762, #40070, #26424, #3425, #51387, #50174, #51979, #56668, #6102 ) ) ;
#44165=EDGE_LOOP ( 'NONE', ( #3567, #62711, #60344, #25828 ) ) ;
#44170=ORIENTED_EDGE ( 'NONE', *, *, #14313, .F. ) ;
#44178=ORIENTED_EDGE ( 'NONE', *, *, #49299, .T. ) ;
#44186=CARTESIAN_POINT ( 'NONE',  ( 4.740315990920131561, -7.811466277050838514, 455.0000000000000568 ) ) ;
#44209=ORIENTED_EDGE ( 'NONE', *, *, #44947, .F. ) ;
#44212=CARTESIAN_POINT ( 'NONE',  ( 1.090483450353338268, -11.34648345035345329, 455.0000000000000568 ) ) ;
#44219=ORIENTED_EDGE ( 'NONE', *, *, #41483, .F. ) ;
#44221=CARTESIAN_POINT ( 'NONE',  ( -9.293516549646779978, -10.92648345035333790, 195.0000000000000284 ) ) ;
#44225=ORIENTED_EDGE ( 'NONE', *, *, #23355, .T. ) ;
#44229=VECTOR ( 'NONE', #16989, 1000.000000000000000 ) ;
#44233=PRODUCT ( 'Aluminum Extrusions (T-Slot Profiles)_5537T808', 'Aluminum Extrusions (T-Slot Profiles)_5537T808', '', ( #54027 ) ) ;
#44234=AXIS2_PLACEMENT_3D ( 'NONE', #34258, #13402, #49845 ) ;
#44235=CARTESIAN_POINT ( 'NONE',  ( -9.942044687070668019, -9.247904806590694804, 455.0000000000000568 ) ) ;
#44236=DIRECTION ( 'NONE',  ( -1.000000000000000000, 1.185108578570163402E-14, 1.836970198721051628E-16 ) ) ;
#44237=EDGE_CURVE ( 'NONE', #28648, #33046, #35953, .T. ) ;
#44239=DIRECTION ( 'NONE',  ( -0.7071067811865474617, 0.7071067811865474617, 2.597868168706479611E-16 ) ) ;
#44244=ORIENTED_EDGE ( 'NONE', *, *, #64407, .T. ) ;
#44249=LINE ( 'NONE', #64797, #29920 ) ;
#44253=CARTESIAN_POINT ( 'NONE',  ( -3.417780618358722933, -7.852485183457003970, 455.0000000000000568 ) ) ;
#44256=AXIS2_PLACEMENT_3D ( 'NONE', #13065, #55523, #7065 ) ;
#44257=CARTESIAN_POINT ( 'NONE',  ( -11.11351654964671098, 4.193516549646605363, 195.0000000000000284 ) ) ;
#44259=VERTEX_POINT ( 'NONE', #51871 ) ;
#44262=CARTESIAN_POINT ( 'NONE',  ( -4.193516549646675529, 11.11351654964658842, 455.0000000000000568 ) ) ;
#44264=CARTESIAN_POINT ( 'NONE',  ( 11.78648345035337819, -4.186483450353492231, 455.0000000000000568 ) ) ;
#44272=CARTESIAN_POINT ( 'NONE',  ( 6.006483450353401921, 5.993516549646582092, 455.0000000000000568 ) ) ;
#44276=ADVANCED_FACE ( 'NONE', ( #46549 ), #36300, .F. ) ;
#44283=DIRECTION ( 'NONE',  ( -0.000000000000000000, 3.673940397442059868E-16, -1.000000000000000000 ) ) ;
#44289=VERTEX_POINT ( 'NONE', #57863 ) ;
#44305=CARTESIAN_POINT ( 'NONE',  ( -4.188533722949421723, -7.272650909786664286, 455.0000000000000568 ) ) ;
#44311=ADVANCED_FACE ( 'NONE', ( #29941 ), #59620, .F. ) ;
#44318=CARTESIAN_POINT ( 'NONE',  ( 4.622483450353380263, -3.606483450353491271, 455.0000000000000568 ) ) ;
#44324=VERTEX_POINT ( 'NONE', #32735 ) ;
#44326=EDGE_CURVE ( 'NONE', #16506, #46286, #26746, .T. ) ;
#44328=CARTESIAN_POINT ( 'NONE',  ( -4.734785091273957747, 5.380658396643156038, 455.0000000000000568 ) ) ;
#44337=ORIENTED_EDGE ( 'NONE', *, *, #10013, .F. ) ;
#44343=CIRCLE ( 'NONE', #47792, 0.1999999999999987899 ) ;
#44347=VECTOR ( 'NONE', #46204, 1000.000000000000000 ) ;
#44350=DIRECTION ( 'NONE',  ( 5.013651664672856055E-16, -1.000000000000000000, -3.673940397442059868E-16 ) ) ;
#44351=DIRECTION ( 'NONE',  ( -9.050731179009442381E-15, -1.000000000000000000, 0.000000000000000000 ) ) ;
#44370=DIRECTION ( 'NONE',  ( -1.000000000000000000, 9.973078850062113474E-15, -1.836970198721011692E-16 ) ) ;
#44373=LINE ( 'NONE', #28464, #1455 ) ;
#44377=ORIENTED_EDGE ( 'NONE', *, *, #11805, .T. ) ;
#44378=CARTESIAN_POINT ( 'NONE',  ( 7.616533956692213003, -8.406483450353396947, 195.0000000000000284 ) ) ;
#44389=VERTEX_POINT ( 'NONE', #59953 ) ;
#44393=AXIS2_PLACEMENT_3D ( 'NONE', #38281, #59835, #33652 ) ;
#44402=PLANE ( 'NONE',  #16199 ) ;
#44408=EDGE_LOOP ( 'NONE', ( #33963, #38695, #14616, #42062 ) ) ;
#44414=ORIENTED_EDGE ( 'NONE', *, *, #52326, .T. ) ;
#44416=CARTESIAN_POINT ( 'NONE',  ( -7.259684009079930611, 4.188533722949235205, 455.0000000000000568 ) ) ;
#44418=ORIENTED_EDGE ( 'NONE', *, *, #13575, .T. ) ;
#44422=VERTEX_POINT ( 'NONE', #66991 ) ;
#44423=AXIS2_PLACEMENT_3D ( 'NONE', #62034, #13254, #2642 ) ;
#44443=ADVANCED_FACE ( 'NONE', ( #34108 ), #6217, .T. ) ;
#44450=EDGE_LOOP ( 'NONE', ( #27241, #40069, #51390, #22533 ) ) ;
#44458=ADVANCED_FACE ( 'NONE', ( #23512 ), #12197, .T. ) ;
#44459=LINE ( 'NONE', #65021, #47670 ) ;
#44460=VERTEX_POINT ( 'NONE', #45069 ) ;
#44469=LINE ( 'NONE', #50819, #10691 ) ;
#44481=ORIENTED_EDGE ( 'NONE', *, *, #12073, .F. ) ;
#44483=CARTESIAN_POINT ( 'NONE',  ( 12.00648345035340903, 7.813516549646560172, 455.0000000000000568 ) ) ;
#44487=EDGE_CURVE ( 'NONE', #59410, #4281, #29512, .T. ) ;
#44488=CARTESIAN_POINT ( 'NONE',  ( 8.606483450353380249, -4.396432944014562416, 195.0000000000000284 ) ) ;
#44489=LINE ( 'NONE', #1714, #39207 ) ;
#44493=EDGE_LOOP ( 'NONE', ( #1469, #51599, #22530, #67888 ) ) ;
#44500=CARTESIAN_POINT ( 'NONE',  ( 9.841277389592722358, -1.690483450353490680, 455.0000000000000568 ) ) ;
#44509=CIRCLE ( 'NONE', #47968, 2.204799999999997429 ) ;
#44511=FACE_OUTER_BOUND ( 'NONE', #5736, .T. ) ;
#44519=PLANE ( 'NONE',  #43034 ) ;
#44522=VERTEX_POINT ( 'NONE', #14653 ) ;
#44526=CARTESIAN_POINT ( 'NONE',  ( -10.08346604330787777, 2.693516549646604918, 455.0000000000000568 ) ) ;
#44534=DIRECTION ( 'NONE',  ( 0.000000000000000000, 0.000000000000000000, 1.000000000000000000 ) ) ;
#44536=CARTESIAN_POINT ( 'NONE',  ( 4.206483450353343478, -11.12648345035338160, 195.0000000000000284 ) ) ;
#44544=DIRECTION ( 'NONE',  ( -8.339399738404102667E-15, -1.000000000000000000, -1.836970198721025990E-16 ) ) ;
#44553=CIRCLE ( 'NONE', #47957, 2.204799999999999205 ) ;
#44560=ORIENTED_EDGE ( 'NONE', *, *, #10666, .T. ) ;
#44561=ORIENTED_EDGE ( 'NONE', *, *, #12390, .T. ) ;
#44564=CARTESIAN_POINT ( 'NONE',  ( -7.793516549646827940, -11.12648345035340647, 455.0000000000000568 ) ) ;
#44574=DIRECTION ( 'NONE',  ( -0.000000000000000000, -0.000000000000000000, -1.000000000000000000 ) ) ;
#44586=DIRECTION ( 'NONE',  ( 2.135044278125299371E-15, -1.000000000000000000, -3.673940397442060361E-16 ) ) ;
#44594=AXIS2_PLACEMENT_3D ( 'NONE', #60400, #333, #11275 ) ;
#44602=EDGE_CURVE ( 'NONE', #34574, #44814, #40823, .T. ) ;
#44606=VECTOR ( 'NONE', #9780, 1000.000000000000000 ) ;
#44611=ADVANCED_FACE ( 'NONE', ( #14314 ), #24912, .F. ) ;
#44622=CARTESIAN_POINT ( 'NONE',  ( 6.006483450353379716, -6.006483450353490738, 455.0000000000000568 ) ) ;
#44626=CARTESIAN_POINT ( 'NONE',  ( 4.206483450353422526, 11.31351654964658415, 455.0000000000000568 ) ) ;
#44644=AXIS2_PLACEMENT_3D ( 'NONE', #31740, #63202, #10159 ) ;
#44647=CARTESIAN_POINT ( 'NONE',  ( 8.465062094116069247, -4.255011587777349114, 455.0000000000000568 ) ) ;
#44648=VECTOR ( 'NONE', #52314, 1000.000000000000000 ) ;
#44650=VERTEX_POINT ( 'NONE', #53207 ) ;
#44653=AXIS2_PLACEMENT_3D ( 'NONE', #5967, #49097, #48757 ) ;
#44656=LINE ( 'NONE', #55982, #32348 ) ;
#44660=STYLED_ITEM ( 'NONE', ( #20909 ), #43625 ) ;
#44663=CARTESIAN_POINT ( 'NONE',  ( -7.252248008019492431, -6.619341603356823533, 455.0000000000000568 ) ) ;
#44666=EDGE_CURVE ( 'NONE', #10486, #37791, #15710, .T. ) ;
#44667=EDGE_LOOP ( 'NONE', ( #62967, #41548, #21502, #18137 ) ) ;
#44669=DIRECTION ( 'NONE',  ( 1.836970198721029934E-16, -1.836970198721036344E-16, 1.000000000000000000 ) ) ;
#44680=VERTEX_POINT ( 'NONE', #63448 ) ;
#44696=DIRECTION ( 'NONE',  ( 0.000000000000000000, 0.000000000000000000, -1.000000000000000000 ) ) ;
#44697=DIRECTION ( 'NONE',  ( -0.000000000000000000, -0.000000000000000000, -1.000000000000000000 ) ) ;
#44705=CARTESIAN_POINT ( 'NONE',  ( 9.306483450353379538, -10.92648345035348534, 455.0000000000000568 ) ) ;
#44712=LINE ( 'NONE', #13242, #25770 ) ;
#44715=LINE ( 'NONE', #16128, #57630 ) ;
#44724=CARTESIAN_POINT ( 'NONE',  ( -2.693516549646675529, 10.91351654964657314, 455.0000000000000568 ) ) ;
#44730=LINE ( 'NONE', #55702, #61587 ) ;
#44764=CARTESIAN_POINT ( 'NONE',  ( -4.188533722949335569, 7.259684009079808931, 455.0000000000000568 ) ) ;
#44771=ORIENTED_EDGE ( 'NONE', *, *, #8638, .T. ) ;
#44778=EDGE_CURVE ( 'NONE', #57965, #25895, #55955, .T. ) ;
#44791=VECTOR ( 'NONE', #29358, 1000.000000000000000 ) ;
#44802=DIRECTION ( 'NONE',  ( -5.013651664672856055E-16, 1.000000000000000000, 0.000000000000000000 ) ) ;
#44807=AXIS2_PLACEMENT_3D ( 'NONE', #52384, #20200, #58743 ) ;
#44814=VERTEX_POINT ( 'NONE', #33354 ) ;
#44826=VERTEX_POINT ( 'NONE', #55610 ) ;
#44831=VECTOR ( 'NONE', #69610, 1000.000000000000000 ) ;
#44833=VERTEX_POINT ( 'NONE', #47358 ) ;
#44836=VERTEX_POINT ( 'NONE', #35072 ) ;
#44838=ORIENTED_EDGE ( 'NONE', *, *, #67231, .T. ) ;
#44841=DIRECTION ( 'NONE',  ( -1.836970198721029934E-16, 1.836970198721036344E-16, -1.000000000000000000 ) ) ;
#44880=FACE_OUTER_BOUND ( 'NONE', #3526, .T. ) ;
#44884=DIRECTION ( 'NONE',  ( -1.836970198721029934E-16, 1.836970198721036344E-16, -1.000000000000000000 ) ) ;
#44894=EDGE_CURVE ( 'NONE', #51193, #47490, #24129, .T. ) ;
#44895=ORIENTED_EDGE ( 'NONE', *, *, #19729, .F. ) ;
#44898=PLANE ( 'NONE',  #10813 ) ;
#44911=CARTESIAN_POINT ( 'NONE',  ( 6.006483450353379716, -6.006483450353490738, 455.0000000000000568 ) ) ;
#44916=CARTESIAN_POINT ( 'NONE',  ( -11.11351654964679270, -7.806483450353373321, 455.0000000000000568 ) ) ;
#44926=LINE ( 'NONE', #39612, #64873 ) ;
#44934=CARTESIAN_POINT ( 'NONE',  ( 1.690483450353344352, -10.74648345035345720, 455.0000000000000568 ) ) ;
#44937=EDGE_CURVE ( 'NONE', #40641, #6826, #69976, .T. ) ;
#44945=ORIENTED_EDGE ( 'NONE', *, *, #27244, .F. ) ;
#44947=EDGE_CURVE ( 'NONE', #55886, #63655, #60047, .T. ) ;
#44950=CYLINDRICAL_SURFACE ( 'NONE', #42201, 0.6000000000000003109 ) ;
#44953=VERTEX_POINT ( 'NONE', #27531 ) ;
#44959=EDGE_CURVE ( 'NONE', #6331, #34313, #50322, .T. ) ;
#44962=LINE ( 'NONE', #39647, #18081 ) ;
#44963=VERTEX_POINT ( 'NONE', #42753 ) ;
#44967=ORIENTED_EDGE ( 'NONE', *, *, #67466, .F. ) ;
#44974=FACE_OUTER_BOUND ( 'NONE', #40388, .T. ) ;
#44980=EDGE_CURVE ( 'NONE', #67623, #16263, #318, .T. ) ;
#44988=ORIENTED_EDGE ( 'NONE', *, *, #11194, .T. ) ;
#44991=VECTOR ( 'NONE', #4167, 1000.000000000000000 ) ;
#44993=ORIENTED_EDGE ( 'NONE', *, *, #60013, .F. ) ;
#45004=ORIENTED_EDGE ( 'NONE', *, *, #56442, .F. ) ;
#45011=CARTESIAN_POINT ( 'NONE',  ( -7.415254214038336400, 3.593516549646602609, 195.0000000000000284 ) ) ;
#45014=CARTESIAN_POINT ( 'NONE',  ( -5.993516549646711766, 5.993516549646603409, 455.0000000000000568 ) ) ;
#45018=ORIENTED_EDGE ( 'NONE', *, *, #38398, .F. ) ;
#45040=AXIS2_PLACEMENT_3D ( 'NONE', #61526, #2491, #62580 ) ;
#45048=LINE ( 'NONE', #56715, #15939 ) ;
#45053=DIRECTION ( 'NONE',  ( -0.000000000000000000, 3.673940397442059868E-16, -1.000000000000000000 ) ) ;
#45062=EDGE_CURVE ( 'NONE', #58819, #65043, #4059, .T. ) ;
#45069=CARTESIAN_POINT ( 'NONE',  ( 11.32648345035340398, 7.593516549646563085, 455.0000000000000568 ) ) ;
#45071=ORIENTED_EDGE ( 'NONE', *, *, #42170, .F. ) ;
#45080=CARTESIAN_POINT ( 'NONE',  ( 8.406483450353379183, -4.396432944014657451, 455.0000000000000568 ) ) ;
#45091=DIRECTION ( 'NONE',  ( 0.000000000000000000, -3.673940397442059868E-16, 1.000000000000000000 ) ) ;
#45095=DIRECTION ( 'NONE',  ( -8.673617379884013384E-15, -1.000000000000000000, 0.000000000000000000 ) ) ;
#45102=ADVANCED_FACE ( 'NONE', ( #7328 ), #12280, .F. ) ;
#45106=CARTESIAN_POINT ( 'NONE',  ( -8.593516549646711411, 4.383466043307770121, 455.0000000000000568 ) ) ;
#45111=LINE ( 'NONE', #18240, #51583 ) ;
#45119=DIRECTION ( 'NONE',  ( 0.000000000000000000, 0.000000000000000000, 1.000000000000000000 ) ) ;
#45128=VECTOR ( 'NONE', #20770, 1000.000000000000114 ) ;
#45131=LINE ( 'NONE', #1326, #21147 ) ;
#45134=ORIENTED_EDGE ( 'NONE', *, *, #65408, .F. ) ;
#45135=EDGE_CURVE ( 'NONE', #64234, #5555, #40218, .T. ) ;
#45158=ORIENTED_EDGE ( 'NONE', *, *, #48517, .T. ) ;
#45164=ORIENTED_EDGE ( 'NONE', *, *, #11965, .T. ) ;
#45167=VECTOR ( 'NONE', #9671, 1000.000000000000114 ) ;
#45168=DIRECTION ( 'NONE',  ( -0.7071067811865464625, 0.7071067811865486830, 0.000000000000000000 ) ) ;
#45170=DIRECTION ( 'NONE',  ( 4.745709458399858621E-16, 1.000000000000000000, 1.836970198721035604E-16 ) ) ;
#45172=CARTESIAN_POINT ( 'NONE',  ( 7.806483450353418618, 11.11351654964657421, 455.0000000000000568 ) ) ;
#45173=ORIENTED_EDGE ( 'NONE', *, *, #53616, .F. ) ;
#45179=EDGE_CURVE ( 'NONE', #62585, #58374, #49787, .T. ) ;
#45180=CARTESIAN_POINT ( 'NONE',  ( -10.19191654964680360, -9.804883450353337082, 195.0000000000000284 ) ) ;
#45186=ORIENTED_EDGE ( 'NONE', *, *, #18686, .F. ) ;
#45190=CARTESIAN_POINT ( 'NONE',  ( 4.186483450353335023, -12.00648345035347830, 455.0000000000000568 ) ) ;
#45191=EDGE_LOOP ( 'NONE', ( #62403, #65037, #26633, #65440 ) ) ;
#45193=EDGE_CURVE ( 'NONE', #42184, #56927, #21064, .T. ) ;
#45196=VECTOR ( 'NONE', #66735, 999.9999999999998863 ) ;
#45204=FACE_OUTER_BOUND ( 'NONE', #46167, .T. ) ;
#45205=PLANE ( 'NONE',  #37337 ) ;
#45216=ORIENTED_EDGE ( 'NONE', *, *, #35709, .F. ) ;
#45218=VECTOR ( 'NONE', #19728, 1000.000000000000000 ) ;
#45220=FACE_OUTER_BOUND ( 'NONE', #20809, .T. ) ;
#45232=CIRCLE ( 'NONE', #41871, 1.399999999999999245 ) ;
#45238=CARTESIAN_POINT ( 'NONE',  ( 8.465062094116099445, 7.744988412222715723, 455.0000000000000568 ) ) ;
#45245=AXIS2_PLACEMENT_3D ( 'NONE', #35892, #25278, #63464 ) ;
#45255=PLANE ( 'NONE',  #12282 ) ;
#45260=AXIS2_PLACEMENT_3D ( 'NONE', #15868, #46992, #37437 ) ;
#45264=DIRECTION ( 'NONE',  ( 0.5000000000000111022, 0.8660254037844322683, 2.509347957447867944E-16 ) ) ;
#45275=DIRECTION ( 'NONE',  ( 1.836970198721029934E-16, 1.836970198721010706E-16, -1.000000000000000000 ) ) ;
#45283=CIRCLE ( 'NONE', #34027, 2.204799999999999205 ) ;
#45288=ORIENTED_EDGE ( 'NONE', *, *, #24599, .F. ) ;
#45295=AXIS2_PLACEMENT_3D ( 'NONE', #33467, #55052, #1290 ) ;
#45299=ORIENTED_EDGE ( 'NONE', *, *, #68876, .F. ) ;
#45301=LINE ( 'NONE', #66871, #67820 ) ;
#45309=LINE ( 'NONE', #50631, #31281 ) ;
#45323=ADVANCED_FACE ( 'NONE', ( #51533 ), #14407, .F. ) ;
#45327=ORIENTED_EDGE ( 'NONE', *, *, #69540, .T. ) ;
#45329=LINE ( 'NONE', #35422, #7631 ) ;
#45330=EDGE_CURVE ( 'NONE', #48598, #11140, #58325, .T. ) ;
#45345=EDGE_CURVE ( 'NONE', #51749, #32671, #1568, .T. ) ;
#45353=VERTEX_POINT ( 'NONE', #67672 ) ;
#45354=ADVANCED_FACE ( 'NONE', ( #51405 ), #23837, .T. ) ;
#45358=DIRECTION ( 'NONE',  ( -1.836970198721029934E-16, -1.836970198721010706E-16, 1.000000000000000000 ) ) ;
#45369=DIRECTION ( 'NONE',  ( -1.836970198721029934E-16, 1.836970198721036344E-16, -1.000000000000000000 ) ) ;
#45370=DIRECTION ( 'NONE',  ( 0.000000000000000000, 1.000000000000000000, 0.000000000000000000 ) ) ;
#45376=EDGE_LOOP ( 'NONE', ( #13465, #38886, #38007, #26587 ) ) ;
#45381=VECTOR ( 'NONE', #46554, 1000.000000000000000 ) ;
#45399=DIRECTION ( 'NONE',  ( 0.000000000000000000, -1.000000000000000000, 0.000000000000000000 ) ) ;
#45400=EDGE_LOOP ( 'NONE', ( #9641, #51454, #63338, #65628 ) ) ;
#45405=AXIS2_PLACEMENT_3D ( 'NONE', #25018, #3450, #51179 ) ;
#45408=PLANE ( 'NONE',  #42646 ) ;
#45409=EDGE_CURVE ( 'NONE', #67467, #57392, #66962, .T. ) ;
#45410=VECTOR ( 'NONE', #23589, 1000.000000000000000 ) ;
#45411=DIRECTION ( 'NONE',  ( -0.000000000000000000, 3.673940397442059868E-16, -1.000000000000000000 ) ) ;
#45428=CARTESIAN_POINT ( 'NONE',  ( -7.415254214038356828, -3.606483450353401121, 455.0000000000000568 ) ) ;
#45429=CARTESIAN_POINT ( 'NONE',  ( 1.090483450353418426, 10.73351654964659829, 455.0000000000000568 ) ) ;
#45430=AXIS2_PLACEMENT_3D ( 'NONE', #11859, #65949, #17520 ) ;
#45449=CARTESIAN_POINT ( 'NONE',  ( 11.08848345035337246, 11.07551654964657573, 195.0000000000000284 ) ) ;
#45455=ORIENTED_EDGE ( 'NONE', *, *, #25349, .F. ) ;
#45461=AXIS2_PLACEMENT_3D ( 'NONE', #19872, #41791, #63368 ) ;
#45465=AXIS2_PLACEMENT_3D ( 'NONE', #35672, #30382, #51954 ) ;
#45470=DIRECTION ( 'NONE',  ( 8.673617379884087537E-15, 1.000000000000000000, 0.000000000000000000 ) ) ;
#45474=DIRECTION ( 'NONE',  ( 1.836970198721029934E-16, 1.836970198721010706E-16, -1.000000000000000000 ) ) ;
#45480=CYLINDRICAL_SURFACE ( 'NONE', #42588, 0.1999999999999987899 ) ;
#45483=ORIENTED_EDGE ( 'NONE', *, *, #50170, .F. ) ;
#45488=FACE_OUTER_BOUND ( 'NONE', #21634, .T. ) ;
#45490=ADVANCED_FACE ( 'NONE', ( #57763 ), #42551, .T. ) ;
#45494=CARTESIAN_POINT ( 'NONE',  ( -8.393516549646745872, -4.396432944014549093, 455.0000000000000568 ) ) ;
#45495=EDGE_CURVE ( 'NONE', #43873, #25493, #10863, .T. ) ;
#45499=AXIS2_PLACEMENT_3D ( 'NONE', #433, #64440, #20944 ) ;
#45500=ADVANCED_FACE ( 'NONE', ( #4033 ), #52112, .T. ) ;
#45502=DIRECTION ( 'NONE',  ( 8.673617379884013384E-15, 1.000000000000000000, 0.000000000000000000 ) ) ;
#45506=EDGE_LOOP ( 'NONE', ( #67743, #40346, #36726, #67544 ) ) ;
#45507=LINE ( 'NONE', #39845, #15149 ) ;
#45510=CARTESIAN_POINT ( 'NONE',  ( -11.99351654964671354, 4.173516549646604901, 195.0000000000000284 ) ) ;
#45517=CARTESIAN_POINT ( 'NONE',  ( 7.811466277050743479, 4.727349090213326832, 455.0000000000000568 ) ) ;
#45520=ORIENTED_EDGE ( 'NONE', *, *, #58023, .F. ) ;
#45524=LINE ( 'NONE', #67101, #7294 ) ;
#45525=DIRECTION ( 'NONE',  ( 0.000000000000000000, 1.000000000000000000, 0.000000000000000000 ) ) ;
#45531=ORIENTED_EDGE ( 'NONE', *, *, #58215, .T. ) ;
#45542=ORIENTED_EDGE ( 'NONE', *, *, #17669, .T. ) ;
#45543=CARTESIAN_POINT ( 'NONE',  ( 4.201500623656053257, 4.727349090213338378, 455.0000000000000568 ) ) ;
#45545=ORIENTED_EDGE ( 'NONE', *, *, #67231, .F. ) ;
#45546=EDGE_CURVE ( 'NONE', #26698, #52016, #30895, .T. ) ;
#45548=CARTESIAN_POINT ( 'NONE',  ( 1.866219381641426533, -9.417013320880872840, 455.0000000000000568 ) ) ;
#45555=VERTEX_POINT ( 'NONE', #58116 ) ;
#45561=CARTESIAN_POINT ( 'NONE',  ( 9.247904806590677040, 9.942044687070474396, 195.0000000000000284 ) ) ;
#45562=CARTESIAN_POINT ( 'NONE',  ( -5.993516549646776603, -6.006483450353426790, 455.0000000000000568 ) ) ;
#45564=AXIS2_PLACEMENT_3D ( 'NONE', #33318, #64465, #10706 ) ;
#45568=LINE ( 'NONE', #41320, #49511 ) ;
#45570=EDGE_LOOP ( 'NONE', ( #35493, #57397, #42080, #43814 ) ) ;
#45576=DIRECTION ( 'NONE',  ( 1.261617073437657735E-14, 1.000000000000000000, 3.673940397442059868E-16 ) ) ;
#45583=FACE_OUTER_BOUND ( 'NONE', #24402, .T. ) ;
#45587=EDGE_CURVE ( 'NONE', #9547, #5555, #14627, .T. ) ;
#45589=LINE ( 'NONE', #3876, #58963 ) ;
#45590=ORIENTED_EDGE ( 'NONE', *, *, #53594, .T. ) ;
#45594=ORIENTED_EDGE ( 'NONE', *, *, #27093, .F. ) ;
#45600=DIRECTION ( 'NONE',  ( 0.000000000000000000, 1.000000000000000000, 0.000000000000000000 ) ) ;
#45610=AXIS2_PLACEMENT_3D ( 'NONE', #44934, #19111, #40679 ) ;
#45631=EDGE_CURVE ( 'NONE', #37791, #56148, #51323, .T. ) ;
#45635=VERTEX_POINT ( 'NONE', #2191 ) ;
#45642=VERTEX_POINT ( 'NONE', #13139 ) ;
#45643=CARTESIAN_POINT ( 'NONE',  ( 11.08848345035334404, -9.804883450353433005, 195.0000000000000284 ) ) ;
#45653=ORIENTED_EDGE ( 'NONE', *, *, #18420, .F. ) ;
#45654=DIRECTION ( 'NONE',  ( -7.457533623526253657E-15, -1.000000000000000000, -1.836970198721024757E-16 ) ) ;
#45656=VECTOR ( 'NONE', #33211, 1000.000000000000000 ) ;
#45671=DIRECTION ( 'NONE',  ( 0.000000000000000000, 0.000000000000000000, 1.000000000000000000 ) ) ;
#45676=CARTESIAN_POINT ( 'NONE',  ( -7.744988412222944874, -8.465062094116097668, 455.0000000000000568 ) ) ;
#45691=DIRECTION ( 'NONE',  ( 3.491481338843132961E-15, 1.000000000000000000, 0.000000000000000000 ) ) ;
#45693=EDGE_LOOP ( 'NONE', ( #16150, #36133, #27687, #15005 ) ) ;
#45699=ORIENTED_EDGE ( 'NONE', *, *, #50368, .T. ) ;
#45704=DIRECTION ( 'NONE',  ( 1.836970198721029934E-16, 1.836970198721010706E-16, -1.000000000000000000 ) ) ;
#45709=LINE ( 'NONE', #30160, #55916 ) ;
#45713=VERTEX_POINT ( 'NONE', #2531 ) ;
#45718=CARTESIAN_POINT ( 'NONE',  ( 4.747751991980655895, 6.606374702650043673, 455.0000000000000568 ) ) ;
#45719=EDGE_CURVE ( 'NONE', #65838, #15525, #45309, .T. ) ;
#45728=ORIENTED_EDGE ( 'NONE', *, *, #69463, .T. ) ;
#45729=EDGE_LOOP ( 'NONE', ( #27246, #20575, #19120, #57741 ) ) ;
#45731=ORIENTED_EDGE ( 'NONE', *, *, #9151, .T. ) ;
#45739=FACE_OUTER_BOUND ( 'NONE', #65442, .T. ) ;
#45751=DIRECTION ( 'NONE',  ( -1.000000000000000000, 0.000000000000000000, 0.000000000000000000 ) ) ;
#45753=VECTOR ( 'NONE', #56141, 1000.000000000000000 ) ;
#45755=CARTESIAN_POINT ( 'NONE',  ( 1.090483450353343819, -10.74648345035345365, 455.0000000000000568 ) ) ;
#45757=AXIS2_PLACEMENT_3D ( 'NONE', #5505, #60265, #53946 ) ;
#45768=CARTESIAN_POINT ( 'NONE',  ( 8.465062094116069247, -7.757955312929635028, 455.0000000000000568 ) ) ;
#45770=ORIENTED_EDGE ( 'NONE', *, *, #63227, .F. ) ;
#45771=VECTOR ( 'NONE', #25771, 1000.000000000000000 ) ;
#45772=CARTESIAN_POINT ( 'NONE',  ( -2.752095193409461071, -9.955011587777271131, 195.0000000000000284 ) ) ;
#45775=ADVANCED_FACE ( 'NONE', ( #53440 ), #26561, .F. ) ;
#45782=DIRECTION ( 'NONE',  ( 1.000000000000000000, 5.013651664672856055E-16, 0.000000000000000000 ) ) ;
#45792=FACE_OUTER_BOUND ( 'NONE', #33445, .T. ) ;
#45807=EDGE_CURVE ( 'NONE', #4376, #38741, #42816, .T. ) ;
#45814=ORIENTED_EDGE ( 'NONE', *, *, #62202, .T. ) ;
#45818=VECTOR ( 'NONE', #44697, 1000.000000000000000 ) ;
#45823=ORIENTED_EDGE ( 'NONE', *, *, #59107, .T. ) ;
#45826=ADVANCED_FACE ( 'NONE', ( #68992 ), #63700, .T. ) ;
#45830=AXIS2_PLACEMENT_3D ( 'NONE', #60736, #50816, #51171 ) ;
#45835=ADVANCED_FACE ( 'NONE', ( #69340 ), #26917, .F. ) ;
#45837=CARTESIAN_POINT ( 'NONE',  ( 8.606483450353382025, 4.383466043307719495, 455.0000000000000568 ) ) ;
#45840=DIRECTION ( 'NONE',  ( 1.836970198721029934E-16, 1.836970198721010706E-16, -1.000000000000000000 ) ) ;
#45854=CARTESIAN_POINT ( 'NONE',  ( 9.417013320880792904, -1.866219381641561759, 455.0000000000000568 ) ) ;
#45857=AXIS2_PLACEMENT_3D ( 'NONE', #34642, #9437, #31005 ) ;
#45861=LINE ( 'NONE', #24653, #44347 ) ;
#45864=CIRCLE ( 'NONE', #34545, 0.2000000000000005107 ) ;
#45871=DIRECTION ( 'NONE',  ( -1.836970198721029934E-16, 1.836970198721036344E-16, -1.000000000000000000 ) ) ;
#45877=AXIS2_PLACEMENT_3D ( 'NONE', #3097, #24659, #35963 ) ;
#45878=ORIENTED_EDGE ( 'NONE', *, *, #32561, .T. ) ;
#45883=ORIENTED_EDGE ( 'NONE', *, *, #52519, .F. ) ;
#45884=CYLINDRICAL_SURFACE ( 'NONE', #58251, 1.399999999999999245 ) ;
#45903=AXIS2_PLACEMENT_3D ( 'NONE', #3641, #2934, #67641 ) ;
#45908=CIRCLE ( 'NONE', #21084, 0.1999999999999996503 ) ;
#45912=ORIENTED_EDGE ( 'NONE', *, *, #42170, .T. ) ;
#45915=DIRECTION ( 'NONE',  ( -1.000000000000000000, 0.000000000000000000, 0.000000000000000000 ) ) ;
#45918=AXIS2_PLACEMENT_3D ( 'NONE', #22775, #53934, #32355 ) ;
#45923=CARTESIAN_POINT ( 'NONE',  ( -11.31351654964674402, -7.806483450353324471, 195.0000000000000284 ) ) ;
#45928=CIRCLE ( 'NONE', #42506, 0.2000000000000000944 ) ;
#45931=VECTOR ( 'NONE', #31875, 1000.000000000000000 ) ;
#45933=LINE ( 'NONE', #67512, #42695 ) ;
#45935=ORIENTED_EDGE ( 'NONE', *, *, #24931, .T. ) ;
#45942=DIRECTION ( 'NONE',  ( -0.000000000000000000, 3.673940397442059868E-16, -1.000000000000000000 ) ) ;
#45945=PLANE ( 'NONE',  #36075 ) ;
#45949=EDGE_CURVE ( 'NONE', #57533, #64711, #16633, .T. ) ;
#45953=DIRECTION ( 'NONE',  ( -0.000000000000000000, 1.000000000000000000, -0.000000000000000000 ) ) ;
#45956=ORIENTED_EDGE ( 'NONE', *, *, #34444, .T. ) ;
#45958=LINE ( 'NONE', #3184, #52032 ) ;
#45966=AXIS2_PLACEMENT_3D ( 'NONE', #36223, #57791, #39006 ) ;
#45969=ORIENTED_EDGE ( 'NONE', *, *, #58241, .F. ) ;
#45972=VERTEX_POINT ( 'NONE', #33589 ) ;
#45977=ORIENTED_EDGE ( 'NONE', *, *, #21418, .F. ) ;
#45979=DIRECTION ( 'NONE',  ( -0.000000000000000000, 3.673940397442059868E-16, -1.000000000000000000 ) ) ;
#45985=CYLINDRICAL_SURFACE ( 'NONE', #31321, 2.204799999999997873 ) ;
#45996=ORIENTED_EDGE ( 'NONE', *, *, #1401, .F. ) ;
#45998=DIRECTION ( 'NONE',  ( 1.836970198721029934E-16, 1.836970198721010706E-16, -1.000000000000000000 ) ) ;
#46005=CARTESIAN_POINT ( 'NONE',  ( -10.08346604330787777, 9.293516549646602343, 455.0000000000000568 ) ) ;
#46008=AXIS2_PLACEMENT_3D ( 'NONE', #50534, #40616, #30365 ) ;
#46009=CIRCLE ( 'NONE', #1547, 2.204799999999999205 ) ;
#46015=CIRCLE ( 'NONE', #2001, 2.204799999999997873 ) ;
#46017=CARTESIAN_POINT ( 'NONE',  ( -1.853252480934758584, 9.404046420173985510, 195.0000000000000284 ) ) ;
#46020=VERTEX_POINT ( 'NONE', #55167 ) ;
#46024=LINE ( 'NONE', #1837, #24417 ) ;
#46034=ORIENTED_EDGE ( 'NONE', *, *, #15980, .F. ) ;
#46045=EDGE_CURVE ( 'NONE', #54282, #55886, #18887, .T. ) ;
#46059=DIRECTION ( 'NONE',  ( 1.000000000000000000, -8.540177112501197482E-15, 0.000000000000000000 ) ) ;
#46061=EDGE_LOOP ( 'NONE', ( #52825, #16780, #30885, #28687 ) ) ;
#46062=LINE ( 'NONE', #2227, #23816 ) ;
#46065=VECTOR ( 'NONE', #22926, 1000.000000000000000 ) ;
#46066=DIRECTION ( 'NONE',  ( -1.000000000000000000, 0.000000000000000000, 0.000000000000000000 ) ) ;
#46074=ORIENTED_EDGE ( 'NONE', *, *, #56854, .T. ) ;
#46078=CARTESIAN_POINT ( 'NONE',  ( 3.606483450353354048, 5.993516549646638047, 195.0000000000000284 ) ) ;
#46083=DIRECTION ( 'NONE',  ( 0.000000000000000000, 3.673940397442059868E-16, -1.000000000000000000 ) ) ;
#46085=ORIENTED_EDGE ( 'NONE', *, *, #19729, .T. ) ;
#46092=ORIENTED_EDGE ( 'NONE', *, *, #10466, .T. ) ;
#46094=EDGE_CURVE ( 'NONE', #20214, #29928, #18713, .T. ) ;
#46095=EDGE_LOOP ( 'NONE', ( #32248, #69489, #27403, #19662 ) ) ;
#46096=ORIENTED_EDGE ( 'NONE', *, *, #40054, .F. ) ;
#46100=CARTESIAN_POINT ( 'NONE',  ( -7.415254214038336400, 2.993516549646603853, 195.0000000000000284 ) ) ;
#46101=EDGE_LOOP ( 'NONE', ( #15731, #7680, #25584, #51658 ) ) ;
#46107=DIRECTION ( 'NONE',  ( 1.836970198721029934E-16, 1.836970198721010706E-16, -1.000000000000000000 ) ) ;
#46135=ORIENTED_EDGE ( 'NONE', *, *, #64668, .T. ) ;
#46149=ORIENTED_EDGE ( 'NONE', *, *, #68324, .T. ) ;
#46158=DIRECTION ( 'NONE',  ( 0.6414496315691539108, -0.7671651518153028704, -2.587583378555131256E-16 ) ) ;
#46163=ORIENTED_EDGE ( 'NONE', *, *, #12904, .F. ) ;
#46165=VECTOR ( 'NONE', #136, 1000.000000000000000 ) ;
#46167=EDGE_LOOP ( 'NONE', ( #10317, #50393, #32891, #17281 ) ) ;
#46168=ORIENTED_EDGE ( 'NONE', *, *, #32741, .F. ) ;
#46173=CYLINDRICAL_SURFACE ( 'NONE', #606, 0.1999999999999987899 ) ;
#46179=VERTEX_POINT ( 'NONE', #19753 ) ;
#46181=AXIS2_PLACEMENT_3D ( 'NONE', #11492, #33072, #18437 ) ;
#46186=LINE ( 'NONE', #3073, #41477 ) ;
#46190=CARTESIAN_POINT ( 'NONE',  ( 5.668387132715918320, -8.406483450353393394, 195.0000000000000284 ) ) ;
#46193=VECTOR ( 'NONE', #21631, 1000.000000000000114 ) ;
#46194=EDGE_CURVE ( 'NONE', #33821, #64137, #58313, .T. ) ;
#46195=DIRECTION ( 'NONE',  ( -1.254221251785257574E-14, -1.000000000000000000, -1.836970198721013417E-16 ) ) ;
#46196=VERTEX_POINT ( 'NONE', #57598 ) ;
#46198=FACE_OUTER_BOUND ( 'NONE', #24658, .T. ) ;
#46204=DIRECTION ( 'NONE',  ( 0.000000000000000000, 0.000000000000000000, -1.000000000000000000 ) ) ;
#46208=ORIENTED_EDGE ( 'NONE', *, *, #48606, .T. ) ;
#46209=LINE ( 'NONE', #20398, #55811 ) ;
#46210=EDGE_CURVE ( 'NONE', #30360, #23736, #31084, .T. ) ;
#46212=VERTEX_POINT ( 'NONE', #9164 ) ;
#46213=DIRECTION ( 'NONE',  ( 1.836970198721029934E-16, 1.836970198721010706E-16, -1.000000000000000000 ) ) ;
#46229=EDGE_CURVE ( 'NONE', #52964, #2177, #68913, .T. ) ;
#46243=DIRECTION ( 'NONE',  ( -1.047444401652939849E-14, -1.000000000000000000, -1.836970198721029934E-16 ) ) ;
#46249=ORIENTED_EDGE ( 'NONE', *, *, #11006, .F. ) ;
#46250=DIRECTION ( 'NONE',  ( -0.7071067811865560104, -0.7071067811865391350, -2.597868168706466792E-16 ) ) ;
#46263=VERTEX_POINT ( 'NONE', #63969 ) ;
#46271=ORIENTED_EDGE ( 'NONE', *, *, #11601, .T. ) ;
#46272=CIRCLE ( 'NONE', #15803, 1.399999999999998579 ) ;
#46280=LINE ( 'NONE', #67519, #33999 ) ;
#46286=VERTEX_POINT ( 'NONE', #37095 ) ;
#46290=EDGE_CURVE ( 'NONE', #62792, #16263, #53357, .T. ) ;
#46298=VERTEX_POINT ( 'NONE', #30379 ) ;
#46302=EDGE_CURVE ( 'NONE', #21517, #43460, #67442, .T. ) ;
#46317=CARTESIAN_POINT ( 'NONE',  ( 7.806483450353379538, -11.12648345035339226, 195.0000000000000284 ) ) ;
#46319=DIRECTION ( 'NONE',  ( -0.6414496315691494699, 0.7671651518153064231, 2.818519042764025305E-16 ) ) ;
#46321=ORIENTED_EDGE ( 'NONE', *, *, #43323, .F. ) ;
#46324=EDGE_LOOP ( 'NONE', ( #45731, #43982, #13078, #4170 ) ) ;
#46328=FACE_OUTER_BOUND ( 'NONE', #69118, .T. ) ;
#46332=CARTESIAN_POINT ( 'NONE',  ( 7.616533956692213003, -8.406483450353491094, 455.0000000000000568 ) ) ;
#46347=VERTEX_POINT ( 'NONE', #21513 ) ;
#46350=CARTESIAN_POINT ( 'NONE',  ( 6.006483450353379716, -6.006483450353490738, 455.0000000000000568 ) ) ;
#46360=LINE ( 'NONE', #52377, #1249 ) ;
#46361=ORIENTED_EDGE ( 'NONE', *, *, #32741, .T. ) ;
#46363=VECTOR ( 'NONE', #37360, 1000.000000000000000 ) ;
#46368=CARTESIAN_POINT ( 'NONE',  ( -10.91351654964670992, -2.706483450353338593, 455.0000000000000568 ) ) ;
#46374=VECTOR ( 'NONE', #17104, 1000.000000000000000 ) ;
#46383=ORIENTED_EDGE ( 'NONE', *, *, #2195, .T. ) ;
#46395=DIRECTION ( 'NONE',  ( 8.673617379884013384E-15, 1.000000000000000000, 0.000000000000000000 ) ) ;
#46396=ORIENTED_EDGE ( 'NONE', *, *, #4750, .F. ) ;
#46403=ORIENTED_EDGE ( 'NONE', *, *, #15282, .F. ) ;
#46405=AXIS2_PLACEMENT_3D ( 'NONE', #50011, #28439, #67336 ) ;
#46414=FACE_BOUND ( 'NONE', #51015, .T. ) ;
#46415=VECTOR ( 'NONE', #19432, 1000.000000000000114 ) ;
#46418=ORIENTED_EDGE ( 'NONE', *, *, #23715, .F. ) ;
#46423=PLANE ( 'NONE',  #12946 ) ;
#46426=CARTESIAN_POINT ( 'NONE',  ( -5.993516549646776603, -6.006483450353426790, 455.0000000000000568 ) ) ;
#46430=ORIENTED_EDGE ( 'NONE', *, *, #5144, .F. ) ;
#46441=ORIENTED_EDGE ( 'NONE', *, *, #47844, .F. ) ;
#46456=CARTESIAN_POINT ( 'NONE',  ( -4.393516549646667713, 11.77351654964658856, 195.0000000000000284 ) ) ;
#46468=AXIS2_PLACEMENT_3D ( 'NONE', #54081, #15204, #21886 ) ;
#46471=CARTESIAN_POINT ( 'NONE',  ( -11.77351654964679106, -7.606483450353366038, 455.0000000000000568 ) ) ;
#46474=DIRECTION ( 'NONE',  ( 0.000000000000000000, 0.000000000000000000, 1.000000000000000000 ) ) ;
#46480=CARTESIAN_POINT ( 'NONE',  ( 8.406483450353379183, -4.396432944014562416, 195.0000000000000284 ) ) ;
#46482=ORIENTED_EDGE ( 'NONE', *, *, #52166, .F. ) ;
#46498=CARTESIAN_POINT ( 'NONE',  ( -4.383466043307969962, -8.606483450353444198, 455.0000000000000568 ) ) ;
#46501=ORIENTED_EDGE ( 'NONE', *, *, #39732, .F. ) ;
#46513=AXIS2_PLACEMENT_3D ( 'NONE', #46498, #67720, #45095 ) ;
#46518=CARTESIAN_POINT ( 'NONE',  ( 8.211283450353400681, 5.993516549646574099, 455.0000000000000568 ) ) ;
#46524=PLANE ( 'NONE',  #49832 ) ;
#46526=ORIENTED_EDGE ( 'NONE', *, *, #67466, .T. ) ;
#46535=CARTESIAN_POINT ( 'NONE',  ( -5.655420232009359616, -8.406483450353428921, 455.0000000000000568 ) ) ;
#46536=ORIENTED_EDGE ( 'NONE', *, *, #48950, .T. ) ;
#46538=LINE ( 'NONE', #2365, #35480 ) ;
#46542=VECTOR ( 'NONE', #3010, 1000.000000000000000 ) ;
#46545=ORIENTED_EDGE ( 'NONE', *, *, #12911, .F. ) ;
#46548=AXIS2_PLACEMENT_3D ( 'NONE', #23232, #66715, #55763 ) ;
#46549=FACE_OUTER_BOUND ( 'NONE', #13227, .T. ) ;
#46553=CARTESIAN_POINT ( 'NONE',  ( -7.798499376344067535, 4.727349090213368576, 455.0000000000000568 ) ) ;
#46554=DIRECTION ( 'NONE',  ( -0.5000000000000004441, 0.8660254037844383745, 3.181725716174720005E-16 ) ) ;
#46557=CARTESIAN_POINT ( 'NONE',  ( -1.677516549646676625, 10.73351654964656987, 195.0000000000000284 ) ) ;
#46564=EDGE_CURVE ( 'NONE', #23831, #5664, #39491, .T. ) ;
#46565=CARTESIAN_POINT ( 'NONE',  ( -4.188533722949369320, -4.740315990920150213, 195.0000000000000284 ) ) ;
#46577=ADVANCED_FACE ( 'NONE', ( #45488 ), #13324, .T. ) ;
#46579=CARTESIAN_POINT ( 'NONE',  ( -10.91351654964670637, 9.293516549646604119, 195.0000000000000284 ) ) ;
#46580=ORIENTED_EDGE ( 'NONE', *, *, #64059, .F. ) ;
#46584=ORIENTED_EDGE ( 'NONE', *, *, #29181, .T. ) ;
#46585=DIRECTION ( 'NONE',  ( 0.000000000000000000, 1.000000000000000000, 0.000000000000000000 ) ) ;
#46590=CARTESIAN_POINT ( 'NONE',  ( 7.265214908726123078, -5.393625297350022052, 455.0000000000000568 ) ) ;
#46592=DIRECTION ( 'NONE',  ( -1.836970198721029934E-16, 1.836970198721036344E-16, -1.000000000000000000 ) ) ;
#46605=CARTESIAN_POINT ( 'NONE',  ( -7.813516549646839948, -12.00648345035340903, 455.0000000000000568 ) ) ;
#46611=ORIENTED_EDGE ( 'NONE', *, *, #43684, .F. ) ;
#46613=CARTESIAN_POINT ( 'NONE',  ( 12.00648345035338060, -7.826483450353395988, 195.0000000000000284 ) ) ;
#46629=CARTESIAN_POINT ( 'NONE',  ( -4.242044687070550602, 8.452095193409279617, 455.0000000000000568 ) ) ;
#46638=DIRECTION ( 'NONE',  ( 0.000000000000000000, 1.000000000000000000, 0.000000000000000000 ) ) ;
#46643=ORIENTED_EDGE ( 'NONE', *, *, #1996, .T. ) ;
#46648=EDGE_CURVE ( 'NONE', #22317, #67902, #36295, .T. ) ;
#46649=ORIENTED_EDGE ( 'NONE', *, *, #26296, .T. ) ;
#46656=ADVANCED_FACE ( 'NONE', ( #36644 ), #47262, .F. ) ;
#46666=CARTESIAN_POINT ( 'NONE',  ( 11.78648345035335865, 7.593516549646607494, 195.0000000000000284 ) ) ;
#46676=CIRCLE ( 'NONE', #29760, 0.1999999999999987899 ) ;
#46682=DIRECTION ( 'NONE',  ( -1.836970198721029934E-16, 1.836970198721036344E-16, -1.000000000000000000 ) ) ;
#46683=DIRECTION ( 'NONE',  ( 1.000000000000000000, -3.016910393003147986E-15, 0.000000000000000000 ) ) ;
#46696=VERTEX_POINT ( 'NONE', #68118 ) ;
#46698=ADVANCED_FACE ( 'NONE', ( #19666 ), #35580, .F. ) ;
#46700=EDGE_CURVE ( 'NONE', #25895, #31596, #26879, .T. ) ;
#46705=ADVANCED_FACE ( 'NONE', ( #15778 ), #10468, .F. ) ;
#46707=ORIENTED_EDGE ( 'NONE', *, *, #55719, .T. ) ;
#46708=DIRECTION ( 'NONE',  ( 1.000000000000000000, -3.016910393003147986E-15, 0.000000000000000000 ) ) ;
#46728=CARTESIAN_POINT ( 'NONE',  ( -9.942044687070568543, 9.234937905883914055, 455.0000000000000568 ) ) ;
#46733=CARTESIAN_POINT ( 'NONE',  ( -7.798499376344109280, -4.740315990920159095, 455.0000000000000568 ) ) ;
#46745=ORIENTED_EDGE ( 'NONE', *, *, #14074, .F. ) ;
#46757=CARTESIAN_POINT ( 'NONE',  ( 2.906483450353369413, 10.08346604330780671, 195.0000000000000284 ) ) ;
#46760=CARTESIAN_POINT ( 'NONE',  ( 4.186483450353337687, -11.78648345035337996, 195.0000000000000284 ) ) ;
#46764=EDGE_LOOP ( 'NONE', ( #5839, #27276, #32709, #15206 ) ) ;
#46769=DIRECTION ( 'NONE',  ( 1.836970198721029934E-16, 1.836970198721010706E-16, -1.000000000000000000 ) ) ;
#46779=ORIENTED_EDGE ( 'NONE', *, *, #51347, .T. ) ;
#46783=DIRECTION ( 'NONE',  ( 0.6414496315691592399, 0.7671651518152985405, 2.309356642088728176E-17 ) ) ;
#46788=EDGE_CURVE ( 'NONE', #32262, #49212, #10816, .T. ) ;
#46793=CARTESIAN_POINT ( 'NONE',  ( 10.92648345035331658, 2.893516549646575786, 195.0000000000000284 ) ) ;
#46798=VERTEX_POINT ( 'NONE', #43696 ) ;
#46808=CARTESIAN_POINT ( 'NONE',  ( 11.34648345035338046, -1.090483450353491035, 455.0000000000000568 ) ) ;
#46811=DIRECTION ( 'NONE',  ( 1.000000000000000000, 0.000000000000000000, 0.000000000000000000 ) ) ;
#46812=CARTESIAN_POINT ( 'NONE',  ( 7.811466277050736373, -7.272650909786728235, 455.0000000000000568 ) ) ;
#46820=CIRCLE ( 'NONE', #53662, 1.399999999999999245 ) ;
#46822=ORIENTED_EDGE ( 'NONE', *, *, #16363, .F. ) ;
#46827=ADVANCED_FACE ( 'NONE', ( #65605 ), #69866, .F. ) ;
#46835=EDGE_CURVE ( 'NONE', #16863, #11814, #65934, .T. ) ;
#46837=DIRECTION ( 'NONE',  ( -0.000000000000000000, 3.673940397442059868E-16, -1.000000000000000000 ) ) ;
#46838=DIRECTION ( 'NONE',  ( -0.7671651518152985405, 0.6414496315691592399, 2.587583378555131749E-16 ) ) ;
#46848=FACE_OUTER_BOUND ( 'NONE', #6610, .T. ) ;
#46849=DIRECTION ( 'NONE',  ( -0.000000000000000000, -0.000000000000000000, -1.000000000000000000 ) ) ;
#46850=VERTEX_POINT ( 'NONE', #50024 ) ;
#46857=DIRECTION ( 'NONE',  ( -1.000000000000000000, 3.491481338843133355E-15, 1.836970198721036344E-16 ) ) ;
#46875=EDGE_CURVE ( 'NONE', #6389, #15026, #14495, .T. ) ;
#46876=CIRCLE ( 'NONE', #59303, 0.5999999999999998668 ) ;
#46884=EDGE_CURVE ( 'NONE', #39630, #14703, #44712, .T. ) ;
#46885=EDGE_LOOP ( 'NONE', ( #43851, #2442, #18804, #1133 ) ) ;
#46887=CARTESIAN_POINT ( 'NONE',  ( 10.09643294401454661, -2.706483450353491804, 455.0000000000000568 ) ) ;
#46893=LINE ( 'NONE', #67432, #68550 ) ;
#46902=CARTESIAN_POINT ( 'NONE',  ( 4.186483450353376767, 11.99351654964663716, 195.0000000000000284 ) ) ;
#46915=AXIS2_PLACEMENT_3D ( 'NONE', #34895, #40910, #29953 ) ;
#46921=AXIS2_PLACEMENT_3D ( 'NONE', #6451, #43578, #54550 ) ;
#46944=DIRECTION ( 'NONE',  ( 1.000000000000000000, -1.047444401652939849E-14, 0.000000000000000000 ) ) ;
#46948=CARTESIAN_POINT ( 'NONE',  ( 11.78648345035337819, -7.826483450353395988, 195.0000000000000284 ) ) ;
#46950=ORIENTED_EDGE ( 'NONE', *, *, #18526, .F. ) ;
#46965=CARTESIAN_POINT ( 'NONE',  ( -9.293516549646710700, 10.91351654964659801, 195.0000000000000284 ) ) ;
#46977=VECTOR ( 'NONE', #50621, 1000.000000000000000 ) ;
#46982=CARTESIAN_POINT ( 'NONE',  ( -7.259684009079963474, -4.201500623656036382, 455.0000000000000568 ) ) ;
#46990=DIRECTION ( 'NONE',  ( 0.6414496315691617934, -0.7671651518152962090, -2.818519042763987834E-16 ) ) ;
#46992=DIRECTION ( 'NONE',  ( -1.836970198721029934E-16, 1.836970198721036344E-16, -1.000000000000000000 ) ) ;
#46994=ORIENTED_EDGE ( 'NONE', *, *, #1401, .T. ) ;
#46995=CARTESIAN_POINT ( 'NONE',  ( -11.07551654964683330, -11.48848345035333907, 455.0000000000000568 ) ) ;
#47008=ORIENTED_EDGE ( 'NONE', *, *, #25118, .T. ) ;
#47014=DIRECTION ( 'NONE',  ( 1.261617073437657735E-14, 1.000000000000000000, 3.673940397442059868E-16 ) ) ;
#47015=ORIENTED_EDGE ( 'NONE', *, *, #41350, .F. ) ;
#47020=AXIS2_PLACEMENT_3D ( 'NONE', #50987, #39335, #45671 ) ;
#47023=AXIS2_PLACEMENT_3D ( 'NONE', #514, #65225, #34048 ) ;
#47030=ORIENTED_EDGE ( 'NONE', *, *, #4892, .F. ) ;
#47034=VECTOR ( 'NONE', #59519, 1000.000000000000000 ) ;
#47036=AXIS2_PLACEMENT_3D ( 'NONE', #722, #48806, #37160 ) ;
#47038=CARTESIAN_POINT ( 'NONE',  ( 11.48848345035337282, 11.07551654964657395, 195.0000000000000284 ) ) ;
#47046=CARTESIAN_POINT ( 'NONE',  ( 10.20488345035340849, 11.07551654964657928, 195.0000000000000284 ) ) ;
#47047=ORIENTED_EDGE ( 'NONE', *, *, #27093, .T. ) ;
#47056=ADVANCED_FACE ( 'NONE', ( #19249 ), #25262, .F. ) ;
#47059=ADVANCED_FACE ( 'NONE', ( #8642 ), #36561, .F. ) ;
#47074=CARTESIAN_POINT ( 'NONE',  ( -7.593516549646711411, 11.77351654964660277, 455.0000000000000568 ) ) ;
#47082=CARTESIAN_POINT ( 'NONE',  ( 11.12648345035337982, -4.206483450353396769, 195.0000000000000284 ) ) ;
#47090=ORIENTED_EDGE ( 'NONE', *, *, #28525, .T. ) ;
#47091=VECTOR ( 'NONE', #5586, 1000.000000000000000 ) ;
#47098=ORIENTED_EDGE ( 'NONE', *, *, #23119, .T. ) ;
#47108=DIRECTION ( 'NONE',  ( -1.000000000000000000, 0.000000000000000000, 0.000000000000000000 ) ) ;
#47116=LINE ( 'NONE', #27209, #22099 ) ;
#47124=VERTEX_POINT ( 'NONE', #38317 ) ;
#47137=EDGE_CURVE ( 'NONE', #46196, #51028, #43260, .T. ) ;
#47143=EDGE_CURVE ( 'NONE', #55385, #64507, #26309, .T. ) ;
#47157=ORIENTED_EDGE ( 'NONE', *, *, #17736, .T. ) ;
#47159=CARTESIAN_POINT ( 'NONE',  ( -8.452095193409434160, -4.255011587777239868, 455.0000000000000568 ) ) ;
#47161=CARTESIAN_POINT ( 'NONE',  ( -10.19191654964686933, -11.48848345035334795, 455.0000000000000568 ) ) ;
#47167=DIRECTION ( 'NONE',  ( -3.903627567395476653E-15, -1.000000000000000000, -1.836970198721029194E-16 ) ) ;
#47176=LINE ( 'NONE', #24199, #11147 ) ;
#47177=CARTESIAN_POINT ( 'NONE',  ( -7.259684009079930611, 4.188533722949235205, 455.0000000000000568 ) ) ;
#47183=CARTESIAN_POINT ( 'NONE',  ( 9.106483450353380249, -10.92648345035348711, 455.0000000000000568 ) ) ;
#47196=CARTESIAN_POINT ( 'NONE',  ( 4.622483450353380263, -3.606483450353395792, 195.0000000000000284 ) ) ;
#47198=CARTESIAN_POINT ( 'NONE',  ( -11.99351654964671354, 7.813516549646603693, 455.0000000000000568 ) ) ;
#47199=( GEOMETRIC_REPRESENTATION_CONTEXT ( 3 ) GLOBAL_UNCERTAINTY_ASSIGNED_CONTEXT ( ( #26025 ) ) GLOBAL_UNIT_ASSIGNED_CONTEXT ( ( #19999, #36253, #27396 ) ) REPRESENTATION_CONTEXT ( 'NONE', 'WORKASPACE' ) );
#47204=EDGE_CURVE ( 'NONE', #65422, #47230, #48928, .T. ) ;
#47205=ADVANCED_FACE ( 'NONE', ( #486 ), #48233, .T. ) ;
#47207=LINE ( 'NONE', #10418, #60301 ) ;
#47210=EDGE_CURVE ( 'NONE', #22923, #54282, #17084, .T. ) ;
#47221=DIRECTION ( 'NONE',  ( -0.000000000000000000, 3.673940397442059868E-16, -1.000000000000000000 ) ) ;
#47222=ORIENTED_EDGE ( 'NONE', *, *, #28965, .T. ) ;
#47225=DIRECTION ( 'NONE',  ( 0.000000000000000000, -3.673940397442059868E-16, 1.000000000000000000 ) ) ;
#47227=DIRECTION ( 'NONE',  ( -0.000000000000000000, 1.000000000000000000, -0.000000000000000000 ) ) ;
#47230=VERTEX_POINT ( 'NONE', #45676 ) ;
#47233=ORIENTED_EDGE ( 'NONE', *, *, #49443, .T. ) ;
#47235=ORIENTED_EDGE ( 'NONE', *, *, #41065, .F. ) ;
#47236=ORIENTED_EDGE ( 'NONE', *, *, #67389, .T. ) ;
#47237=CARTESIAN_POINT ( 'NONE',  ( 8.406483450353379183, -6.344579767990935260, 455.0000000000000568 ) ) ;
#47239=CARTESIAN_POINT ( 'NONE',  ( -8.393516549646744096, -7.616533956692189022, 195.0000000000000284 ) ) ;
#47254=ORIENTED_EDGE ( 'NONE', *, *, #34405, .F. ) ;
#47260=DIRECTION ( 'NONE',  ( 0.000000000000000000, 1.000000000000000000, 0.000000000000000000 ) ) ;
#47262=PLANE ( 'NONE',  #33618 ) ;
#47271=FACE_OUTER_BOUND ( 'NONE', #3625, .T. ) ;
#47283=ORIENTED_EDGE ( 'NONE', *, *, #67053, .F. ) ;
#47289=ORIENTED_EDGE ( 'NONE', *, *, #14695, .F. ) ;
#47290=LINE ( 'NONE', #62477, #44991 ) ;
#47304=DIRECTION ( 'NONE',  ( -3.491481338843132961E-15, -1.000000000000000000, 0.000000000000000000 ) ) ;
#47306=CARTESIAN_POINT ( 'NONE',  ( -1.853252480934882929, -9.417013320880883498, 455.0000000000000568 ) ) ;
#47327=DIRECTION ( 'NONE',  ( -0.000000000000000000, -0.000000000000000000, -1.000000000000000000 ) ) ;
#47329=VERTEX_POINT ( 'NONE', #28046 ) ;
#47331=DIRECTION ( 'NONE',  ( 4.745709458399858621E-16, 1.000000000000000000, 1.836970198721035604E-16 ) ) ;
#47342=FACE_OUTER_BOUND ( 'NONE', #62565, .T. ) ;
#47345=DIRECTION ( 'NONE',  ( 1.000000000000000000, 0.000000000000000000, 0.000000000000000000 ) ) ;
#47351=LINE ( 'NONE', #48053, #17206 ) ;
#47358=CARTESIAN_POINT ( 'NONE',  ( -11.47551654964683010, -11.08848345035333338, 455.0000000000000568 ) ) ;
#47366=ORIENTED_EDGE ( 'NONE', *, *, #50409, .F. ) ;
#47368=ORIENTED_EDGE ( 'NONE', *, *, #59332, .T. ) ;
#47370=ORIENTED_EDGE ( 'NONE', *, *, #13817, .F. ) ;
#47386=LINE ( 'NONE', #42079, #25343 ) ;
#47390=CARTESIAN_POINT ( 'NONE',  ( -11.77351654964674310, -7.606483450353318965, 195.0000000000000284 ) ) ;
#47398=AXIS2_PLACEMENT_3D ( 'NONE', #6816, #55277, #55614 ) ;
#47420=DIRECTION ( 'NONE',  ( 1.836970198721029934E-16, 1.836970198721010706E-16, -1.000000000000000000 ) ) ;
#47426=CIRCLE ( 'NONE', #13553, 0.5999999999999998668 ) ;
#47429=ORIENTED_EDGE ( 'NONE', *, *, #25209, .F. ) ;
#47436=CIRCLE ( 'NONE', #18042, 0.1999999999999987899 ) ;
#47455=CIRCLE ( 'NONE', #16972, 0.1999999999999987899 ) ;
#47459=VERTEX_POINT ( 'NONE', #24825 ) ;
#47460=EDGE_CURVE ( 'NONE', #33281, #31845, #23560, .T. ) ;
#47465=ORIENTED_EDGE ( 'NONE', *, *, #24123, .T. ) ;
#47475=ORIENTED_EDGE ( 'NONE', *, *, #12685, .T. ) ;
#47478=LINE ( 'NONE', #10012, #62684 ) ;
#47479=DIRECTION ( 'NONE',  ( -0.7071067811865527908, -0.7071067811865422437, 0.000000000000000000 ) ) ;
#47485=VERTEX_POINT ( 'NONE', #67962 ) ;
#47486=VERTEX_POINT ( 'NONE', #19165 ) ;
#47490=VERTEX_POINT ( 'NONE', #20824 ) ;
#47502=CARTESIAN_POINT ( 'NONE',  ( -10.19191654964671301, 11.47551654964660450, 455.0000000000000568 ) ) ;
#47503=DIRECTION ( 'NONE',  ( 1.000000000000000000, -3.903627567395476653E-15, 0.000000000000000000 ) ) ;
#47512=LINE ( 'NONE', #52842, #15990 ) ;
#47515=EDGE_CURVE ( 'NONE', #47649, #43371, #21189, .T. ) ;
#47517=CARTESIAN_POINT ( 'NONE',  ( -8.593516549646711411, 4.383466043307770121, 455.0000000000000568 ) ) ;
#47523=ADVANCED_FACE ( 'NONE', ( #40736 ), #62292, .F. ) ;
#47531=CIRCLE ( 'NONE', #17047, 1.399999999999998579 ) ;
#47540=AXIS2_PLACEMENT_3D ( 'NONE', #44911, #28638, #66474 ) ;
#47542=LINE ( 'NONE', #4764, #55685 ) ;
#47545=LINE ( 'NONE', #63107, #31749 ) ;
#47551=EDGE_CURVE ( 'NONE', #48678, #35336, #17246, .T. ) ;
#47557=DIRECTION ( 'NONE',  ( 0.000000000000000000, -3.673940397442059868E-16, 1.000000000000000000 ) ) ;
#47562=LINE ( 'NONE', #25293, #29598 ) ;
#47565=ORIENTED_EDGE ( 'NONE', *, *, #28406, .T. ) ;
#47571=ORIENTED_EDGE ( 'NONE', *, *, #16194, .F. ) ;
#47573=ORIENTED_EDGE ( 'NONE', *, *, #30122, .F. ) ;
#47576=ORIENTED_EDGE ( 'NONE', *, *, #9643, .T. ) ;
#47577=PLANE ( 'NONE',  #68872 ) ;
#47579=DIRECTION ( 'NONE',  ( 1.000000000000000000, 2.135044278125301343E-15, 0.000000000000000000 ) ) ;
#47587=EDGE_CURVE ( 'NONE', #13563, #55579, #54125, .T. ) ;
#47592=FACE_OUTER_BOUND ( 'NONE', #11873, .T. ) ;
#47596=VECTOR ( 'NONE', #15991, 1000.000000000000000 ) ;
#47601=DIRECTION ( 'NONE',  ( -0.000000000000000000, 3.673940397442059868E-16, -1.000000000000000000 ) ) ;
#47602=PLANE ( 'NONE',  #33554 ) ;
#47604=DIRECTION ( 'NONE',  ( 0.8660254037844510311, 0.4999999999999785727, 0.000000000000000000 ) ) ;
#47607=CARTESIAN_POINT ( 'NONE',  ( 4.747751991980625696, -6.619341603356844850, 195.0000000000000284 ) ) ;
#47621=DIRECTION ( 'NONE',  ( -0.6414496315691537998, 0.7671651518153029814, 0.000000000000000000 ) ) ;
#47625=DIRECTION ( 'NONE',  ( 0.7671651518153105309, -0.6414496315691445849, -0.000000000000000000 ) ) ;
#47628=ORIENTED_EDGE ( 'NONE', *, *, #55077, .F. ) ;
#47635=EDGE_CURVE ( 'NONE', #22923, #29997, #64655, .T. ) ;
#47642=ORIENTED_EDGE ( 'NONE', *, *, #12386, .T. ) ;
#47646=FACE_OUTER_BOUND ( 'NONE', #39126, .T. ) ;
#47648=CARTESIAN_POINT ( 'NONE',  ( -4.734785091273957747, 6.606374702650051667, 455.0000000000000568 ) ) ;
#47649=VERTEX_POINT ( 'NONE', #10919 ) ;
#47653=CARTESIAN_POINT ( 'NONE',  ( 11.08848345035334404, -9.804883450353528929, 455.0000000000000568 ) ) ;
#47656=EDGE_LOOP ( 'NONE', ( #19103, #53646, #35975, #59729 ) ) ;
#47668=CARTESIAN_POINT ( 'NONE',  ( 11.12648345035337982, -7.806483450353490561, 455.0000000000000568 ) ) ;
#47670=VECTOR ( 'NONE', #663, 1000.000000000000000 ) ;
#47676=LINE ( 'NONE', #63950, #12477 ) ;
#47689=CARTESIAN_POINT ( 'NONE',  ( 11.78648345035337819, -7.606483450353398013, 195.0000000000000284 ) ) ;
#47697=DIRECTION ( 'NONE',  ( -1.000000000000000000, 0.000000000000000000, 0.000000000000000000 ) ) ;
#47698=DIRECTION ( 'NONE',  ( 0.6414496315691565753, 0.7671651518153006499, 2.818519042764004597E-16 ) ) ;
#47704=CIRCLE ( 'NONE', #65764, 0.1999999999999987899 ) ;
#47734=DIRECTION ( 'NONE',  ( -0.000000000000000000, 3.673940397442059868E-16, -1.000000000000000000 ) ) ;
#47736=VECTOR ( 'NONE', #21572, 1000.000000000000000 ) ;
#47739=CARTESIAN_POINT ( 'NONE',  ( -5.993516549646776603, -6.006483450353426790, 455.0000000000000568 ) ) ;
#47744=CARTESIAN_POINT ( 'NONE',  ( -9.093516549646711411, 11.11351654964659730, 455.0000000000000568 ) ) ;
#47755=VECTOR ( 'NONE', #11577, 1000.000000000000000 ) ;
#47758=ORIENTED_EDGE ( 'NONE', *, *, #36659, .T. ) ;
#47760=VECTOR ( 'NONE', #29387, 1000.000000000000000 ) ;
#47762=CARTESIAN_POINT ( 'NONE',  ( -11.99351654964671354, 4.173516549646604901, 195.0000000000000284 ) ) ;
#47764=EDGE_CURVE ( 'NONE', #57794, #62883, #29589, .T. ) ;
#47765=ORIENTED_EDGE ( 'NONE', *, *, #38895, .F. ) ;
#47767=VERTEX_POINT ( 'NONE', #40549 ) ;
#47769=LINE ( 'NONE', #27263, #44229 ) ;
#47774=LINE ( 'NONE', #37186, #15720 ) ;
#47776=ORIENTED_EDGE ( 'NONE', *, *, #20413, .T. ) ;
#47788=ORIENTED_EDGE ( 'NONE', *, *, #16153, .F. ) ;
#47792=AXIS2_PLACEMENT_3D ( 'NONE', #63744, #10346, #16699 ) ;
#47796=ORIENTED_EDGE ( 'NONE', *, *, #50576, .T. ) ;
#47799=LINE ( 'NONE', #24841, #57964 ) ;
#47810=ORIENTED_EDGE ( 'NONE', *, *, #27642, .F. ) ;
#47817=CARTESIAN_POINT ( 'NONE',  ( -1.677516549646816291, -9.841277389592811176, 455.0000000000000568 ) ) ;
#47822=EDGE_LOOP ( 'NONE', ( #2120, #36441, #23181, #21458 ) ) ;
#47825=CARTESIAN_POINT ( 'NONE',  ( 11.12648345035337982, -7.806483450353490561, 455.0000000000000568 ) ) ;
#47832=VERTEX_POINT ( 'NONE', #41961 ) ;
#47844=EDGE_CURVE ( 'NONE', #68196, #15146, #13420, .T. ) ;
#47850=DIRECTION ( 'NONE',  ( -0.000000000000000000, 3.673940397442059868E-16, -1.000000000000000000 ) ) ;
#47857=CARTESIAN_POINT ( 'NONE',  ( -8.393516549646712122, 5.655420232009161552, 195.0000000000000284 ) ) ;
#47859=AXIS2_PLACEMENT_3D ( 'NONE', #35094, #56675, #35443 ) ;
#47863=FACE_BOUND ( 'NONE', #50283, .T. ) ;
#47864=EDGE_CURVE ( 'NONE', #30586, #56148, #3432, .T. ) ;
#47873=CARTESIAN_POINT ( 'NONE',  ( 4.201500623655991085, 7.259684009079854228, 195.0000000000000284 ) ) ;
#47876=EDGE_CURVE ( 'NONE', #52264, #19534, #60857, .T. ) ;
#47894=VECTOR ( 'NONE', #47479, 1000.000000000000000 ) ;
#47898=VERTEX_POINT ( 'NONE', #19674 ) ;
#47899=DIRECTION ( 'NONE',  ( 0.000000000000000000, 0.000000000000000000, 1.000000000000000000 ) ) ;
#47913=VECTOR ( 'NONE', #60021, 1000.000000000000114 ) ;
#47916=ORIENTED_EDGE ( 'NONE', *, *, #5135, .T. ) ;
#47919=LINE ( 'NONE', #26708, #14699 ) ;
#47929=DIRECTION ( 'NONE',  ( -0.000000000000000000, 3.673940397442059868E-16, -1.000000000000000000 ) ) ;
#47943=ORIENTED_EDGE ( 'NONE', *, *, #52519, .T. ) ;
#47946=VECTOR ( 'NONE', #34679, 1000.000000000000114 ) ;
#47948=CARTESIAN_POINT ( 'NONE',  ( 7.272650909786598561, -7.811466277050860718, 455.0000000000000568 ) ) ;
#47951=DIRECTION ( 'NONE',  ( -0.000000000000000000, -0.000000000000000000, -1.000000000000000000 ) ) ;
#47953=LINE ( 'NONE', #64570, #55644 ) ;
#47954=AXIS2_PLACEMENT_3D ( 'NONE', #46426, #24867, #25222 ) ;
#47955=DIRECTION ( 'NONE',  ( -1.836970198721029934E-16, 1.836970198721036344E-16, -1.000000000000000000 ) ) ;
#47957=AXIS2_PLACEMENT_3D ( 'NONE', #36338, #4180, #25748 ) ;
#47961=CARTESIAN_POINT ( 'NONE',  ( -10.91351654964670992, -2.706483450353338593, 455.0000000000000568 ) ) ;
#47968=AXIS2_PLACEMENT_3D ( 'NONE', #39289, #62243, #39624 ) ;
#47978=LINE ( 'NONE', #36672, #13566 ) ;
#47979=EDGE_LOOP ( 'NONE', ( #11382, #4028, #48324, #32274 ) ) ;
#47983=DIRECTION ( 'NONE',  ( -1.000000000000000000, 1.260948829465470062E-14, -1.836970198721007008E-16 ) ) ;
#47991=DIRECTION ( 'NONE',  ( 0.000000000000000000, -1.000000000000000000, 0.000000000000000000 ) ) ;
#47993=EDGE_CURVE ( 'NONE', #54514, #705, #27786, .T. ) ;
#47994=ORIENTED_EDGE ( 'NONE', *, *, #30306, .F. ) ;
#47998=DIRECTION ( 'NONE',  ( -1.000000000000000000, 5.626525616968433120E-15, 0.000000000000000000 ) ) ;
#48003=ORIENTED_EDGE ( 'NONE', *, *, #40978, .T. ) ;
#48007=VECTOR ( 'NONE', #48360, 1000.000000000000000 ) ;
#48026=CARTESIAN_POINT ( 'NONE',  ( -5.993516549646799696, -8.211283450353425550, 455.0000000000000568 ) ) ;
#48032=CARTESIAN_POINT ( 'NONE',  ( -11.99351654964674374, -4.186483450353318148, 455.0000000000000568 ) ) ;
#48046=FACE_OUTER_BOUND ( 'NONE', #32198, .T. ) ;
#48049=CIRCLE ( 'NONE', #58192, 0.5999999999999989786 ) ;
#48053=CARTESIAN_POINT ( 'NONE',  ( -1.677516549646683730, 9.828310488885911411, 455.0000000000000568 ) ) ;
#48062=CARTESIAN_POINT ( 'NONE',  ( 9.106483450353380249, -10.92648345035348711, 455.0000000000000568 ) ) ;
#48071=CARTESIAN_POINT ( 'NONE',  ( 4.396432944014577515, 8.593516549646585290, 455.0000000000000568 ) ) ;
#48072=VERTEX_POINT ( 'NONE', #55025 ) ;
#48075=EDGE_CURVE ( 'NONE', #27294, #21746, #49698, .T. ) ;
#48078=ADVANCED_FACE ( 'NONE', ( #28808 ), #62033, .F. ) ;
#48080=CARTESIAN_POINT ( 'NONE',  ( -6.606374702650259501, -7.265214908726163046, 455.0000000000000568 ) ) ;
#48084=EDGE_CURVE ( 'NONE', #11897, #39293, #7599, .T. ) ;
#48087=EDGE_LOOP ( 'NONE', ( #60644, #59161, #38136, #69766 ) ) ;
#48093=ORIENTED_EDGE ( 'NONE', *, *, #1534, .T. ) ;
#48099=ORIENTED_EDGE ( 'NONE', *, *, #17074, .T. ) ;
#48109=VECTOR ( 'NONE', #39450, 1000.000000000000000 ) ;
#48113=ORIENTED_EDGE ( 'NONE', *, *, #52727, .T. ) ;
#48124=LINE ( 'NONE', #38, #13747 ) ;
#48138=ORIENTED_EDGE ( 'NONE', *, *, #24756, .T. ) ;
#48144=VECTOR ( 'NONE', #27693, 1000.000000000000000 ) ;
#48147=EDGE_LOOP ( 'NONE', ( #47047, #39459, #65155, #38861 ) ) ;
#48158=CARTESIAN_POINT ( 'NONE',  ( -4.173516549646666185, 11.99351654964658920, 195.0000000000000284 ) ) ;
#48179=LINE ( 'NONE', #42859, #20686 ) ;
#48184=ORIENTED_EDGE ( 'NONE', *, *, #25749, .F. ) ;
#48185=ORIENTED_EDGE ( 'NONE', *, *, #31040, .T. ) ;
#48196=CARTESIAN_POINT ( 'NONE',  ( -8.393516549646768965, -5.668387132715940524, 455.0000000000000568 ) ) ;
#48197=ORIENTED_EDGE ( 'NONE', *, *, #4359, .T. ) ;
#48211=CARTESIAN_POINT ( 'NONE',  ( -4.393516549646788505, -11.78648345035339418, 195.0000000000000284 ) ) ;
#48214=ORIENTED_EDGE ( 'NONE', *, *, #6233, .T. ) ;
#48219=VECTOR ( 'NONE', #1987, 1000.000000000000000 ) ;
#48221=CARTESIAN_POINT ( 'NONE',  ( 8.406483450353405829, 7.603567055985406498, 455.0000000000000568 ) ) ;
#48232=CARTESIAN_POINT ( 'NONE',  ( -6.331612867284244217, -8.406483450353421816, 455.0000000000000568 ) ) ;
#48233=PLANE ( 'NONE',  #33712 ) ;
#48234=ORIENTED_EDGE ( 'NONE', *, *, #44959, .F. ) ;
#48240=DIRECTION ( 'NONE',  ( -0.000000000000000000, -0.000000000000000000, -1.000000000000000000 ) ) ;
#48264=AXIS2_PLACEMENT_3D ( 'NONE', #21078, #25702, #42989 ) ;
#48276=DIRECTION ( 'NONE',  ( -1.000000000000000000, -2.135044278125301343E-15, -7.844025423732065664E-31 ) ) ;
#48287=LINE ( 'NONE', #64551, #55907 ) ;
#48297=DIRECTION ( 'NONE',  ( 1.836970198721029934E-16, -1.836970198721036344E-16, 1.000000000000000000 ) ) ;
#48307=AXIS2_PLACEMENT_3D ( 'NONE', #37395, #58262, #31406 ) ;
#48308=EDGE_CURVE ( 'NONE', #4905, #10643, #20312, .T. ) ;
#48314=CARTESIAN_POINT ( 'NONE',  ( -7.593516549646711411, 11.31351654964660014, 455.0000000000000568 ) ) ;
#48321=CARTESIAN_POINT ( 'NONE',  ( -4.242044687070550602, 8.452095193409279617, 195.0000000000000284 ) ) ;
#48322=DIRECTION ( 'NONE',  ( 0.7071067811865422437, -0.7071067811865529018, 0.000000000000000000 ) ) ;
#48324=ORIENTED_EDGE ( 'NONE', *, *, #32425, .T. ) ;
#48348=CARTESIAN_POINT ( 'NONE',  ( -11.99351654964669756, -4.186483450353271074, 195.0000000000000284 ) ) ;
#48355=ORIENTED_EDGE ( 'NONE', *, *, #6254, .T. ) ;
#48357=VECTOR ( 'NONE', #17295, 1000.000000000000000 ) ;
#48359=CARTESIAN_POINT ( 'NONE',  ( -11.18071654964676753, -11.19368345035331203, 195.0000000000000284 ) ) ;
#48360=DIRECTION ( 'NONE',  ( -1.836970198721029934E-16, 1.836970198721036344E-16, -1.000000000000000000 ) ) ;
#48365=ORIENTED_EDGE ( 'NONE', *, *, #28665, .T. ) ;
#48372=ORIENTED_EDGE ( 'NONE', *, *, #28113, .F. ) ;
#48373=ORIENTED_EDGE ( 'NONE', *, *, #4546, .F. ) ;
#48375=ORIENTED_EDGE ( 'NONE', *, *, #32693, .T. ) ;
#48381=CARTESIAN_POINT ( 'NONE',  ( 2.906483450353349429, -10.09643294401463365, 455.0000000000000568 ) ) ;
#48389=EDGE_CURVE ( 'NONE', #16263, #52016, #22520, .T. ) ;
#48394=EDGE_LOOP ( 'NONE', ( #1463, #42427, #27736, #45590 ) ) ;
#48396=CARTESIAN_POINT ( 'NONE',  ( 11.32648345035337734, -4.206483450353492692, 455.0000000000000568 ) ) ;
#48397=DIRECTION ( 'NONE',  ( -0.8660254037844375974, 0.5000000000000019984, 1.836970198721037330E-16 ) ) ;
#48398=AXIS2_PLACEMENT_3D ( 'NONE', #60748, #28568, #50140 ) ;
#48405=EDGE_CURVE ( 'NONE', #27698, #41049, #37634, .T. ) ;
#48414=EDGE_CURVE ( 'NONE', #705, #57915, #10406, .T. ) ;
#48426=DIRECTION ( 'NONE',  ( -0.000000000000000000, -0.000000000000000000, -1.000000000000000000 ) ) ;
#48437=CARTESIAN_POINT ( 'NONE',  ( 5.668387132715968058, 8.393516549646582448, 455.0000000000000568 ) ) ;
#48444=ORIENTED_EDGE ( 'NONE', *, *, #23078, .T. ) ;
#48453=AXIS2_PLACEMENT_3D ( 'NONE', #7137, #38647, #55253 ) ;
#48462=ORIENTED_EDGE ( 'NONE', *, *, #59332, .F. ) ;
#48473=LINE ( 'NONE', #4646, #22642 ) ;
#48477=DIRECTION ( 'NONE',  ( 0.000000000000000000, 1.000000000000000000, 0.000000000000000000 ) ) ;
#48481=EDGE_CURVE ( 'NONE', #33646, #64293, #39347, .T. ) ;
#48484=ORIENTED_EDGE ( 'NONE', *, *, #31491, .T. ) ;
#48485=CARTESIAN_POINT ( 'NONE',  ( 9.804883450353379715, -10.20488345035352928, 455.0000000000000568 ) ) ;
#48487=VERTEX_POINT ( 'NONE', #17430 ) ;
#48488=CARTESIAN_POINT ( 'NONE',  ( -5.655420232009250370, 8.393516549646600211, 455.0000000000000568 ) ) ;
#48489=ORIENTED_EDGE ( 'NONE', *, *, #10872, .F. ) ;
#48491=DIRECTION ( 'NONE',  ( -0.000000000000000000, -0.000000000000000000, -1.000000000000000000 ) ) ;
#48497=FACE_OUTER_BOUND ( 'NONE', #67034, .T. ) ;
#48498=LINE ( 'NONE', #28302, #56351 ) ;
#48501=CIRCLE ( 'NONE', #17987, 0.2000000000000005107 ) ;
#48514=DIRECTION ( 'NONE',  ( -0.000000000000000000, -0.000000000000000000, -1.000000000000000000 ) ) ;
#48517=EDGE_CURVE ( 'NONE', #56963, #28943, #20343, .T. ) ;
#48518=DIRECTION ( 'NONE',  ( -1.000000000000000000, 0.000000000000000000, 0.000000000000000000 ) ) ;
#48520=DIRECTION ( 'NONE',  ( 1.047444401652940007E-14, 1.000000000000000000, 1.836970198721029934E-16 ) ) ;
#48524=LINE ( 'NONE', #59826, #30960 ) ;
#48525=CYLINDRICAL_SURFACE ( 'NONE', #9755, 0.1999999999999987899 ) ;
#48526=EDGE_LOOP ( 'NONE', ( #68007, #20208, #14436, #33223 ) ) ;
#48527=CARTESIAN_POINT ( 'NONE',  ( -7.813516549646711162, 11.99351654964660341, 455.0000000000000568 ) ) ;
#48538=ORIENTED_EDGE ( 'NONE', *, *, #37157, .T. ) ;
#48542=VERTEX_POINT ( 'NONE', #35076 ) ;
#48546=AXIS2_PLACEMENT_3D ( 'NONE', #12483, #50324, #18141 ) ;
#48554=VERTEX_POINT ( 'NONE', #18828 ) ;
#48562=DIRECTION ( 'NONE',  ( -0.8660254037844363761, 0.5000000000000038858, -0.000000000000000000 ) ) ;
#48567=VECTOR ( 'NONE', #67664, 1000.000000000000000 ) ;
#48569=FACE_BOUND ( 'NONE', #267, .T. ) ;
#48590=VERTEX_POINT ( 'NONE', #29088 ) ;
#48591=LINE ( 'NONE', #160, #32191 ) ;
#48594=CARTESIAN_POINT ( 'NONE',  ( 6.006483450353401921, 5.993516549646582092, 455.0000000000000568 ) ) ;
#48598=VERTEX_POINT ( 'NONE', #50651 ) ;
#48600=DIRECTION ( 'NONE',  ( 1.000000000000000000, -1.356437060717831815E-15, -1.836970198721032646E-16 ) ) ;
#48601=DIRECTION ( 'NONE',  ( -0.4999999999999785727, 0.8660254037844510311, 3.181725716174766844E-16 ) ) ;
#48606=EDGE_CURVE ( 'NONE', #45353, #65774, #63371, .T. ) ;
#48616=CARTESIAN_POINT ( 'NONE',  ( -4.173516549646839380, -12.00648345035344811, 455.0000000000000568 ) ) ;
#48618=ORIENTED_EDGE ( 'NONE', *, *, #33765, .T. ) ;
#48621=FACE_OUTER_BOUND ( 'NONE', #18263, .T. ) ;
#48625=EDGE_LOOP ( 'NONE', ( #30817, #3974, #56191, #55455 ) ) ;
#48633=CIRCLE ( 'NONE', #67801, 0.5999999999999989786 ) ;
#48639=AXIS2_PLACEMENT_3D ( 'NONE', #1931, #23497, #44696 ) ;
#48642=EDGE_CURVE ( 'NONE', #11897, #30360, #12392, .T. ) ;
#48662=EDGE_CURVE ( 'NONE', #44153, #41828, #68318, .T. ) ;
#48671=CARTESIAN_POINT ( 'NONE',  ( -2.693516549646772340, -10.09643294401458036, 195.0000000000000284 ) ) ;
#48676=DIRECTION ( 'NONE',  ( 1.000000000000000000, -3.016910393003147986E-15, 0.000000000000000000 ) ) ;
#48677=ORIENTED_EDGE ( 'NONE', *, *, #28920, .T. ) ;
#48678=VERTEX_POINT ( 'NONE', #9628 ) ;
#48680=VECTOR ( 'NONE', #53682, 1000.000000000000000 ) ;
#48683=DIRECTION ( 'NONE',  ( -0.000000000000000000, -0.000000000000000000, -1.000000000000000000 ) ) ;
#48685=VERTEX_POINT ( 'NONE', #31553 ) ;
#48690=FACE_OUTER_BOUND ( 'NONE', #68329, .T. ) ;
#48692=VERTEX_POINT ( 'NONE', #62303 ) ;
#48695=DIRECTION ( 'NONE',  ( 1.000000000000000000, -7.457533623526253657E-15, 1.836970198721016375E-16 ) ) ;
#48699=VECTOR ( 'NONE', #12972, 999.9999999999998863 ) ;
#48703=EDGE_CURVE ( 'NONE', #3786, #7925, #46272, .T. ) ;
#48710=DIRECTION ( 'NONE',  ( -0.000000000000000000, 1.000000000000000000, -0.000000000000000000 ) ) ;
#48718=AXIS2_PLACEMENT_3D ( 'NONE', #38315, #59871, #11425 ) ;
#48720=EDGE_CURVE ( 'NONE', #51749, #4323, #52785, .T. ) ;
#48721=VERTEX_POINT ( 'NONE', #3973 ) ;
#48722=CARTESIAN_POINT ( 'NONE',  ( -11.47551654964667733, 10.19191654964664018, 455.0000000000000568 ) ) ;
#48723=CARTESIAN_POINT ( 'NONE',  ( 4.740315990920129785, -4.201500623656146516, 455.0000000000000568 ) ) ;
#48728=EDGE_CURVE ( 'NONE', #24032, #11040, #14690, .T. ) ;
#48733=CARTESIAN_POINT ( 'NONE',  ( 7.428221114744945730, 2.993516549646613623, 195.0000000000000284 ) ) ;
#48739=EDGE_LOOP ( 'NONE', ( #57200, #50704, #57759, #39346 ) ) ;
#48741=DIRECTION ( 'NONE',  ( 1.000000000000000000, -1.185108578570163244E-14, 0.000000000000000000 ) ) ;
#48753=EDGE_LOOP ( 'NONE', ( #22783, #43514, #43520, #19948 ) ) ;
#48755=LINE ( 'NONE', #10230, #67874 ) ;
#48757=DIRECTION ( 'NONE',  ( 0.000000000000000000, -1.000000000000000000, 0.000000000000000000 ) ) ;
#48760=CARTESIAN_POINT ( 'NONE',  ( -6.331612867284244217, -8.406483450353421816, 455.0000000000000568 ) ) ;
#48761=LINE ( 'NONE', #38826, #41112 ) ;
#48762=LINE ( 'NONE', #322, #59862 ) ;
#48772=CIRCLE ( 'NONE', #53326, 0.1999999999999996503 ) ;
#48773=EDGE_CURVE ( 'NONE', #20589, #57392, #37206, .T. ) ;
#48774=DIRECTION ( 'NONE',  ( 1.836970198721029934E-16, 1.836970198721010706E-16, -1.000000000000000000 ) ) ;
#48779=ORIENTED_EDGE ( 'NONE', *, *, #14246, .T. ) ;
#48787=ORIENTED_EDGE ( 'NONE', *, *, #66524, .F. ) ;
#48797=VECTOR ( 'NONE', #28214, 1000.000000000000000 ) ;
#48798=ORIENTED_EDGE ( 'NONE', *, *, #35071, .F. ) ;
#48802=EDGE_LOOP ( 'NONE', ( #18383, #69144, #41010, #785 ) ) ;
#48806=DIRECTION ( 'NONE',  ( -0.000000000000000000, -0.000000000000000000, -1.000000000000000000 ) ) ;
#48812=ORIENTED_EDGE ( 'NONE', *, *, #65655, .T. ) ;
#48814=DIRECTION ( 'NONE',  ( 1.836970198721029934E-16, 1.836970198721010706E-16, -1.000000000000000000 ) ) ;
#48820=DIRECTION ( 'NONE',  ( 8.540177112501197482E-15, 1.000000000000000000, -0.000000000000000000 ) ) ;
#48838=CARTESIAN_POINT ( 'NONE',  ( -11.77351654964679284, -7.826483450353365789, 455.0000000000000568 ) ) ;
#48850=DIRECTION ( 'NONE',  ( -0.7071067811865391350, 0.7071067811865560104, 1.750285133459120294E-30 ) ) ;
#48853=CIRCLE ( 'NONE', #18326, 2.204799999999999205 ) ;
#48864=ORIENTED_EDGE ( 'NONE', *, *, #43149, .T. ) ;
#48865=CARTESIAN_POINT ( 'NONE',  ( -11.11351654964670921, 8.693516549646615132, 455.0000000000000568 ) ) ;
#48868=ADVANCED_FACE ( 'NONE', ( #22668 ), #13438, .F. ) ;
#48869=DIRECTION ( 'NONE',  ( 0.000000000000000000, 3.673940397442059868E-16, -1.000000000000000000 ) ) ;
#48872=CARTESIAN_POINT ( 'NONE',  ( -11.77351654964670935, 7.593516549646604830, 195.0000000000000284 ) ) ;
#48877=DIRECTION ( 'NONE',  ( 0.000000000000000000, 1.000000000000000000, 0.000000000000000000 ) ) ;
#48880=ADVANCED_FACE ( 'NONE', ( #12373 ), #45255, .F. ) ;
#48885=LINE ( 'NONE', #20134, #66053 ) ;
#48889=DIRECTION ( 'NONE',  ( 1.836970198721029934E-16, 1.836970198721010706E-16, -1.000000000000000000 ) ) ;
#48890=VECTOR ( 'NONE', #52021, 1000.000000000000000 ) ;
#48895=DIRECTION ( 'NONE',  ( 1.000000000000000000, -5.626525616968433909E-15, -1.836970198721040534E-16 ) ) ;
#48898=EDGE_LOOP ( 'NONE', ( #7777, #69136, #2959, #63564 ) ) ;
#48904=ORIENTED_EDGE ( 'NONE', *, *, #64668, .F. ) ;
#48905=CARTESIAN_POINT ( 'NONE',  ( 1.690483450353418737, 10.73351654964659652, 455.0000000000000568 ) ) ;
#48910=LINE ( 'NONE', #5077, #22477 ) ;
#48911=LINE ( 'NONE', #65182, #8614 ) ;
#48912=CARTESIAN_POINT ( 'NONE',  ( -11.11351654964668612, 8.693516549646636449, 194.9999952000000292 ) ) ;
#48915=ADVANCED_FACE ( 'NONE', ( #27976 ), #61167, .F. ) ;
#48916=ORIENTED_EDGE ( 'NONE', *, *, #25349, .T. ) ;
#48917=LINE ( 'NONE', #64487, #37159 ) ;
#48920=DIRECTION ( 'NONE',  ( 0.7071067811865500152, 0.7071067811865451302, -4.683861624749757595E-31 ) ) ;
#48928=LINE ( 'NONE', #5094, #66420 ) ;
#48931=FACE_OUTER_BOUND ( 'NONE', #13182, .T. ) ;
#48936=LINE ( 'NONE', #32667, #2691 ) ;
#48940=ORIENTED_EDGE ( 'NONE', *, *, #45807, .T. ) ;
#48941=CARTESIAN_POINT ( 'NONE',  ( -10.73351654964671020, 1.677516549646604016, 195.0000000000000284 ) ) ;
#48945=FACE_OUTER_BOUND ( 'NONE', #62067, .T. ) ;
#48947=EDGE_LOOP ( 'NONE', ( #1374, #22360, #62141, #63487 ) ) ;
#48950=EDGE_CURVE ( 'NONE', #51945, #51749, #37167, .T. ) ;
#48951=CARTESIAN_POINT ( 'NONE',  ( 11.12648345035340647, 7.793516549646564151, 455.0000000000000568 ) ) ;
#48955=VECTOR ( 'NONE', #17977, 1000.000000000000000 ) ;
#48956=EDGE_CURVE ( 'NONE', #3545, #65838, #17348, .T. ) ;
#48957=FACE_OUTER_BOUND ( 'NONE', #22785, .T. ) ;
#48961=VERTEX_POINT ( 'NONE', #23360 ) ;
#48971=EDGE_LOOP ( 'NONE', ( #55048, #63415, #48113, #41836 ) ) ;
#48993=DIRECTION ( 'NONE',  ( 1.000000000000000000, -8.728482790395504563E-15, -3.206792553201184024E-30 ) ) ;
#49003=DIRECTION ( 'NONE',  ( -1.836970198721029934E-16, 1.836970198721036344E-16, -1.000000000000000000 ) ) ;
#49014=DIRECTION ( 'NONE',  ( 0.000000000000000000, 1.000000000000000000, 3.673940397442059868E-16 ) ) ;
#49023=DIRECTION ( 'NONE',  ( 1.000000000000000000, 2.135044278125299371E-15, 7.844025423732059533E-31 ) ) ;
#49030=CARTESIAN_POINT ( 'NONE',  ( 3.006483450353407250, 7.415254214038215608, 455.0000000000000568 ) ) ;
#49047=VECTOR ( 'NONE', #24917, 1000.000000000000000 ) ;
#49051=ORIENTED_EDGE ( 'NONE', *, *, #32419, .T. ) ;
#49052=AXIS2_PLACEMENT_3D ( 'NONE', #39179, #55447, #67453 ) ;
#49054=VERTEX_POINT ( 'NONE', #8472 ) ;
#49056=DIRECTION ( 'NONE',  ( -1.836970198721029934E-16, 1.836970198721036344E-16, -1.000000000000000000 ) ) ;
#49057=ORIENTED_EDGE ( 'NONE', *, *, #10519, .F. ) ;
#49063=VECTOR ( 'NONE', #51419, 1000.000000000000000 ) ;
#49068=DIRECTION ( 'NONE',  ( -1.836970198721029934E-16, -1.836970198721010706E-16, 1.000000000000000000 ) ) ;
#49069=PLANE ( 'NONE',  #38059 ) ;
#49076=DIRECTION ( 'NONE',  ( 1.836970198721029934E-16, 1.836970198721010706E-16, -1.000000000000000000 ) ) ;
#49079=EDGE_CURVE ( 'NONE', #52737, #60571, #14498, .T. ) ;
#49084=PLANE ( 'NONE',  #66178 ) ;
#49091=CARTESIAN_POINT ( 'NONE',  ( 10.74648345035337904, -1.690483450353491124, 455.0000000000000568 ) ) ;
#49097=DIRECTION ( 'NONE',  ( -1.836970198721029934E-16, 1.836970198721036344E-16, -1.000000000000000000 ) ) ;
#49103=DIRECTION ( 'NONE',  ( -0.000000000000000000, -0.000000000000000000, -1.000000000000000000 ) ) ;
#49108=DIRECTION ( 'NONE',  ( 0.000000000000000000, 0.000000000000000000, 1.000000000000000000 ) ) ;
#49114=CIRCLE ( 'NONE', #26511, 1.399999999999998579 ) ;
#49117=ORIENTED_EDGE ( 'NONE', *, *, #20670, .T. ) ;
#49127=VECTOR ( 'NONE', #22033, 1000.000000000000000 ) ;
#49134=ORIENTED_EDGE ( 'NONE', *, *, #15677, .T. ) ;
#49135=ORIENTED_EDGE ( 'NONE', *, *, #31560, .T. ) ;
#49143=CIRCLE ( 'NONE', #63233, 0.5999999999999989786 ) ;
#49146=ORIENTED_EDGE ( 'NONE', *, *, #9658, .F. ) ;
#49150=CIRCLE ( 'NONE', #66034, 0.2000000000000000944 ) ;
#49151=ORIENTED_EDGE ( 'NONE', *, *, #15280, .T. ) ;
#49160=ADVANCED_FACE ( 'NONE', ( #51142 ), #12254, .F. ) ;
#49161=DIRECTION ( 'NONE',  ( 1.000000000000000000, 0.000000000000000000, -0.000000000000000000 ) ) ;
#49179=LINE ( 'NONE', #66468, #61493 ) ;
#49182=CARTESIAN_POINT ( 'NONE',  ( -8.693516549646709279, 11.11351654964659907, 455.0000000000000568 ) ) ;
#49193=CARTESIAN_POINT ( 'NONE',  ( 9.306483450353415066, 10.08346604330773744, 455.0000000000000568 ) ) ;
#49194=CARTESIAN_POINT ( 'NONE',  ( 3.006483450353369502, -7.428221114745093168, 455.0000000000000568 ) ) ;
#49200=EDGE_CURVE ( 'NONE', #21581, #56475, #39822, .T. ) ;
#49201=DIRECTION ( 'NONE',  ( -1.000000000000000000, 1.813998472013049822E-14, -1.836970198720996654E-16 ) ) ;
#49203=EDGE_CURVE ( 'NONE', #42601, #48598, #55753, .T. ) ;
#49206=CARTESIAN_POINT ( 'NONE',  ( 11.12648345035335851, 7.793516549646610336, 195.0000000000000284 ) ) ;
#49207=VECTOR ( 'NONE', #60995, 1000.000000000000000 ) ;
#49209=EDGE_LOOP ( 'NONE', ( #23726, #54946, #11948, #33562 ) ) ;
#49212=VERTEX_POINT ( 'NONE', #1323 ) ;
#49214=ORIENTED_EDGE ( 'NONE', *, *, #56331, .T. ) ;
#49215=AXIS2_PLACEMENT_3D ( 'NONE', #46100, #25946, #10028 ) ;
#49218=LINE ( 'NONE', #12058, #63128 ) ;
#49221=DIRECTION ( 'NONE',  ( 1.836970198721029934E-16, -1.836970198721036344E-16, 1.000000000000000000 ) ) ;
#49228=CARTESIAN_POINT ( 'NONE',  ( -4.383466043307859827, 8.393516549646591329, 455.0000000000000568 ) ) ;
#49236=EDGE_CURVE ( 'NONE', #5474, #7017, #27057, .T. ) ;
#49240=DIRECTION ( 'NONE',  ( 1.836970198721029934E-16, 1.836970198721010706E-16, -1.000000000000000000 ) ) ;
#49242=ORIENTED_EDGE ( 'NONE', *, *, #61402, .T. ) ;
#49245=CARTESIAN_POINT ( 'NONE',  ( -4.393516549646671265, 11.31351654964658771, 455.0000000000000568 ) ) ;
#49246=ORIENTED_EDGE ( 'NONE', *, *, #56515, .T. ) ;
#49255=ORIENTED_EDGE ( 'NONE', *, *, #6572, .T. ) ;
#49257=LINE ( 'NONE', #21337, #39101 ) ;
#49273=LINE ( 'NONE', #11422, #36896 ) ;
#49276=CYLINDRICAL_SURFACE ( 'NONE', #26168, 0.1999999999999987899 ) ;
#49292=EDGE_LOOP ( 'NONE', ( #49926, #29247, #55846, #38137 ) ) ;
#49294=CARTESIAN_POINT ( 'NONE',  ( -4.734785091273957747, 6.606374702650051667, 195.0000000000000284 ) ) ;
#49299=EDGE_CURVE ( 'NONE', #5817, #25935, #22513, .T. ) ;
#49306=CARTESIAN_POINT ( 'NONE',  ( 6.344579767990823349, -8.406483450353491094, 455.0000000000000568 ) ) ;
#49311=DIRECTION ( 'NONE',  ( 1.000000000000000000, -3.491481338843132961E-15, -1.836970198721036344E-16 ) ) ;
#49313=CIRCLE ( 'NONE', #33490, 0.5999999999999989786 ) ;
#49314=VERTEX_POINT ( 'NONE', #68814 ) ;
#49318=LINE ( 'NONE', #49980, #2770 ) ;
#49326=ORIENTED_EDGE ( 'NONE', *, *, #18988, .T. ) ;
#49329=CARTESIAN_POINT ( 'NONE',  ( -8.393516549646792058, -7.616533956692236096, 455.0000000000000568 ) ) ;
#49331=ORIENTED_EDGE ( 'NONE', *, *, #69892, .F. ) ;
#49337=CARTESIAN_POINT ( 'NONE',  ( -3.417780618358722933, -7.852485183457003970, 455.0000000000000568 ) ) ;
#49356=AXIS2_PLACEMENT_3D ( 'NONE', #42720, #64300, #58299 ) ;
#49357=DIRECTION ( 'NONE',  ( 0.000000000000000000, 1.000000000000000000, 0.000000000000000000 ) ) ;
#49360=AXIS2_PLACEMENT_3D ( 'NONE', #31794, #20127, #46638 ) ;
#49363=EDGE_CURVE ( 'NONE', #18151, #41573, #15072, .T. ) ;
#49364=DIRECTION ( 'NONE',  ( 1.000000000000000000, -8.728482790395504563E-15, -3.206792553201184024E-30 ) ) ;
#49375=AXIS2_PLACEMENT_3D ( 'NONE', #26046, #5176, #10125 ) ;
#49381=LINE ( 'NONE', #11862, #22600 ) ;
#49383=AXIS2_PLACEMENT_3D ( 'NONE', #4212, #57930, #21500 ) ;
#49390=ORIENTED_EDGE ( 'NONE', *, *, #45949, .T. ) ;
#49404=EDGE_LOOP ( 'NONE', ( #57138, #65086, #42105, #2559 ) ) ;
#49405=EDGE_CURVE ( 'NONE', #62698, #46179, #17996, .T. ) ;
#49406=CARTESIAN_POINT ( 'NONE',  ( -10.08346604330783336, -2.706483450353306175, 195.0000000000000284 ) ) ;
#49410=ORIENTED_EDGE ( 'NONE', *, *, #42234, .F. ) ;
#49420=ORIENTED_EDGE ( 'NONE', *, *, #40759, .F. ) ;
#49424=VECTOR ( 'NONE', #41993, 1000.000000000000000 ) ;
#49434=ORIENTED_EDGE ( 'NONE', *, *, #42634, .T. ) ;
#49441=VERTEX_POINT ( 'NONE', #7133 ) ;
#49443=EDGE_CURVE ( 'NONE', #29674, #43112, #55591, .T. ) ;
#49462=LINE ( 'NONE', #6320, #12794 ) ;
#49464=DIRECTION ( 'NONE',  ( -1.000000000000000000, -3.016910393003147986E-15, -0.000000000000000000 ) ) ;
#49478=DIRECTION ( 'NONE',  ( -1.000000000000000000, -2.135044278125301343E-15, 0.000000000000000000 ) ) ;
#49485=CARTESIAN_POINT ( 'NONE',  ( -7.252248008019532399, -6.619341603356871495, 455.0000000000000568 ) ) ;
#49491=FACE_OUTER_BOUND ( 'NONE', #48753, .T. ) ;
#49492=CARTESIAN_POINT ( 'NONE',  ( 8.606483450353380249, -7.616533956692230767, 195.0000000000000284 ) ) ;
#49497=CARTESIAN_POINT ( 'NONE',  ( -9.293516549646827940, -10.92648345035338764, 455.0000000000000568 ) ) ;
#49511=VECTOR ( 'NONE', #51595, 1000.000000000000000 ) ;
#49518=DIRECTION ( 'NONE',  ( 0.000000000000000000, 0.000000000000000000, -1.000000000000000000 ) ) ;
#49519=ADVANCED_FACE ( 'NONE', ( #69511 ), #60878, .F. ) ;
#49520=CARTESIAN_POINT ( 'NONE',  ( -11.99351654964671354, 7.813516549646603693, 455.0000000000000568 ) ) ;
#49523=ORIENTED_EDGE ( 'NONE', *, *, #49679, .T. ) ;
#49529=ORIENTED_EDGE ( 'NONE', *, *, #11056, .T. ) ;
#49531=DIRECTION ( 'NONE',  ( -1.000000000000000000, 0.000000000000000000, 0.000000000000000000 ) ) ;
#49538=CARTESIAN_POINT ( 'NONE',  ( -10.91351654964680584, -9.306483450353375986, 455.0000000000000568 ) ) ;
#49542=ORIENTED_EDGE ( 'NONE', *, *, #14074, .T. ) ;
#49544=PLANE ( 'NONE',  #3317 ) ;
#49554=DIRECTION ( 'NONE',  ( 0.000000000000000000, 1.000000000000000000, 0.000000000000000000 ) ) ;
#49556=CARTESIAN_POINT ( 'NONE',  ( 7.826483450353374671, 11.77351654964661876, 195.0000000000000284 ) ) ;
#49560=CARTESIAN_POINT ( 'NONE',  ( -9.404046420174113408, -1.866219381641437636, 455.0000000000000568 ) ) ;
#49572=ORIENTED_EDGE ( 'NONE', *, *, #38021, .F. ) ;
#49587=VERTEX_POINT ( 'NONE', #35876 ) ;
#49593=DIRECTION ( 'NONE',  ( -1.000000000000000000, 0.000000000000000000, 0.000000000000000000 ) ) ;
#49598=VECTOR ( 'NONE', #68336, 1000.000000000000000 ) ;
#49599=LINE ( 'NONE', #26385, #35576 ) ;
#49606=CIRCLE ( 'NONE', #14576, 0.2000000000000005107 ) ;
#49618=VERTEX_POINT ( 'NONE', #47873 ) ;
#49626=PLANE ( 'NONE',  #61647 ) ;
#49632=DIRECTION ( 'NONE',  ( 1.836970198721029934E-16, -1.836970198721036344E-16, 1.000000000000000000 ) ) ;
#49639=ORIENTED_EDGE ( 'NONE', *, *, #67556, .T. ) ;
#49640=EDGE_CURVE ( 'NONE', #62095, #41426, #9713, .T. ) ;
#49641=VERTEX_POINT ( 'NONE', #15009 ) ;
#49642=LINE ( 'NONE', #11462, #3952 ) ;
#49643=CARTESIAN_POINT ( 'NONE',  ( 6.006483450353379716, -4.606483450353492159, 455.0000000000000568 ) ) ;
#49646=CYLINDRICAL_SURFACE ( 'NONE', #51865, 0.1999999999999987899 ) ;
#49650=ADVANCED_FACE ( 'NONE', ( #43528 ), #69101, .F. ) ;
#49652=PLANE ( 'NONE',  #38475 ) ;
#49653=ORIENTED_EDGE ( 'NONE', *, *, #27489, .F. ) ;
#49668=ORIENTED_EDGE ( 'NONE', *, *, #7258, .T. ) ;
#49670=VECTOR ( 'NONE', #20986, 999.9999999999998863 ) ;
#49671=ADVANCED_FACE ( 'NONE', ( #55187 ), #23687, .F. ) ;
#49672=CARTESIAN_POINT ( 'NONE',  ( -7.593516549646791347, -11.78648345035336042, 195.0000000000000284 ) ) ;
#49675=FACE_OUTER_BOUND ( 'NONE', #19465, .T. ) ;
#49679=EDGE_CURVE ( 'NONE', #10422, #3591, #1101, .T. ) ;
#49683=EDGE_LOOP ( 'NONE', ( #69072, #5052, #55924, #57203 ) ) ;
#49691=VECTOR ( 'NONE', #6156, 999.9999999999998863 ) ;
#49693=AXIS2_PLACEMENT_3D ( 'NONE', #41283, #68868, #47998 ) ;
#49698=LINE ( 'NONE', #26752, #53021 ) ;
#49700=AXIS2_PLACEMENT_3D ( 'NONE', #11243, #44802, #27180 ) ;
#49707=CIRCLE ( 'NONE', #63239, 0.2000000000000005107 ) ;
#49709=DIRECTION ( 'NONE',  ( -0.7071067811865475727, 0.7071067811865475727, 2.597868168706480597E-16 ) ) ;
#49714=CARTESIAN_POINT ( 'NONE',  ( -8.452095193409434160, -4.255011587777239868, 455.0000000000000568 ) ) ;
#49718=CARTESIAN_POINT ( 'NONE',  ( -8.393516549646792058, -7.616533956692236096, 455.0000000000000568 ) ) ;
#49724=VERTEX_POINT ( 'NONE', #17013 ) ;
#49727=DIRECTION ( 'NONE',  ( -0.7671651518153006499, 0.6414496315691565753, -0.000000000000000000 ) ) ;
#49740=DIRECTION ( 'NONE',  ( -0.000000000000000000, -0.000000000000000000, -1.000000000000000000 ) ) ;
#49744=DIRECTION ( 'NONE',  ( 0.7671651518153087546, 0.6414496315691468054, 0.000000000000000000 ) ) ;
#49749=ORIENTED_EDGE ( 'NONE', *, *, #5489, .F. ) ;
#49753=VECTOR ( 'NONE', #6587, 1000.000000000000227 ) ;
#49754=EDGE_CURVE ( 'NONE', #58797, #15862, #54509, .T. ) ;
#49757=DIRECTION ( 'NONE',  ( -0.6414496315691645689, -0.7671651518152939886, -2.587583378555115478E-16 ) ) ;
#49763=ORIENTED_EDGE ( 'NONE', *, *, #26934, .F. ) ;
#49768=DIRECTION ( 'NONE',  ( 1.836970198721029934E-16, 1.836970198721010706E-16, -1.000000000000000000 ) ) ;
#49771=DIRECTION ( 'NONE',  ( -0.000000000000000000, 3.673940397442059868E-16, -1.000000000000000000 ) ) ;
#49773=EDGE_CURVE ( 'NONE', #42528, #14259, #38586, .T. ) ;
#49787=LINE ( 'NONE', #45510, #15418 ) ;
#49799=LINE ( 'NONE', #11273, #17848 ) ;
#49802=DIRECTION ( 'NONE',  ( -1.000000000000000000, 1.047444401652939849E-14, 0.000000000000000000 ) ) ;
#49809=ORIENTED_EDGE ( 'NONE', *, *, #49828, .T. ) ;
#49828=EDGE_CURVE ( 'NONE', #23630, #6256, #14493, .T. ) ;
#49832=AXIS2_PLACEMENT_3D ( 'NONE', #7986, #19303, #62797 ) ;
#49835=CARTESIAN_POINT ( 'NONE',  ( 9.106483450353380249, -10.09643294401456259, 195.0000000000000284 ) ) ;
#49841=ORIENTED_EDGE ( 'NONE', *, *, #25001, .T. ) ;
#49845=DIRECTION ( 'NONE',  ( -1.000000000000000000, 0.000000000000000000, 0.000000000000000000 ) ) ;
#49855=CARTESIAN_POINT ( 'NONE',  ( -11.77351654964670935, 4.173516549646604901, 455.0000000000000568 ) ) ;
#49856=LINE ( 'NONE', #64739, #66525 ) ;
#49858=CARTESIAN_POINT ( 'NONE',  ( 7.265214908726123078, -5.393625297350022052, 455.0000000000000568 ) ) ;
#49865=DIRECTION ( 'NONE',  ( -4.336808689942025625E-15, -1.000000000000000000, 0.000000000000000000 ) ) ;
#49867=VECTOR ( 'NONE', #2205, 1000.000000000000000 ) ;
#49871=ADVANCED_FACE ( 'NONE', ( #34648 ), #8831, .F. ) ;
#49875=LINE ( 'NONE', #22332, #11087 ) ;
#49882=ORIENTED_EDGE ( 'NONE', *, *, #58265, .F. ) ;
#49887=ORIENTED_EDGE ( 'NONE', *, *, #42572, .F. ) ;
#49896=DIRECTION ( 'NONE',  ( 1.836970198721029934E-16, 1.836970198721010706E-16, -1.000000000000000000 ) ) ;
#49902=EDGE_LOOP ( 'NONE', ( #7189, #11082, #22346, #57451 ) ) ;
#49907=LINE ( 'NONE', #13467, #8401 ) ;
#49911=EDGE_LOOP ( 'NONE', ( #47429, #4388, #36679, #36178, #67707, #6719, #53361, #45520 ) ) ;
#49919=DIRECTION ( 'NONE',  ( -0.7071067811865348052, 0.7071067811865602293, 0.000000000000000000 ) ) ;
#49920=CARTESIAN_POINT ( 'NONE',  ( -11.99351654964671354, 7.813516549646603693, 455.0000000000000568 ) ) ;
#49923=DIRECTION ( 'NONE',  ( -1.000000000000000000, 6.308085367188446447E-15, 0.000000000000000000 ) ) ;
#49926=ORIENTED_EDGE ( 'NONE', *, *, #9379, .T. ) ;
#49930=AXIS2_PLACEMENT_3D ( 'NONE', #32788, #54369, #49744 ) ;
#49936=PLANE ( 'NONE',  #32658 ) ;
#49939=LINE ( 'NONE', #11760, #11797 ) ;
#49940=PLANE ( 'NONE',  #47020 ) ;
#49941=DIRECTION ( 'NONE',  ( -0.000000000000000000, -0.000000000000000000, -1.000000000000000000 ) ) ;
#49961=DIRECTION ( 'NONE',  ( -0.000000000000000000, -0.000000000000000000, -1.000000000000000000 ) ) ;
#49968=DIRECTION ( 'NONE',  ( 1.349135440953254805E-14, 1.000000000000000000, 1.836970198721035604E-16 ) ) ;
#49970=LINE ( 'NONE', #5819, #32734 ) ;
#49973=ORIENTED_EDGE ( 'NONE', *, *, #17074, .F. ) ;
#49977=ORIENTED_EDGE ( 'NONE', *, *, #14626, .T. ) ;
#49979=VERTEX_POINT ( 'NONE', #30047 ) ;
#49980=CARTESIAN_POINT ( 'NONE',  ( 8.406483450353379183, -6.344579767990935260, 455.0000000000000568 ) ) ;
#49985=EDGE_CURVE ( 'NONE', #26484, #48487, #25451, .T. ) ;
#49990=ORIENTED_EDGE ( 'NONE', *, *, #22843, .F. ) ;
#49995=ORIENTED_EDGE ( 'NONE', *, *, #67796, .T. ) ;
#50011=CARTESIAN_POINT ( 'NONE',  ( -7.813516549646711162, 11.99351654964660341, 455.0000000000000568 ) ) ;
#50021=ORIENTED_EDGE ( 'NONE', *, *, #60355, .T. ) ;
#50024=CARTESIAN_POINT ( 'NONE',  ( 4.255011587777218551, -8.465062094116072799, 195.0000000000000284 ) ) ;
#50031=CARTESIAN_POINT ( 'NONE',  ( -9.791916549646867196, -11.08848345035335115, 455.0000000000000568 ) ) ;
#50047=DIRECTION ( 'NONE',  ( 1.000000000000000000, -1.047444401652940007E-14, 1.836970198721010706E-16 ) ) ;
#50051=DIRECTION ( 'NONE',  ( -1.836970198721029934E-16, 1.836970198721036344E-16, -1.000000000000000000 ) ) ;
#50057=DIRECTION ( 'NONE',  ( -0.7671651518152939886, 0.6414496315691645689, 0.000000000000000000 ) ) ;
#50058=AXIS2_PLACEMENT_3D ( 'NONE', #10362, #52448, #53164 ) ;
#50074=ORIENTED_EDGE ( 'NONE', *, *, #55932, .F. ) ;
#50108=DIRECTION ( 'NONE',  ( 0.000000000000000000, 1.000000000000000000, 0.000000000000000000 ) ) ;
#50119=DIRECTION ( 'NONE',  ( 1.836970198721029934E-16, 1.836970198721010706E-16, -1.000000000000000000 ) ) ;
#50122=LINE ( 'NONE', #39172, #48797 ) ;
#50128=DIRECTION ( 'NONE',  ( -1.000000000000000000, 0.000000000000000000, 0.000000000000000000 ) ) ;
#50129=CARTESIAN_POINT ( 'NONE',  ( 8.406483450353384512, 4.383466043307721272, 455.0000000000000568 ) ) ;
#50131=CARTESIAN_POINT ( 'NONE',  ( 9.247904806590689475, -9.955011587777253368, 195.0000000000000284 ) ) ;
#50139=CIRCLE ( 'NONE', #30975, 0.3999999999999993006 ) ;
#50140=DIRECTION ( 'NONE',  ( -1.000000000000000000, 0.000000000000000000, 0.000000000000000000 ) ) ;
#50143=DIRECTION ( 'NONE',  ( -0.5000000000000129896, -0.8660254037844311581, -2.509347957447868930E-16 ) ) ;
#50151=DIRECTION ( 'NONE',  ( -0.6414496315691420314, 0.7671651518153128624, 2.587583378555127804E-16 ) ) ;
#50162=DIRECTION ( 'NONE',  ( -1.000000000000000000, 1.260948829465470062E-14, -1.836970198721007008E-16 ) ) ;
#50169=ORIENTED_EDGE ( 'NONE', *, *, #38441, .F. ) ;
#50170=EDGE_CURVE ( 'NONE', #26479, #3872, #27200, .T. ) ;
#50171=CARTESIAN_POINT ( 'NONE',  ( -2.893516549646673930, 11.11351654964657598, 455.0000000000000568 ) ) ;
#50174=ORIENTED_EDGE ( 'NONE', *, *, #62173, .F. ) ;
#50176=DIRECTION ( 'NONE',  ( 4.336808689942006692E-15, 1.000000000000000000, 0.000000000000000000 ) ) ;
#50182=ORIENTED_EDGE ( 'NONE', *, *, #52399, .F. ) ;
#50193=CARTESIAN_POINT ( 'NONE',  ( 9.106483450353419329, 11.11351654964656710, 455.0000000000000568 ) ) ;
#50207=ADVANCED_FACE ( 'NONE', ( #17610 ), #22581, .F. ) ;
#50210=EDGE_LOOP ( 'NONE', ( #32236, #24534, #26251, #44414 ) ) ;
#50212=EDGE_CURVE ( 'NONE', #10486, #30586, #48762, .T. ) ;
#50222=DIRECTION ( 'NONE',  ( -1.836970198721029934E-16, 1.836970198721036344E-16, -1.000000000000000000 ) ) ;
#50223=DIRECTION ( 'NONE',  ( -0.7071067811865361374, 0.7071067811865588970, 2.810316974849854557E-30 ) ) ;
#50224=AXIS2_PLACEMENT_3D ( 'NONE', #45854, #67440, #19672 ) ;
#50225=EDGE_CURVE ( 'NONE', #29928, #36409, #49707, .T. ) ;
#50227=DIRECTION ( 'NONE',  ( -0.7071067811865451302, 0.7071067811865500152, 0.000000000000000000 ) ) ;
#50230=AXIS2_PLACEMENT_3D ( 'NONE', #3211, #25126, #46683 ) ;
#50238=ORIENTED_EDGE ( 'NONE', *, *, #47635, .F. ) ;
#50239=CARTESIAN_POINT ( 'NONE',  ( -4.193516549646673752, 11.31351654964658771, 195.0000000000000284 ) ) ;
#50240=DIRECTION ( 'NONE',  ( -0.7071067811865441310, 0.7071067811865510144, 0.000000000000000000 ) ) ;
#50251=CARTESIAN_POINT ( 'NONE',  ( -4.734785091273985280, -5.393625297349913694, 195.0000000000000284 ) ) ;
#50252=ADVANCED_FACE ( 'NONE', ( #29602 ), #68146, .F. ) ;
#50254=AXIS2_PLACEMENT_3D ( 'NONE', #61459, #39886, #29279 ) ;
#50275=VERTEX_POINT ( 'NONE', #56480 ) ;
#50278=DIRECTION ( 'NONE',  ( -3.491481338843132961E-15, -1.000000000000000000, -1.836970198721029934E-16 ) ) ;
#50283=EDGE_LOOP ( 'NONE', ( #52168, #49134, #40425, #60244, #56964, #50722, #62554, #20519, #24039, #469, #2501, #3488, #12470, #1070, #21695, #41379, #59665, #45814, #29695, #21054, #60493, #43413, #37329, #7563, #39270, #45728, #37328, #63201, #54208, #47090, #5117, #39044, #64912, #61734, #27303, #40225, #57830, #1498, #27831, #13678, #52451, #15141, #27178, #3161, #46536, #24146, #26506, #47916, #63773, #55319, #61352, #47642, #4297, #46074, #11950, #52315 ) ) ;
#50287=EDGE_CURVE ( 'NONE', #43460, #38308, #51887, .T. ) ;
#50293=VECTOR ( 'NONE', #67627, 1000.000000000000000 ) ;
#50299=EDGE_CURVE ( 'NONE', #59438, #66768, #61791, .T. ) ;
#50302=AXIS2_PLACEMENT_3D ( 'NONE', #58323, #53707, #37105 ) ;
#50314=ORIENTED_EDGE ( 'NONE', *, *, #64107, .T. ) ;
#50322=CIRCLE ( 'NONE', #44653, 0.1999999999999987899 ) ;
#50324=DIRECTION ( 'NONE',  ( -0.000000000000000000, -0.000000000000000000, -1.000000000000000000 ) ) ;
#50325=CARTESIAN_POINT ( 'NONE',  ( -9.828310488886049967, -2.290483450353357320, 455.0000000000000568 ) ) ;
#50328=CYLINDRICAL_SURFACE ( 'NONE', #40100, 1.399999999999999245 ) ;
#50332=VERTEX_POINT ( 'NONE', #51176 ) ;
#50361=VECTOR ( 'NONE', #42978, 1000.000000000000000 ) ;
#50364=CARTESIAN_POINT ( 'NONE',  ( -5.993516549646711766, 5.993516549646603409, 195.0000000000000284 ) ) ;
#50368=EDGE_CURVE ( 'NONE', #5249, #4384, #47978, .T. ) ;
#50379=CARTESIAN_POINT ( 'NONE',  ( -4.173516549646669738, 11.77351654964658678, 195.0000000000000284 ) ) ;
#50387=FACE_OUTER_BOUND ( 'NONE', #25838, .T. ) ;
#50392=DIRECTION ( 'NONE',  ( -1.000000000000000000, 0.000000000000000000, 0.000000000000000000 ) ) ;
#50393=ORIENTED_EDGE ( 'NONE', *, *, #40536, .F. ) ;
#50402=EDGE_CURVE ( 'NONE', #31564, #12232, #69548, .T. ) ;
#50409=EDGE_CURVE ( 'NONE', #56223, #50982, #66659, .T. ) ;
#50418=CARTESIAN_POINT ( 'NONE',  ( -1.077516549646832189, -11.34648345035347994, 455.0000000000000568 ) ) ;
#50429=ORIENTED_EDGE ( 'NONE', *, *, #42728, .T. ) ;
#50436=DIRECTION ( 'NONE',  ( 0.6414496315691617934, 0.7671651518152962090, -0.000000000000000000 ) ) ;
#50449=VECTOR ( 'NONE', #39564, 1000.000000000000000 ) ;
#50458=VERTEX_POINT ( 'NONE', #26415 ) ;
#50467=ORIENTED_EDGE ( 'NONE', *, *, #35369, .F. ) ;
#50468=LINE ( 'NONE', #8011, #8711 ) ;
#50476=ORIENTED_EDGE ( 'NONE', *, *, #56129, .T. ) ;
#50478=PLANE ( 'NONE',  #66745 ) ;
#50481=CARTESIAN_POINT ( 'NONE',  ( -10.08346604330792928, -9.306483450353335130, 195.0000000000000284 ) ) ;
#50512=DIRECTION ( 'NONE',  ( 1.000000000000000000, 0.000000000000000000, 0.000000000000000000 ) ) ;
#50516=ORIENTED_EDGE ( 'NONE', *, *, #63329, .T. ) ;
#50521=DIRECTION ( 'NONE',  ( -1.000000000000000000, 3.491481338843134144E-15, 0.000000000000000000 ) ) ;
#50522=ORIENTED_EDGE ( 'NONE', *, *, #22446, .F. ) ;
#50530=DIRECTION ( 'NONE',  ( 0.000000000000000000, -1.000000000000000000, 0.000000000000000000 ) ) ;
#50531=ADVANCED_FACE ( 'NONE', ( #54336 ), #16500, .F. ) ;
#50532=PLANE ( 'NONE',  #9749 ) ;
#50534=CARTESIAN_POINT ( 'NONE',  ( -10.08346604330783869, -2.906483450353305020, 195.0000000000000284 ) ) ;
#50539=PLANE ( 'NONE',  #65167 ) ;
#50548=DIRECTION ( 'NONE',  ( -1.836970198721029934E-16, -1.836970198721010706E-16, 1.000000000000000000 ) ) ;
#50552=ADVANCED_FACE ( 'NONE', ( #28474 ), #59635, .F. ) ;
#50558=EDGE_CURVE ( 'NONE', #58112, #26502, #27108, .T. ) ;
#50576=EDGE_CURVE ( 'NONE', #62061, #22868, #65626, .T. ) ;
#50577=DIRECTION ( 'NONE',  ( 0.7671651518153131954, 0.6414496315691415873, 2.587583378555109562E-16 ) ) ;
#50591=CARTESIAN_POINT ( 'NONE',  ( 11.32648345035340576, 7.793516549646564151, 455.0000000000000568 ) ) ;
#50601=FACE_OUTER_BOUND ( 'NONE', #49292, .T. ) ;
#50607=EDGE_CURVE ( 'NONE', #14411, #28648, #11866, .T. ) ;
#50611=EDGE_CURVE ( 'NONE', #55024, #12559, #239, .T. ) ;
#50621=DIRECTION ( 'NONE',  ( -1.836970198721029934E-16, 1.836970198721036344E-16, -1.000000000000000000 ) ) ;
#50630=CARTESIAN_POINT ( 'NONE',  ( 5.668387132715968058, 8.393516549646582448, 455.0000000000000568 ) ) ;
#50631=CARTESIAN_POINT ( 'NONE',  ( -8.393516549646712122, 6.331612867284047041, 195.0000000000000284 ) ) ;
#50634=CYLINDRICAL_SURFACE ( 'NONE', #42633, 0.6000000000000003109 ) ;
#50635=ORIENTED_EDGE ( 'NONE', *, *, #18726, .T. ) ;
#50651=CARTESIAN_POINT ( 'NONE',  ( -7.798499376344150136, -7.272650909786627871, 195.0000000000000284 ) ) ;
#50659=CARTESIAN_POINT ( 'NONE',  ( 10.74648345035337904, -1.690483450353395201, 195.0000000000000284 ) ) ;
#50661=DIRECTION ( 'NONE',  ( -0.7671651518153043137, 0.6414496315691521344, 2.587583378555129776E-16 ) ) ;
#50673=CARTESIAN_POINT ( 'NONE',  ( -7.415254214038336400, 2.993516549646603853, 455.0000000000000568 ) ) ;
#50677=CARTESIAN_POINT ( 'NONE',  ( 4.255011587777221216, 8.452095193409324025, 195.0000000000000284 ) ) ;
#50704=ORIENTED_EDGE ( 'NONE', *, *, #40175, .F. ) ;
#50709=AXIS2_PLACEMENT_3D ( 'NONE', #53957, #37341, #27071 ) ;
#50715=CARTESIAN_POINT ( 'NONE',  ( -11.77351654964674310, -4.406483450353321452, 455.0000000000000568 ) ) ;
#50721=CARTESIAN_POINT ( 'NONE',  ( -11.11351654964671631, -2.906483450353335218, 455.0000000000000568 ) ) ;
#50722=ORIENTED_EDGE ( 'NONE', *, *, #57567, .T. ) ;
#50732=EDGE_CURVE ( 'NONE', #49441, #14815, #67370, .T. ) ;
#50733=CARTESIAN_POINT ( 'NONE',  ( 7.852485183456877849, 3.417780618358537748, 195.0000000000000284 ) ) ;
#50736=CARTESIAN_POINT ( 'NONE',  ( 4.206483450353343478, -11.12648345035347575, 455.0000000000000568 ) ) ;
#50742=ORIENTED_EDGE ( 'NONE', *, *, #21697, .F. ) ;
#50749=VERTEX_POINT ( 'NONE', #34123 ) ;
#50757=LINE ( 'NONE', #17195, #12539 ) ;
#50758=FACE_OUTER_BOUND ( 'NONE', #10527, .T. ) ;
#50762=VERTEX_POINT ( 'NONE', #29527 ) ;
#50772=DIRECTION ( 'NONE',  ( 2.135044278125299371E-15, -1.000000000000000000, -3.673940397442060361E-16 ) ) ;
#50774=EDGE_CURVE ( 'NONE', #24992, #16139, #28819, .T. ) ;
#50776=CARTESIAN_POINT ( 'NONE',  ( -10.91351654964680584, -9.106483450353376696, 455.0000000000000568 ) ) ;
#50780=ORIENTED_EDGE ( 'NONE', *, *, #4897, .F. ) ;
#50785=EDGE_CURVE ( 'NONE', #43706, #65422, #36229, .T. ) ;
#50804=AXIS2_PLACEMENT_3D ( 'NONE', #9320, #2961, #41498 ) ;
#50816=DIRECTION ( 'NONE',  ( 0.000000000000000000, 3.673940397442059868E-16, -1.000000000000000000 ) ) ;
#50819=CARTESIAN_POINT ( 'NONE',  ( 11.32648345035337734, -4.406483450353491982, 455.0000000000000568 ) ) ;
#50822=ORIENTED_EDGE ( 'NONE', *, *, #58586, .T. ) ;
#50831=ADVANCED_FACE ( 'NONE', ( #19613 ), #9725, .T. ) ;
#50845=DIRECTION ( 'NONE',  ( -0.000000000000000000, -0.000000000000000000, -1.000000000000000000 ) ) ;
#50850=ORIENTED_EDGE ( 'NONE', *, *, #51079, .T. ) ;
#50853=AXIS2_PLACEMENT_3D ( 'NONE', #53992, #49709, #37723 ) ;
#50856=VECTOR ( 'NONE', #69415, 999.9999999999998863 ) ;
#50865=CARTESIAN_POINT ( 'NONE',  ( 4.206483450353341702, -11.32648345035337911, 195.0000000000000284 ) ) ;
#50869=DIRECTION ( 'NONE',  ( -1.000000000000000000, 1.047444401652940007E-14, -1.836970198721010952E-16 ) ) ;
#50871=ADVANCED_FACE ( 'NONE', ( #9365 ), #10073, .F. ) ;
#50881=ORIENTED_EDGE ( 'NONE', *, *, #19213, .T. ) ;
#50885=DIRECTION ( 'NONE',  ( 1.000000000000000000, 0.000000000000000000, 0.000000000000000000 ) ) ;
#50887=CARTESIAN_POINT ( 'NONE',  ( 9.106483450353380249, -11.12648345035348640, 455.0000000000000568 ) ) ;
#50893=VERTEX_POINT ( 'NONE', #4770 ) ;
#50898=VECTOR ( 'NONE', #16312, 1000.000000000000000 ) ;
#50899=VERTEX_POINT ( 'NONE', #4433 ) ;
#50901=FACE_OUTER_BOUND ( 'NONE', #28742, .T. ) ;
#50920=CARTESIAN_POINT ( 'NONE',  ( -3.417780618358626565, 7.839518282750134404, 455.0000000000000568 ) ) ;
#50926=DIRECTION ( 'NONE',  ( 0.000000000000000000, 1.000000000000000000, 0.000000000000000000 ) ) ;
#50928=CARTESIAN_POINT ( 'NONE',  ( 2.765062094116041980, -9.955011587777228499, 195.0000000000000284 ) ) ;
#50930=LINE ( 'NONE', #56588, #39952 ) ;
#50933=EDGE_CURVE ( 'NONE', #3671, #9740, #64515, .T. ) ;
#50938=LINE ( 'NONE', #2500, #41382 ) ;
#50949=EDGE_CURVE ( 'NONE', #61820, #54840, #55463, .T. ) ;
#50952=ADVANCED_FACE ( 'NONE', ( #32336 ), #6510, .F. ) ;
#50961=EDGE_LOOP ( 'NONE', ( #3933, #52338, #29614, #2341 ) ) ;
#50965=ORIENTED_EDGE ( 'NONE', *, *, #2562, .T. ) ;
#50974=CARTESIAN_POINT ( 'NONE',  ( -4.393516549646788505, -11.78648345035339418, 195.0000000000000284 ) ) ;
#50976=CARTESIAN_POINT ( 'NONE',  ( 7.826483450353421745, 11.77351654964657257, 455.0000000000000568 ) ) ;
#50982=VERTEX_POINT ( 'NONE', #32675 ) ;
#50987=CARTESIAN_POINT ( 'NONE',  ( 11.78648345035337819, -7.826483450353491023, 455.0000000000000568 ) ) ;
#50997=ADVANCED_FACE ( 'NONE', ( #28068 ), #60579, .F. ) ;
#50999=CARTESIAN_POINT ( 'NONE',  ( -9.234937905884127218, -9.955011587777249815, 455.0000000000000568 ) ) ;
#51007=ORIENTED_EDGE ( 'NONE', *, *, #51095, .T. ) ;
#51008=LINE ( 'NONE', #54950, #16395 ) ;
#51009=ADVANCED_FACE ( 'NONE', ( #48945 ), #16769, .F. ) ;
#51010=AXIS2_PLACEMENT_3D ( 'NONE', #28484, #28151, #16854 ) ;
#51015=EDGE_LOOP ( 'NONE', ( #45186, #6048, #43581, #62937, #64516, #43286, #57046, #10708, #43198, #14154, #4518, #67501, #46321, #28666, #55878, #30613, #17085, #46545, #52566, #28769, #27901, #6449, #17957, #40438, #23392, #33813, #15325, #57314, #59979, #15596, #57994, #35251, #37216, #62801, #24044, #69930, #13828, #47573, #52046, #63122, #10515, #63716, #44481, #3742, #45004, #69839, #37754, #52936, #64126, #12051, #1918, #63708, #59918, #19275, #24323, #34293 ) ) ;
#51019=CIRCLE ( 'NONE', #20538, 0.1999999999999987899 ) ;
#51020=ORIENTED_EDGE ( 'NONE', *, *, #57477, .F. ) ;
#51021=LINE ( 'NONE', #40413, #49598 ) ;
#51028=VERTEX_POINT ( 'NONE', #27721 ) ;
#51031=EDGE_CURVE ( 'NONE', #2080, #68417, #38510, .T. ) ;
#51044=ORIENTED_EDGE ( 'NONE', *, *, #44778, .T. ) ;
#51046=CARTESIAN_POINT ( 'NONE',  ( 11.08848345035334404, -11.48848345035339591, 195.0000000000000284 ) ) ;
#51055=DIRECTION ( 'NONE',  ( 0.000000000000000000, 1.000000000000000000, 0.000000000000000000 ) ) ;
#51061=PLANE ( 'NONE',  #46405 ) ;
#51066=CARTESIAN_POINT ( 'NONE',  ( 4.201500623656003519, -4.740315990920286104, 455.0000000000000568 ) ) ;
#51074=CARTESIAN_POINT ( 'NONE',  ( -7.603567055985637424, -8.606483450353410447, 455.0000000000000568 ) ) ;
#51079=EDGE_CURVE ( 'NONE', #24080, #17336, #56318, .T. ) ;
#51083=LINE ( 'NONE', #62741, #36442 ) ;
#51086=CARTESIAN_POINT ( 'NONE',  ( -11.99351654964671354, 11.18071654964658990, 455.0000000000000568 ) ) ;
#51092=EDGE_CURVE ( 'NONE', #33822, #41049, #7866, .T. ) ;
#51094=FACE_OUTER_BOUND ( 'NONE', #905, .T. ) ;
#51095=EDGE_CURVE ( 'NONE', #31596, #66404, #29791, .T. ) ;
#51128=ORIENTED_EDGE ( 'NONE', *, *, #37355, .F. ) ;
#51134=EDGE_CURVE ( 'NONE', #43261, #30530, #35436, .T. ) ;
#51136=EDGE_CURVE ( 'NONE', #56003, #59410, #37407, .T. ) ;
#51137=VECTOR ( 'NONE', #56314, 1000.000000000000000 ) ;
#51139=LINE ( 'NONE', #7651, #7805 ) ;
#51142=FACE_OUTER_BOUND ( 'NONE', #56735, .T. ) ;
#51160=VECTOR ( 'NONE', #35352, 1000.000000000000000 ) ;
#51162=DIRECTION ( 'NONE',  ( -1.000000000000000000, 0.000000000000000000, 0.000000000000000000 ) ) ;
#51166=VERTEX_POINT ( 'NONE', #55971 ) ;
#51171=DIRECTION ( 'NONE',  ( -1.000000000000000000, 0.000000000000000000, 0.000000000000000000 ) ) ;
#51176=CARTESIAN_POINT ( 'NONE',  ( 10.74648345035330443, 1.677516549646577371, 195.0000000000000284 ) ) ;
#51179=DIRECTION ( 'NONE',  ( 0.000000000000000000, 1.000000000000000000, 0.000000000000000000 ) ) ;
#51183=EDGE_LOOP ( 'NONE', ( #65571, #7946, #24486, #62680 ) ) ;
#51188=CYLINDRICAL_SURFACE ( 'NONE', #11933, 0.6000000000000000888 ) ;
#51192=DIRECTION ( 'NONE',  ( -5.120954910632640039E-15, -1.000000000000000000, -3.673940397442059868E-16 ) ) ;
#51193=VERTEX_POINT ( 'NONE', #3632 ) ;
#51212=FACE_OUTER_BOUND ( 'NONE', #34369, .T. ) ;
#51225=AXIS2_PLACEMENT_3D ( 'NONE', #20467, #57941, #63613 ) ;
#51227=VECTOR ( 'NONE', #53860, 1000.000000000000000 ) ;
#51232=ORIENTED_EDGE ( 'NONE', *, *, #55077, .T. ) ;
#51241=ORIENTED_EDGE ( 'NONE', *, *, #54475, .T. ) ;
#51246=ORIENTED_EDGE ( 'NONE', *, *, #46700, .F. ) ;
#51250=ORIENTED_EDGE ( 'NONE', *, *, #4415, .T. ) ;
#51262=VECTOR ( 'NONE', #45369, 1000.000000000000000 ) ;
#51266=ORIENTED_EDGE ( 'NONE', *, *, #5486, .F. ) ;
#51276=DIRECTION ( 'NONE',  ( -0.000000000000000000, -0.000000000000000000, -1.000000000000000000 ) ) ;
#51278=EDGE_CURVE ( 'NONE', #68417, #19877, #63026, .T. ) ;
#51286=DIRECTION ( 'NONE',  ( -0.000000000000000000, 3.673940397442059868E-16, -1.000000000000000000 ) ) ;
#51287=CARTESIAN_POINT ( 'NONE',  ( 3.606483450353380249, -4.622483450353396250, 195.0000000000000284 ) ) ;
#51300=EDGE_CURVE ( 'NONE', #31731, #51166, #9637, .T. ) ;
#51301=VERTEX_POINT ( 'NONE', #36498 ) ;
#51307=ORIENTED_EDGE ( 'NONE', *, *, #24267, .F. ) ;
#51310=CARTESIAN_POINT ( 'NONE',  ( 5.393625297349938563, 7.252248008019325454, 455.0000000000000568 ) ) ;
#51312=AXIS2_PLACEMENT_3D ( 'NONE', #54675, #16837, #53636 ) ;
#51316=DIRECTION ( 'NONE',  ( 0.000000000000000000, -1.000000000000000000, -3.673940397442060361E-16 ) ) ;
#51317=ORIENTED_EDGE ( 'NONE', *, *, #18864, .F. ) ;
#51318=EDGE_LOOP ( 'NONE', ( #21236, #59124, #30852, #19297 ) ) ;
#51323=LINE ( 'NONE', #61569, #40273 ) ;
#51341=CARTESIAN_POINT ( 'NONE',  ( -9.791916549646712653, 10.19191654964664018, 195.0000000000000284 ) ) ;
#51347=EDGE_CURVE ( 'NONE', #38001, #15827, #27633, .T. ) ;
#51349=VERTEX_POINT ( 'NONE', #65133 ) ;
#51352=DIRECTION ( 'NONE',  ( 1.221996412923863792E-14, 1.000000000000000000, 1.836970198721013910E-16 ) ) ;
#51353=DIRECTION ( 'NONE',  ( 1.000000000000000000, 0.000000000000000000, 0.000000000000000000 ) ) ;
#51358=VERTEX_POINT ( 'NONE', #10675 ) ;
#51366=VECTOR ( 'NONE', #60778, 1000.000000000000000 ) ;
#51367=CARTESIAN_POINT ( 'NONE',  ( 10.09643294401453062, 2.693516549646537417, 455.0000000000000568 ) ) ;
#51370=DIRECTION ( 'NONE',  ( -0.000000000000000000, -0.000000000000000000, -1.000000000000000000 ) ) ;
#51371=CARTESIAN_POINT ( 'NONE',  ( 4.406483450353420928, 11.77351654964658501, 455.0000000000000568 ) ) ;
#51376=ORIENTED_EDGE ( 'NONE', *, *, #8336, .F. ) ;
#51379=ORIENTED_EDGE ( 'NONE', *, *, #3869, .T. ) ;
#51384=DIRECTION ( 'NONE',  ( -1.000000000000000000, 0.000000000000000000, 0.000000000000000000 ) ) ;
#51387=ORIENTED_EDGE ( 'NONE', *, *, #43149, .F. ) ;
#51390=ORIENTED_EDGE ( 'NONE', *, *, #33037, .F. ) ;
#51398=EDGE_LOOP ( 'NONE', ( #62293, #59474, #64836, #42987 ) ) ;
#51401=CARTESIAN_POINT ( 'NONE',  ( -9.791916549646856538, -10.20488345035338718, 455.0000000000000568 ) ) ;
#51403=CARTESIAN_POINT ( 'NONE',  ( 1.090483450353343819, -10.74648345035345365, 455.0000000000000568 ) ) ;
#51405=FACE_OUTER_BOUND ( 'NONE', #16777, .T. ) ;
#51410=LINE ( 'NONE', #34086, #56551 ) ;
#51414=ORIENTED_EDGE ( 'NONE', *, *, #21833, .F. ) ;
#51415=DIRECTION ( 'NONE',  ( 0.000000000000000000, 3.673940397442059868E-16, -1.000000000000000000 ) ) ;
#51419=DIRECTION ( 'NONE',  ( -1.836970198721029934E-16, 1.836970198721036344E-16, -1.000000000000000000 ) ) ;
#51427=VECTOR ( 'NONE', #15389, 1000.000000000000000 ) ;
#51428=DIRECTION ( 'NONE',  ( -1.221996412923863792E-14, -1.000000000000000000, 0.000000000000000000 ) ) ;
#51430=ADVANCED_FACE ( 'NONE', ( #42850 ), #21293, .F. ) ;
#51433=VECTOR ( 'NONE', #67042, 1000.000000000000000 ) ;
#51441=DIRECTION ( 'NONE',  ( 0.000000000000000000, -1.000000000000000000, -3.673940397442059868E-16 ) ) ;
#51446=DIRECTION ( 'NONE',  ( 1.000000000000000000, -8.540177112501197482E-15, 0.000000000000000000 ) ) ;
#51447=CYLINDRICAL_SURFACE ( 'NONE', #54260, 0.5999999999999998668 ) ;
#51448=CARTESIAN_POINT ( 'NONE',  ( 10.74648345035334529, 1.077516549646528876, 455.0000000000000568 ) ) ;
#51450=CARTESIAN_POINT ( 'NONE',  ( -9.791916549646712653, 10.19191654964664018, 455.0000000000000568 ) ) ;
#51454=ORIENTED_EDGE ( 'NONE', *, *, #63329, .F. ) ;
#51460=VECTOR ( 'NONE', #38383, 1000.000000000000000 ) ;
#51461=CARTESIAN_POINT ( 'NONE',  ( -7.393516549646727221, -6.006483450353401921, 195.0000000000000284 ) ) ;
#51463=AXIS2_PLACEMENT_3D ( 'NONE', #51448, #2649, #62390 ) ;
#51468=CARTESIAN_POINT ( 'NONE',  ( 2.765062094116107705, 9.942044687070449527, 455.0000000000000568 ) ) ;
#51469=CARTESIAN_POINT ( 'NONE',  ( 7.806483450353418618, 11.31351654964657172, 455.0000000000000568 ) ) ;
#51485=LINE ( 'NONE', #63140, #34979 ) ;
#51499=DIRECTION ( 'NONE',  ( 0.000000000000000000, 1.000000000000000000, 0.000000000000000000 ) ) ;
#51501=EDGE_CURVE ( 'NONE', #44814, #21914, #60492, .T. ) ;
#51507=ORIENTED_EDGE ( 'NONE', *, *, #38116, .T. ) ;
#51515=CARTESIAN_POINT ( 'NONE',  ( -10.91351654964670637, 2.693516549646604030, 455.0000000000000568 ) ) ;
#51533=FACE_OUTER_BOUND ( 'NONE', #64425, .T. ) ;
#51543=ORIENTED_EDGE ( 'NONE', *, *, #35693, .T. ) ;
#51546=ORIENTED_EDGE ( 'NONE', *, *, #39047, .T. ) ;
#51550=DIRECTION ( 'NONE',  ( 1.836970198721029934E-16, 1.836970198721010706E-16, -1.000000000000000000 ) ) ;
#51555=ORIENTED_EDGE ( 'NONE', *, *, #30941, .F. ) ;
#51565=FACE_OUTER_BOUND ( 'NONE', #9381, .T. ) ;
#51580=ORIENTED_EDGE ( 'NONE', *, *, #63512, .F. ) ;
#51583=VECTOR ( 'NONE', #18588, 1000.000000000000000 ) ;
#51590=EDGE_CURVE ( 'NONE', #28734, #14243, #38561, .T. ) ;
#51595=DIRECTION ( 'NONE',  ( 1.079558018506126625E-14, 1.000000000000000000, 1.836970198721016622E-16 ) ) ;
#51597=ORIENTED_EDGE ( 'NONE', *, *, #356, .T. ) ;
#51599=ORIENTED_EDGE ( 'NONE', *, *, #52625, .F. ) ;
#51603=CARTESIAN_POINT ( 'NONE',  ( 11.78648345035337819, -4.406483450353490205, 455.0000000000000568 ) ) ;
#51604=CARTESIAN_POINT ( 'NONE',  ( -5.993516549646711766, 5.993516549646603409, 195.0000000000000284 ) ) ;
#51605=ORIENTED_EDGE ( 'NONE', *, *, #56858, .F. ) ;
#51608=LINE ( 'NONE', #26142, #30038 ) ;
#51612=VECTOR ( 'NONE', #36389, 1000.000000000000000 ) ;
#51613=CARTESIAN_POINT ( 'NONE',  ( -2.277516549646682709, 9.828310488885916740, 455.0000000000000568 ) ) ;
#51615=ORIENTED_EDGE ( 'NONE', *, *, #7853, .F. ) ;
#51617=LINE ( 'NONE', #62214, #46415 ) ;
#51621=LINE ( 'NONE', #23352, #14465 ) ;
#51630=EDGE_LOOP ( 'NONE', ( #16724, #67218, #47289, #9124 ) ) ;
#51640=CARTESIAN_POINT ( 'NONE',  ( 11.12648345035337982, -4.206483450353492692, 455.0000000000000568 ) ) ;
#51644=ORIENTED_EDGE ( 'NONE', *, *, #54726, .T. ) ;
#51651=ORIENTED_EDGE ( 'NONE', *, *, #42493, .T. ) ;
#51654=DIRECTION ( 'NONE',  ( 0.5000000000000019984, 0.8660254037844375974, 3.181725716174716554E-16 ) ) ;
#51655=ORIENTED_EDGE ( 'NONE', *, *, #23559, .F. ) ;
#51658=ORIENTED_EDGE ( 'NONE', *, *, #30121, .T. ) ;
#51660=DIRECTION ( 'NONE',  ( 0.000000000000000000, -1.000000000000000000, 0.000000000000000000 ) ) ;
#51662=VERTEX_POINT ( 'NONE', #16160 ) ;
#51663=AXIS2_PLACEMENT_3D ( 'NONE', #61237, #61588, #28727 ) ;
#51670=AXIS2_PLACEMENT_3D ( 'NONE', #25711, #30646, #58218 ) ;
#51672=LINE ( 'NONE', #29738, #48890 ) ;
#51674=ORIENTED_EDGE ( 'NONE', *, *, #25862, .T. ) ;
#51684=ORIENTED_EDGE ( 'NONE', *, *, #951, .T. ) ;
#51693=LINE ( 'NONE', #8532, #65575 ) ;
#51697=CARTESIAN_POINT ( 'NONE',  ( 1.090483450353338268, -11.34648345035335737, 195.0000000000000284 ) ) ;
#51702=CARTESIAN_POINT ( 'NONE',  ( -4.727349090213461835, 4.188533722949259186, 195.0000000000000284 ) ) ;
#51710=ORIENTED_EDGE ( 'NONE', *, *, #15717, .T. ) ;
#51718=FACE_OUTER_BOUND ( 'NONE', #23566, .T. ) ;
#51731=CARTESIAN_POINT ( 'NONE',  ( -8.393516549646712122, 4.383466043307770121, 195.0000000000000284 ) ) ;
#51733=VECTOR ( 'NONE', #33222, 1000.000000000000000 ) ;
#51737=DIRECTION ( 'NONE',  ( -1.836970198721029934E-16, 1.836970198721036344E-16, -1.000000000000000000 ) ) ;
#51738=VERTEX_POINT ( 'NONE', #31738 ) ;
#51739=ORIENTED_EDGE ( 'NONE', *, *, #59667, .F. ) ;
#51740=ORIENTED_EDGE ( 'NONE', *, *, #60291, .F. ) ;
#51743=DIRECTION ( 'NONE',  ( -0.000000000000000000, -0.000000000000000000, -1.000000000000000000 ) ) ;
#51749=VERTEX_POINT ( 'NONE', #32077 ) ;
#51756=EDGE_LOOP ( 'NONE', ( #32168, #56872, #56897, #1132 ) ) ;
#51761=VERTEX_POINT ( 'NONE', #20415 ) ;
#51767=ORIENTED_EDGE ( 'NONE', *, *, #64526, .F. ) ;
#51771=CARTESIAN_POINT ( 'NONE',  ( -11.11351654964674474, -7.806483450353326248, 195.0000000000000284 ) ) ;
#51772=CYLINDRICAL_SURFACE ( 'NONE', #27118, 2.204799999999999205 ) ;
#51780=ORIENTED_EDGE ( 'NONE', *, *, #17557, .T. ) ;
#51786=EDGE_LOOP ( 'NONE', ( #32517, #31390, #8951, #26180 ) ) ;
#51787=DIRECTION ( 'NONE',  ( -7.665540703601096574E-15, -1.000000000000000000, -3.673940397442059868E-16 ) ) ;
#51788=CARTESIAN_POINT ( 'NONE',  ( -8.393516549646768965, -5.668387132715940524, 455.0000000000000568 ) ) ;
#51790=CARTESIAN_POINT ( 'NONE',  ( -9.293516549646710700, 10.91351654964659801, 455.0000000000000568 ) ) ;
#51798=DIRECTION ( 'NONE',  ( -0.000000000000000000, -0.000000000000000000, -1.000000000000000000 ) ) ;
#51799=FACE_OUTER_BOUND ( 'NONE', #9612, .T. ) ;
#51811=EDGE_CURVE ( 'NONE', #50899, #37032, #27815, .T. ) ;
#51818=EDGE_LOOP ( 'NONE', ( #22841, #32105, #14487, #46779 ) ) ;
#51820=DIRECTION ( 'NONE',  ( 1.836970198721029934E-16, -1.836970198721036344E-16, 1.000000000000000000 ) ) ;
#51821=VECTOR ( 'NONE', #37221, 1000.000000000000000 ) ;
#51830=CARTESIAN_POINT ( 'NONE',  ( -7.259684009079963474, -4.201500623656036382, 455.0000000000000568 ) ) ;
#51842=ADVANCED_FACE ( 'NONE', ( #55717 ), #6592, .F. ) ;
#51843=VECTOR ( 'NONE', #42658, 1000.000000000000000 ) ;
#51849=ORIENTED_EDGE ( 'NONE', *, *, #33836, .F. ) ;
#51850=VECTOR ( 'NONE', #31533, 1000.000000000000000 ) ;
#51852=DIRECTION ( 'NONE',  ( -1.000000000000000000, 0.000000000000000000, 0.000000000000000000 ) ) ;
#51853=EDGE_CURVE ( 'NONE', #56701, #27098, #54689, .T. ) ;
#51855=ADVANCED_FACE ( 'NONE', ( #38426 ), #59976, .T. ) ;
#51865=AXIS2_PLACEMENT_3D ( 'NONE', #23817, #7885, #45370 ) ;
#51869=DIRECTION ( 'NONE',  ( -1.836970198721029934E-16, 1.836970198721036344E-16, -1.000000000000000000 ) ) ;
#51871=CARTESIAN_POINT ( 'NONE',  ( -11.11351654964674474, -7.806483450353326248, 195.0000000000000284 ) ) ;
#51887=LINE ( 'NONE', #23601, #11297 ) ;
#51893=PLANE ( 'NONE',  #4929 ) ;
#51900=EDGE_LOOP ( 'NONE', ( #14258, #69538, #53495, #31974 ) ) ;
#51909=LINE ( 'NONE', #3471, #11060 ) ;
#51918=ORIENTED_EDGE ( 'NONE', *, *, #58865, .F. ) ;
#51923=VECTOR ( 'NONE', #37301, 1000.000000000000000 ) ;
#51936=CYLINDRICAL_SURFACE ( 'NONE', #55450, 0.2000000000000005107 ) ;
#51939=EDGE_LOOP ( 'NONE', ( #49051, #34037, #3866, #69310 ) ) ;
#51940=AXIS2_PLACEMENT_3D ( 'NONE', #68680, #14225, #46395 ) ;
#51941=EDGE_CURVE ( 'NONE', #64793, #6389, #62402, .T. ) ;
#51942=LINE ( 'NONE', #4219, #61751 ) ;
#51943=FACE_OUTER_BOUND ( 'NONE', #47656, .T. ) ;
#51945=VERTEX_POINT ( 'NONE', #50418 ) ;
#51954=DIRECTION ( 'NONE',  ( 0.000000000000000000, 1.000000000000000000, 0.000000000000000000 ) ) ;
#51956=DIRECTION ( 'NONE',  ( -1.000000000000000000, 1.047444401652940007E-14, -1.836970198721010706E-16 ) ) ;
#51966=CARTESIAN_POINT ( 'NONE',  ( -10.19191654964671301, 10.19191654964664018, 455.0000000000000568 ) ) ;
#51972=EDGE_CURVE ( 'NONE', #33646, #66510, #30731, .T. ) ;
#51975=EDGE_LOOP ( 'NONE', ( #47565, #40711, #25577, #9750 ) ) ;
#51976=CARTESIAN_POINT ( 'NONE',  ( -10.91351654964670637, 9.293516549646604119, 455.0000000000000568 ) ) ;
#51979=ORIENTED_EDGE ( 'NONE', *, *, #28002, .F. ) ;
#51980=AXIS2_PLACEMENT_3D ( 'NONE', #32733, #38394, #65281 ) ;
#51996=DIRECTION ( 'NONE',  ( 8.673617379884087537E-15, 1.000000000000000000, 0.000000000000000000 ) ) ;
#51997=LINE ( 'NONE', #57642, #44791 ) ;
#52001=ORIENTED_EDGE ( 'NONE', *, *, #62202, .F. ) ;
#52007=ORIENTED_EDGE ( 'NONE', *, *, #49200, .F. ) ;
#52009=ORIENTED_EDGE ( 'NONE', *, *, #61454, .F. ) ;
#52011=ORIENTED_EDGE ( 'NONE', *, *, #20670, .F. ) ;
#52013=DIRECTION ( 'NONE',  ( -0.000000000000000000, -0.000000000000000000, -1.000000000000000000 ) ) ;
#52016=VERTEX_POINT ( 'NONE', #51461 ) ;
#52021=DIRECTION ( 'NONE',  ( -0.000000000000000000, 3.673940397442059868E-16, -1.000000000000000000 ) ) ;
#52027=DIRECTION ( 'NONE',  ( -0.000000000000000000, 3.673940397442059868E-16, -1.000000000000000000 ) ) ;
#52028=CARTESIAN_POINT ( 'NONE',  ( 2.765062094116041980, -9.955011587777324422, 455.0000000000000568 ) ) ;
#52029=ADVANCED_FACE ( 'NONE', ( #7622 ), #29179, .F. ) ;
#52031=ORIENTED_EDGE ( 'NONE', *, *, #41299, .T. ) ;
#52032=VECTOR ( 'NONE', #67538, 1000.000000000000000 ) ;
#52034=CARTESIAN_POINT ( 'NONE',  ( -5.993516549646711766, 5.993516549646603409, 195.0000000000000284 ) ) ;
#52046=ORIENTED_EDGE ( 'NONE', *, *, #10525, .F. ) ;
#52049=DIRECTION ( 'NONE',  ( 1.836970198721029934E-16, 1.836970198721010706E-16, -1.000000000000000000 ) ) ;
#52051=ORIENTED_EDGE ( 'NONE', *, *, #33978, .T. ) ;
#52069=DIRECTION ( 'NONE',  ( 1.920885163218982051E-15, 1.000000000000000000, 1.836970198721033139E-16 ) ) ;
#52078=LINE ( 'NONE', #57024, #358 ) ;
#52091=VECTOR ( 'NONE', #59123, 1000.000000000000000 ) ;
#52092=LINE ( 'NONE', #13206, #52356 ) ;
#52094=ORIENTED_EDGE ( 'NONE', *, *, #30879, .T. ) ;
#52095=EDGE_LOOP ( 'NONE', ( #6427, #67271, #47994, #54942 ) ) ;
#52099=ORIENTED_EDGE ( 'NONE', *, *, #66524, .T. ) ;
#52112=PLANE ( 'NONE',  #68461 ) ;
#52119=DIRECTION ( 'NONE',  ( 1.836970198721029934E-16, 1.836970198721010706E-16, -1.000000000000000000 ) ) ;
#52120=AXIS2_PLACEMENT_3D ( 'NONE', #48912, #5080, #59859 ) ;
#52123=CYLINDRICAL_SURFACE ( 'NONE', #1556, 1.399999999999999245 ) ;
#52128=CARTESIAN_POINT ( 'NONE',  ( -11.99351654964679526, -7.826483450353362237, 455.0000000000000568 ) ) ;
#52130=DIRECTION ( 'NONE',  ( -0.000000000000000000, -0.000000000000000000, -1.000000000000000000 ) ) ;
#52136=VECTOR ( 'NONE', #45979, 1000.000000000000000 ) ;
#52140=CARTESIAN_POINT ( 'NONE',  ( -9.234937905884127218, -9.955011587777249815, 455.0000000000000568 ) ) ;
#52143=LINE ( 'NONE', #13954, #12033 ) ;
#52146=DIRECTION ( 'NONE',  ( -1.000000000000000000, 0.000000000000000000, 0.000000000000000000 ) ) ;
#52147=DIRECTION ( 'NONE',  ( -0.6414496315691617934, 0.7671651518152962090, 0.000000000000000000 ) ) ;
#52157=EDGE_CURVE ( 'NONE', #12808, #938, #41555, .T. ) ;
#52161=EDGE_CURVE ( 'NONE', #26006, #36409, #53235, .T. ) ;
#52166=EDGE_CURVE ( 'NONE', #44324, #3209, #68426, .T. ) ;
#52168=ORIENTED_EDGE ( 'NONE', *, *, #9939, .T. ) ;
#52172=EDGE_CURVE ( 'NONE', #2958, #5311, #64191, .T. ) ;
#52176=ORIENTED_EDGE ( 'NONE', *, *, #985, .F. ) ;
#52179=ORIENTED_EDGE ( 'NONE', *, *, #28049, .T. ) ;
#52184=DIRECTION ( 'NONE',  ( -1.836970198721029934E-16, 1.836970198721036344E-16, -1.000000000000000000 ) ) ;
#52193=EDGE_CURVE ( 'NONE', #22396, #12404, #47562, .T. ) ;
#52194=CARTESIAN_POINT ( 'NONE',  ( 9.841277389592722358, -2.290483450353490547, 455.0000000000000568 ) ) ;
#52197=DIRECTION ( 'NONE',  ( 0.000000000000000000, -1.000000000000000000, 0.000000000000000000 ) ) ;
#52208=ORIENTED_EDGE ( 'NONE', *, *, #62429, .T. ) ;
#52211=AXIS2_PLACEMENT_3D ( 'NONE', #48733, #42727, #37435 ) ;
#52222=CARTESIAN_POINT ( 'NONE',  ( -10.08346604330788665, -2.906483450353353426, 455.0000000000000568 ) ) ;
#52223=EDGE_CURVE ( 'NONE', #31671, #67553, #36972, .T. ) ;
#52231=DIRECTION ( 'NONE',  ( -0.6414496315691494699, -0.7671651518153064231, -0.000000000000000000 ) ) ;
#52233=ORIENTED_EDGE ( 'NONE', *, *, #40847, .T. ) ;
#52239=EDGE_CURVE ( 'NONE', #67654, #47832, #32688, .T. ) ;
#52241=VERTEX_POINT ( 'NONE', #44663 ) ;
#52246=CARTESIAN_POINT ( 'NONE',  ( -8.198316549646774476, -6.006483450353403697, 455.0000000000000568 ) ) ;
#52247=ORIENTED_EDGE ( 'NONE', *, *, #2364, .F. ) ;
#52248=CARTESIAN_POINT ( 'NONE',  ( -4.609516549646713202, 3.593516549646603941, 195.0000000000000284 ) ) ;
#52250=CIRCLE ( 'NONE', #21766, 1.399999999999998579 ) ;
#52258=DIRECTION ( 'NONE',  ( 1.000000000000000000, -3.491481338843133750E-15, -1.836970198721036590E-16 ) ) ;
#52260=VERTEX_POINT ( 'NONE', #17812 ) ;
#52264=VERTEX_POINT ( 'NONE', #53927 ) ;
#52274=CARTESIAN_POINT ( 'NONE',  ( 8.465062094116072799, 4.242044687070411157, 455.0000000000000568 ) ) ;
#52277=AXIS2_PLACEMENT_3D ( 'NONE', #4280, #9221, #52723 ) ;
#52283=CARTESIAN_POINT ( 'NONE',  ( 1.866219381641484931, 9.404046420174006826, 455.0000000000000568 ) ) ;
#52287=DIRECTION ( 'NONE',  ( -0.000000000000000000, 3.673940397442059868E-16, -1.000000000000000000 ) ) ;
#52292=EDGE_LOOP ( 'NONE', ( #16319, #33780, #57786, #53411 ) ) ;
#52296=VECTOR ( 'NONE', #38499, 1000.000000000000000 ) ;
#52299=CARTESIAN_POINT ( 'NONE',  ( -11.99351654964683078, -11.19368345035334933, 455.0000000000000568 ) ) ;
#52303=DIRECTION ( 'NONE',  ( 2.891205793294683355E-15, 1.000000000000000000, 0.000000000000000000 ) ) ;
#52309=ORIENTED_EDGE ( 'NONE', *, *, #1572, .T. ) ;
#52312=LINE ( 'NONE', #57262, #65720 ) ;
#52314=DIRECTION ( 'NONE',  ( -0.000000000000000000, -0.000000000000000000, -1.000000000000000000 ) ) ;
#52315=ORIENTED_EDGE ( 'NONE', *, *, #63066, .T. ) ;
#52317=CYLINDRICAL_SURFACE ( 'NONE', #3475, 0.3999999999999993006 ) ;
#52326=EDGE_CURVE ( 'NONE', #67578, #5297, #60242, .T. ) ;
#52337=ORIENTED_EDGE ( 'NONE', *, *, #51092, .T. ) ;
#52338=ORIENTED_EDGE ( 'NONE', *, *, #39572, .F. ) ;
#52341=ORIENTED_EDGE ( 'NONE', *, *, #43353, .F. ) ;
#52346=CIRCLE ( 'NONE', #25238, 0.1999999999999987899 ) ;
#52356=VECTOR ( 'NONE', #8241, 1000.000000000000000 ) ;
#52360=VERTEX_POINT ( 'NONE', #7538 ) ;
#52370=ORIENTED_EDGE ( 'NONE', *, *, #54589, .F. ) ;
#52374=EDGE_CURVE ( 'NONE', #58876, #1978, #29115, .T. ) ;
#52377=CARTESIAN_POINT ( 'NONE',  ( -9.942044687070568543, 2.752095193409294982, 195.0000000000000284 ) ) ;
#52379=VERTEX_POINT ( 'NONE', #12489 ) ;
#52384=CARTESIAN_POINT ( 'NONE',  ( 7.616533956692213003, -8.406483450353491094, 455.0000000000000568 ) ) ;
#52388=ADVANCED_FACE ( 'NONE', ( #35098 ), #1895, .F. ) ;
#52397=VECTOR ( 'NONE', #66596, 1000.000000000000000 ) ;
#52399=EDGE_CURVE ( 'NONE', #67569, #41197, #40770, .T. ) ;
#52408=VECTOR ( 'NONE', #15863, 1000.000000000000000 ) ;
#52412=FACE_OUTER_BOUND ( 'NONE', #37963, .T. ) ;
#52417=VECTOR ( 'NONE', #21654, 1000.000000000000000 ) ;
#52425=ORIENTED_EDGE ( 'NONE', *, *, #61442, .F. ) ;
#52432=CARTESIAN_POINT ( 'NONE',  ( 4.740315990920131561, -4.201500623656049704, 195.0000000000000284 ) ) ;
#52445=LINE ( 'NONE', #58088, #40105 ) ;
#52448=DIRECTION ( 'NONE',  ( -1.000000000000000000, 1.819560449471430698E-15, 1.836970198721033385E-16 ) ) ;
#52451=ORIENTED_EDGE ( 'NONE', *, *, #63495, .T. ) ;
#52455=CIRCLE ( 'NONE', #56918, 0.1999999999999987899 ) ;
#52457=DIRECTION ( 'NONE',  ( 1.000000000000000000, 0.000000000000000000, 0.000000000000000000 ) ) ;
#52460=CARTESIAN_POINT ( 'NONE',  ( 2.706483450353343478, -10.92648345035346225, 455.0000000000000568 ) ) ;
#52462=DIRECTION ( 'NONE',  ( -1.000000000000000000, 1.280238727658158235E-15, 0.000000000000000000 ) ) ;
#52467=FACE_OUTER_BOUND ( 'NONE', #24678, .T. ) ;
#52471=VERTEX_POINT ( 'NONE', #18849 ) ;
#52497=LINE ( 'NONE', #47196, #41023 ) ;
#52503=CARTESIAN_POINT ( 'NONE',  ( 10.74648345035337904, -1.690483450353490680, 455.0000000000000568 ) ) ;
#52505=VECTOR ( 'NONE', #57032, 1000.000000000000114 ) ;
#52519=EDGE_CURVE ( 'NONE', #3656, #35382, #23072, .T. ) ;
#52534=LINE ( 'NONE', #63134, #9039 ) ;
#52541=DIRECTION ( 'NONE',  ( -0.000000000000000000, 3.673940397442059868E-16, -1.000000000000000000 ) ) ;
#52545=VECTOR ( 'NONE', #68803, 1000.000000000000000 ) ;
#52551=ORIENTED_EDGE ( 'NONE', *, *, #60371, .F. ) ;
#52565=LINE ( 'NONE', #68470, #25407 ) ;
#52566=ORIENTED_EDGE ( 'NONE', *, *, #22399, .F. ) ;
#52579=EDGE_CURVE ( 'NONE', #43306, #48961, #10616, .T. ) ;
#52580=CARTESIAN_POINT ( 'NONE',  ( -5.993516549646711766, 5.993516549646603409, 455.0000000000000568 ) ) ;
#52584=DIRECTION ( 'NONE',  ( -0.000000000000000000, -0.000000000000000000, -1.000000000000000000 ) ) ;
#52598=VECTOR ( 'NONE', #53286, 1000.000000000000000 ) ;
#52604=PLANE ( 'NONE',  #20179 ) ;
#52613=PLANE ( 'NONE',  #57836 ) ;
#52619=DIRECTION ( 'NONE',  ( -1.000000000000000000, 0.000000000000000000, 0.000000000000000000 ) ) ;
#52623=CARTESIAN_POINT ( 'NONE',  ( -11.11351654964680336, -9.106483450353373144, 455.0000000000000568 ) ) ;
#52625=EDGE_CURVE ( 'NONE', #4940, #24424, #36885, .T. ) ;
#52626=ORIENTED_EDGE ( 'NONE', *, *, #67057, .F. ) ;
#52638=EDGE_CURVE ( 'NONE', #5044, #60174, #11763, .T. ) ;
#52640=ORIENTED_EDGE ( 'NONE', *, *, #44937, .F. ) ;
#52653=LINE ( 'NONE', #36020, #13197 ) ;
#52661=CIRCLE ( 'NONE', #23306, 0.8128000000000145109 ) ;
#52669=EDGE_CURVE ( 'NONE', #21676, #31344, #22686, .T. ) ;
#52670=ORIENTED_EDGE ( 'NONE', *, *, #14141, .F. ) ;
#52671=LINE ( 'NONE', #46995, #1900 ) ;
#52674=EDGE_CURVE ( 'NONE', #59671, #9593, #16002, .T. ) ;
#52683=CARTESIAN_POINT ( 'NONE',  ( 4.740315990920124456, 7.798499376343988487, 195.0000000000000284 ) ) ;
#52685=ORIENTED_EDGE ( 'NONE', *, *, #22446, .T. ) ;
#52691=ORIENTED_EDGE ( 'NONE', *, *, #16132, .T. ) ;
#52704=LINE ( 'NONE', #19105, #6947 ) ;
#52706=ADVANCED_FACE ( 'NONE', ( #6759 ), #28326, .F. ) ;
#52719=PLANE ( 'NONE',  #50230 ) ;
#52723=DIRECTION ( 'NONE',  ( -0.7071067811865500152, -0.7071067811865451302, 0.000000000000000000 ) ) ;
#52727=EDGE_CURVE ( 'NONE', #62021, #44522, #48524, .T. ) ;
#52728=DIRECTION ( 'NONE',  ( -1.836970198721029934E-16, 1.836970198721036344E-16, -1.000000000000000000 ) ) ;
#52733=EDGE_CURVE ( 'NONE', #9315, #8669, #21308, .T. ) ;
#52737=VERTEX_POINT ( 'NONE', #5745 ) ;
#52739=ADVANCED_FACE ( 'NONE', ( #64443 ), #60509, .F. ) ;
#52755=PLANE ( 'NONE',  #54983 ) ;
#52756=DIRECTION ( 'NONE',  ( -8.903847840905249551E-15, -1.000000000000000000, -1.836970198721027222E-16 ) ) ;
#52757=VECTOR ( 'NONE', #19419, 1000.000000000000000 ) ;
#52769=LINE ( 'NONE', #46728, #24454 ) ;
#52780=VECTOR ( 'NONE', #54042, 1000.000000000000000 ) ;
#52785=LINE ( 'NONE', #30840, #56418 ) ;
#52786=ORIENTED_EDGE ( 'NONE', *, *, #9379, .F. ) ;
#52802=EDGE_CURVE ( 'NONE', #31596, #55024, #34311, .T. ) ;
#52810=CIRCLE ( 'NONE', #46008, 0.1999999999999992339 ) ;
#52812=AXIS2_PLACEMENT_3D ( 'NONE', #53613, #20721, #37007 ) ;
#52819=EDGE_LOOP ( 'NONE', ( #39182, #65249, #1552, #36907 ) ) ;
#52824=VECTOR ( 'NONE', #15485, 1000.000000000000000 ) ;
#52825=ORIENTED_EDGE ( 'NONE', *, *, #14352, .F. ) ;
#52827=DIRECTION ( 'NONE',  ( 0.7071067811865514585, 0.7071067811865435759, -0.000000000000000000 ) ) ;
#52830=ORIENTED_EDGE ( 'NONE', *, *, #40317, .T. ) ;
#52832=DIRECTION ( 'NONE',  ( 1.920292680692490463E-14, 1.000000000000000000, 0.000000000000000000 ) ) ;
#52834=ORIENTED_EDGE ( 'NONE', *, *, #35071, .T. ) ;
#52837=DIRECTION ( 'NONE',  ( 3.491481338843133355E-15, 1.000000000000000000, 1.836970198721029934E-16 ) ) ;
#52842=CARTESIAN_POINT ( 'NONE',  ( -6.331612867284196255, -8.406483450353375630, 195.0000000000000284 ) ) ;
#52873=CARTESIAN_POINT ( 'NONE',  ( 6.344579767990805585, 8.393516549646626856, 195.0000000000000284 ) ) ;
#52876=VERTEX_POINT ( 'NONE', #35358 ) ;
#52877=CARTESIAN_POINT ( 'NONE',  ( 9.417013320880768035, 1.853252480934615809, 455.0000000000000568 ) ) ;
#52881=EDGE_CURVE ( 'NONE', #52379, #57399, #44509, .T. ) ;
#52884=DIRECTION ( 'NONE',  ( 0.7071067811865486830, 0.7071067811865464625, 0.000000000000000000 ) ) ;
#52890=ORIENTED_EDGE ( 'NONE', *, *, #68540, .T. ) ;
#52893=ORIENTED_EDGE ( 'NONE', *, *, #49203, .T. ) ;
#52903=CARTESIAN_POINT ( 'NONE',  ( -11.77351654964679284, -7.826483450353365789, 455.0000000000000568 ) ) ;
#52905=ORIENTED_EDGE ( 'NONE', *, *, #59288, .F. ) ;
#52918=AXIS2_PLACEMENT_3D ( 'NONE', #9141, #3830, #45915 ) ;
#52919=DIRECTION ( 'NONE',  ( -1.000000000000000000, 0.000000000000000000, 0.000000000000000000 ) ) ;
#52927=ORIENTED_EDGE ( 'NONE', *, *, #34876, .T. ) ;
#52931=ADVANCED_FACE ( 'NONE', ( #64028 ), #52719, .F. ) ;
#52936=ORIENTED_EDGE ( 'NONE', *, *, #54726, .F. ) ;
#52941=ORIENTED_EDGE ( 'NONE', *, *, #25872, .F. ) ;
#52945=CARTESIAN_POINT ( 'NONE',  ( -2.752095193409509033, -9.955011587777317317, 455.0000000000000568 ) ) ;
#52949=DIRECTION ( 'NONE',  ( 1.836970198721029934E-16, 1.836970198721010706E-16, -1.000000000000000000 ) ) ;
#52964=VERTEX_POINT ( 'NONE', #9218 ) ;
#52965=CARTESIAN_POINT ( 'NONE',  ( -8.393516549646712122, 7.603567055985436696, 195.0000000000000284 ) ) ;
#52976=ORIENTED_EDGE ( 'NONE', *, *, #4604, .T. ) ;
#52977=DIRECTION ( 'NONE',  ( -1.000000000000000000, 3.491481338843132961E-15, 1.836970198721036344E-16 ) ) ;
#52997=VECTOR ( 'NONE', #18495, 1000.000000000000000 ) ;
#53002=CIRCLE ( 'NONE', #22505, 0.1999999999999987899 ) ;
#53010=VECTOR ( 'NONE', #20558, 1000.000000000000000 ) ;
#53013=DIRECTION ( 'NONE',  ( -1.836970198721029934E-16, -1.836970198721010706E-16, 1.000000000000000000 ) ) ;
#53015=AXIS2_PLACEMENT_3D ( 'NONE', #56103, #67422, #7654 ) ;
#53016=DIRECTION ( 'NONE',  ( -0.000000000000000000, 3.673940397442059868E-16, -1.000000000000000000 ) ) ;
#53020=DIRECTION ( 'NONE',  ( -0.000000000000000000, -0.000000000000000000, -1.000000000000000000 ) ) ;
#53021=VECTOR ( 'NONE', #69875, 1000.000000000000114 ) ;
#53028=CARTESIAN_POINT ( 'NONE',  ( 8.406483450353384512, 4.383466043307721272, 455.0000000000000568 ) ) ;
#53046=EDGE_CURVE ( 'NONE', #39509, #35023, #4277, .T. ) ;
#53051=DIRECTION ( 'NONE',  ( -0.8660254037844435926, -0.4999999999999913403, 0.000000000000000000 ) ) ;
#53054=VECTOR ( 'NONE', #54094, 1000.000000000000114 ) ;
#53062=ORIENTED_EDGE ( 'NONE', *, *, #25621, .T. ) ;
#53071=VERTEX_POINT ( 'NONE', #37489 ) ;
#53087=EDGE_LOOP ( 'NONE', ( #7991, #63112, #51651, #45327 ) ) ;
#53096=DIRECTION ( 'NONE',  ( 1.053224967557347660E-14, 1.000000000000000000, 0.000000000000000000 ) ) ;
#53106=AXIS2_PLACEMENT_3D ( 'NONE', #30692, #42689, #46585 ) ;
#53108=SURFACE_SIDE_STYLE ('',( #15264 ) ) ;
#53110=CARTESIAN_POINT ( 'NONE',  ( -11.11351654964670743, 9.093516549646603053, 195.0000000000000284 ) ) ;
#53114=CARTESIAN_POINT ( 'NONE',  ( -5.993516549646711766, 8.198316549646602169, 455.0000000000000568 ) ) ;
#53119=ORIENTED_EDGE ( 'NONE', *, *, #49828, .F. ) ;
#53123=AXIS2_PLACEMENT_3D ( 'NONE', #38704, #19923, #25595 ) ;
#53138=EDGE_CURVE ( 'NONE', #31731, #60141, #18574, .T. ) ;
#53142=VERTEX_POINT ( 'NONE', #11969 ) ;
#53143=CARTESIAN_POINT ( 'NONE',  ( -5.380658396643233310, 7.252248008019342329, 195.0000000000000284 ) ) ;
#53146=EDGE_LOOP ( 'NONE', ( #3879, #69449, #13868, #44377 ) ) ;
#53155=CARTESIAN_POINT ( 'NONE',  ( 11.32648345035337734, -4.406483450353395170, 195.0000000000000284 ) ) ;
#53164=DIRECTION ( 'NONE',  ( -1.819560449471430698E-15, -1.000000000000000000, 0.000000000000000000 ) ) ;
#53174=VECTOR ( 'NONE', #13616, 1000.000000000000000 ) ;
#53176=CARTESIAN_POINT ( 'NONE',  ( -8.393516549646712122, 5.655420232009161552, 455.0000000000000568 ) ) ;
#53178=EDGE_LOOP ( 'NONE', ( #27926, #49887, #36897, #57367 ) ) ;
#53181=PLANE ( 'NONE',  #11050 ) ;
#53182=DIRECTION ( 'NONE',  ( 8.673617379884051249E-15, 1.000000000000000000, 0.000000000000000000 ) ) ;
#53186=LINE ( 'NONE', #4730, #18614 ) ;
#53193=FACE_BOUND ( 'NONE', #58991, .T. ) ;
#53206=VECTOR ( 'NONE', #8267, 1000.000000000000000 ) ;
#53207=CARTESIAN_POINT ( 'NONE',  ( 7.265214908726139065, 5.380658396643097419, 455.0000000000000568 ) ) ;
#53214=VECTOR ( 'NONE', #14489, 1000.000000000000114 ) ;
#53235=LINE ( 'NONE', #30948, #65707 ) ;
#53237=ORIENTED_EDGE ( 'NONE', *, *, #61679, .F. ) ;
#53247=DIRECTION ( 'NONE',  ( -1.047444401652940007E-14, -1.000000000000000000, -1.836970198721029934E-16 ) ) ;
#53253=VECTOR ( 'NONE', #37956, 1000.000000000000114 ) ;
#53266=AXIS2_PLACEMENT_3D ( 'NONE', #6077, #48514, #788 ) ;
#53269=PLANE ( 'NONE',  #52812 ) ;
#53272=DIRECTION ( 'NONE',  ( 0.000000000000000000, 1.000000000000000000, 0.000000000000000000 ) ) ;
#53277=DIRECTION ( 'NONE',  ( -1.000000000000000000, -2.135044278125301343E-15, 0.000000000000000000 ) ) ;
#53279=EDGE_CURVE ( 'NONE', #8459, #34152, #14069, .T. ) ;
#53286=DIRECTION ( 'NONE',  ( -1.920292680692490463E-14, -1.000000000000000000, -1.836970198721045958E-16 ) ) ;
#53291=DIRECTION ( 'NONE',  ( 1.000000000000000000, 0.000000000000000000, 0.000000000000000000 ) ) ;
#53306=ORIENTED_EDGE ( 'NONE', *, *, #37299, .F. ) ;
#53314=EDGE_LOOP ( 'NONE', ( #30533, #3805, #34205, #69041 ) ) ;
#53321=ORIENTED_EDGE ( 'NONE', *, *, #54240, .F. ) ;
#53326=AXIS2_PLACEMENT_3D ( 'NONE', #58045, #8901, #67961 ) ;
#53327=CARTESIAN_POINT ( 'NONE',  ( -11.47551654964678214, -11.08848345035328542, 195.0000000000000284 ) ) ;
#53336=ORIENTED_EDGE ( 'NONE', *, *, #65097, .T. ) ;
#53338=CYLINDRICAL_SURFACE ( 'NONE', #13635, 0.1999999999999987899 ) ;
#53340=VERTEX_POINT ( 'NONE', #36700 ) ;
#53353=ORIENTED_EDGE ( 'NONE', *, *, #13187, .F. ) ;
#53357=LINE ( 'NONE', #15867, #9866 ) ;
#53361=ORIENTED_EDGE ( 'NONE', *, *, #54622, .F. ) ;
#53364=CARTESIAN_POINT ( 'NONE',  ( 6.006483450353379716, -6.006483450353490738, 455.0000000000000568 ) ) ;
#53365=DIRECTION ( 'NONE',  ( -6.508391731846281342E-15, -1.000000000000000000, -1.836970198721024757E-16 ) ) ;
#53366=LINE ( 'NONE', #21185, #2857 ) ;
#53367=VERTEX_POINT ( 'NONE', #46948 ) ;
#53373=CIRCLE ( 'NONE', #38669, 0.4000000000000010214 ) ;
#53377=CARTESIAN_POINT ( 'NONE',  ( -4.609516549646752281, -3.606483450353441533, 455.0000000000000568 ) ) ;
#53385=AXIS2_PLACEMENT_3D ( 'NONE', #819, #22376, #60181 ) ;
#53388=DIRECTION ( 'NONE',  ( -0.7671651518153006499, -0.6414496315691565753, 0.000000000000000000 ) ) ;
#53392=VECTOR ( 'NONE', #42662, 1000.000000000000000 ) ;
#53411=ORIENTED_EDGE ( 'NONE', *, *, #8428, .T. ) ;
#53423=VERTEX_POINT ( 'NONE', #10869 ) ;
#53426=EDGE_CURVE ( 'NONE', #68804, #45972, #20301, .T. ) ;
#53428=DIRECTION ( 'NONE',  ( -0.000000000000000000, -0.000000000000000000, -1.000000000000000000 ) ) ;
#53430=VECTOR ( 'NONE', #1066, 1000.000000000000000 ) ;
#53434=ORIENTED_EDGE ( 'NONE', *, *, #24931, .F. ) ;
#53438=DIRECTION ( 'NONE',  ( 1.000000000000000000, 1.570596175624152290E-15, 5.770276737693577136E-31 ) ) ;
#53440=FACE_OUTER_BOUND ( 'NONE', #58714, .T. ) ;
#53443=CARTESIAN_POINT ( 'NONE',  ( -11.11351654964670921, 8.333516549646644123, 455.0000000000000568 ) ) ;
#53457=ORIENTED_EDGE ( 'NONE', *, *, #50225, .F. ) ;
#53458=LINE ( 'NONE', #25886, #38793 ) ;
#53461=EDGE_CURVE ( 'NONE', #35182, #47329, #31755, .T. ) ;
#53464=EDGE_CURVE ( 'NONE', #8621, #67098, #64616, .T. ) ;
#53465=EDGE_CURVE ( 'NONE', #64137, #68801, #21413, .T. ) ;
#53472=VECTOR ( 'NONE', #47014, 1000.000000000000000 ) ;
#53473=DIRECTION ( 'NONE',  ( 0.000000000000000000, 1.000000000000000000, 3.673940397442059868E-16 ) ) ;
#53476=AXIS2_PLACEMENT_3D ( 'NONE', #37588, #68718, #43225 ) ;
#53484=VERTEX_POINT ( 'NONE', #53327 ) ;
#53486=LINE ( 'NONE', #60503, #477 ) ;
#53488=DIRECTION ( 'NONE',  ( -1.000000000000000000, 0.000000000000000000, 0.000000000000000000 ) ) ;
#53492=VECTOR ( 'NONE', #66144, 1000.000000000000000 ) ;
#53493=ORIENTED_EDGE ( 'NONE', *, *, #53675, .F. ) ;
#53495=ORIENTED_EDGE ( 'NONE', *, *, #62513, .F. ) ;
#53504=AXIS2_PLACEMENT_3D ( 'NONE', #29517, #60987, #39083 ) ;
#53508=CARTESIAN_POINT ( 'NONE',  ( 1.090483450353338268, -11.34648345035335737, 195.0000000000000284 ) ) ;
#53523=EDGE_LOOP ( 'NONE', ( #39204, #28636, #28580, #21822 ) ) ;
#53528=EDGE_CURVE ( 'NONE', #18151, #62060, #58964, .T. ) ;
#53531=VECTOR ( 'NONE', #44236, 1000.000000000000000 ) ;
#53535=CARTESIAN_POINT ( 'NONE',  ( -9.093516549646828651, -11.12648345035338870, 455.0000000000000568 ) ) ;
#53542=LINE ( 'NONE', #31288, #5406 ) ;
#53550=ORIENTED_EDGE ( 'NONE', *, *, #2023, .T. ) ;
#53554=DIRECTION ( 'NONE',  ( -1.356437060717832013E-15, -1.000000000000000000, -1.836970198721033878E-16 ) ) ;
#53560=ORIENTED_EDGE ( 'NONE', *, *, #49773, .F. ) ;
#53564=AXIS2_PLACEMENT_3D ( 'NONE', #68786, #25669, #31667 ) ;
#53572=VECTOR ( 'NONE', #68745, 1000.000000000000000 ) ;
#53574=ORIENTED_EDGE ( 'NONE', *, *, #1996, .F. ) ;
#53578=DIRECTION ( 'NONE',  ( -1.047444401652940007E-14, -1.000000000000000000, -1.836970198721029934E-16 ) ) ;
#53585=VECTOR ( 'NONE', #68345, 1000.000000000000000 ) ;
#53586=DIRECTION ( 'NONE',  ( -1.836970198721029934E-16, 1.836970198721036344E-16, -1.000000000000000000 ) ) ;
#53587=ORIENTED_EDGE ( 'NONE', *, *, #60423, .T. ) ;
#53590=ORIENTED_EDGE ( 'NONE', *, *, #7721, .F. ) ;
#53594=EDGE_CURVE ( 'NONE', #43722, #8790, #7919, .T. ) ;
#53597=CARTESIAN_POINT ( 'NONE',  ( -4.173516549646666185, 11.99351654964658920, 455.0000000000000568 ) ) ;
#53604=EDGE_CURVE ( 'NONE', #14259, #938, #19131, .T. ) ;
#53611=VECTOR ( 'NONE', #10014, 1000.000000000000000 ) ;
#53613=CARTESIAN_POINT ( 'NONE',  ( 11.48848345035334617, -11.08848345035349148, 455.0000000000000568 ) ) ;
#53615=CYLINDRICAL_SURFACE ( 'NONE', #67433, 0.2000000000000005107 ) ;
#53616=EDGE_CURVE ( 'NONE', #10422, #11140, #41150, .T. ) ;
#53620=VECTOR ( 'NONE', #65566, 1000.000000000000000 ) ;
#53625=CARTESIAN_POINT ( 'NONE',  ( 3.606483450353402009, 5.993516549646589198, 455.0000000000000568 ) ) ;
#53626=PLANE ( 'NONE',  #67269 ) ;
#53627=ADVANCED_FACE ( 'NONE', ( #30206 ), #51772, .F. ) ;
#53633=DIRECTION ( 'NONE',  ( 0.7071067811865529018, 0.7071067811865422437, 0.000000000000000000 ) ) ;
#53636=DIRECTION ( 'NONE',  ( 0.000000000000000000, 1.000000000000000000, 0.000000000000000000 ) ) ;
#53646=ORIENTED_EDGE ( 'NONE', *, *, #46835, .F. ) ;
#53662=AXIS2_PLACEMENT_3D ( 'NONE', #4627, #43132, #16267 ) ;
#53669=EDGE_LOOP ( 'NONE', ( #41436, #38992, #10024, #1470 ) ) ;
#53670=EDGE_CURVE ( 'NONE', #64892, #34655, #19941, .T. ) ;
#53675=EDGE_CURVE ( 'NONE', #41573, #60909, #56718, .T. ) ;
#53676=ADVANCED_FACE ( 'NONE', ( #25612 ), #68031, .F. ) ;
#53679=ORIENTED_EDGE ( 'NONE', *, *, #31093, .T. ) ;
#53682=DIRECTION ( 'NONE',  ( -0.000000000000000000, -0.000000000000000000, -1.000000000000000000 ) ) ;
#53687=ORIENTED_EDGE ( 'NONE', *, *, #120, .T. ) ;
#53702=DIRECTION ( 'NONE',  ( -1.836970198721029934E-16, 1.836970198721036344E-16, -1.000000000000000000 ) ) ;
#53706=CYLINDRICAL_SURFACE ( 'NONE', #61621, 0.6000000000000007550 ) ;
#53707=DIRECTION ( 'NONE',  ( -0.000000000000000000, -0.000000000000000000, -1.000000000000000000 ) ) ;
#53708=ORIENTED_EDGE ( 'NONE', *, *, #19900, .F. ) ;
#53712=VECTOR ( 'NONE', #5239, 1000.000000000000114 ) ;
#53718=AXIS2_PLACEMENT_3D ( 'NONE', #1894, #11794, #65891 ) ;
#53725=DIRECTION ( 'NONE',  ( -1.000000000000000000, 0.000000000000000000, 0.000000000000000000 ) ) ;
#53728=CARTESIAN_POINT ( 'NONE',  ( -7.798499376344067535, 7.259684009079840017, 195.0000000000000284 ) ) ;
#53746=LINE ( 'NONE', #30775, #34935 ) ;
#53748=CARTESIAN_POINT ( 'NONE',  ( -7.793516549646712477, 11.11351654964660085, 455.0000000000000568 ) ) ;
#53758=VECTOR ( 'NONE', #24594, 1000.000000000000000 ) ;
#53766=AXIS2_PLACEMENT_3D ( 'NONE', #52580, #4143, #4490 ) ;
#53769=ADVANCED_FACE ( 'NONE', ( #11081 ), #38307, .F. ) ;
#53770=VERTEX_POINT ( 'NONE', #26298 ) ;
#53790=CARTESIAN_POINT ( 'NONE',  ( -11.11351654964671098, 7.793516549646603231, 455.0000000000000568 ) ) ;
#53792=DIRECTION ( 'NONE',  ( -1.000000000000000000, -0.000000000000000000, -0.000000000000000000 ) ) ;
#53796=FACE_OUTER_BOUND ( 'NONE', #53087, .T. ) ;
#53803=LINE ( 'NONE', #53114, #18253 ) ;
#53805=EDGE_CURVE ( 'NONE', #35336, #59438, #65529, .T. ) ;
#53810=EDGE_CURVE ( 'NONE', #15525, #48685, #15341, .T. ) ;
#53824=LINE ( 'NONE', #31213, #21208 ) ;
#53825=AXIS2_PLACEMENT_3D ( 'NONE', #29492, #24195, #45751 ) ;
#53831=ORIENTED_EDGE ( 'NONE', *, *, #65655, .F. ) ;
#53832=ORIENTED_EDGE ( 'NONE', *, *, #50732, .T. ) ;
#53835=ORIENTED_EDGE ( 'NONE', *, *, #20253, .F. ) ;
#53836=VECTOR ( 'NONE', #14289, 1000.000000000000000 ) ;
#53842=DIRECTION ( 'NONE',  ( -0.000000000000000000, 3.673940397442059868E-16, -1.000000000000000000 ) ) ;
#53846=ORIENTED_EDGE ( 'NONE', *, *, #16379, .F. ) ;
#53852=FACE_OUTER_BOUND ( 'NONE', #9801, .T. ) ;
#53855=ORIENTED_EDGE ( 'NONE', *, *, #33129, .T. ) ;
#53860=DIRECTION ( 'NONE',  ( -1.836970198721029934E-16, 1.836970198721036344E-16, -1.000000000000000000 ) ) ;
#53868=CYLINDRICAL_SURFACE ( 'NONE', #18098, 1.399999999999999245 ) ;
#53874=CIRCLE ( 'NONE', #15448, 0.2000000000000005107 ) ;
#53883=CARTESIAN_POINT ( 'NONE',  ( 11.34648345035334671, 1.077516549646521327, 455.0000000000000568 ) ) ;
#53887=ORIENTED_EDGE ( 'NONE', *, *, #59527, .F. ) ;
#53891=DIRECTION ( 'NONE',  ( 1.836970198721029934E-16, 1.836970198721010706E-16, -1.000000000000000000 ) ) ;
#53893=DIRECTION ( 'NONE',  ( 1.836970198721029934E-16, 1.836970198721010706E-16, -1.000000000000000000 ) ) ;
#53896=ORIENTED_EDGE ( 'NONE', *, *, #64407, .F. ) ;
#53917=VECTOR ( 'NONE', #42928, 1000.000000000000000 ) ;
#53918=CIRCLE ( 'NONE', #1952, 0.1999999999999996503 ) ;
#53919=PLANE ( 'NONE',  #5650 ) ;
#53920=EDGE_LOOP ( 'NONE', ( #47030, #27123, #45699, #66674 ) ) ;
#53926=PLANE ( 'NONE',  #6260 ) ;
#53927=CARTESIAN_POINT ( 'NONE',  ( 9.955011587777235604, -2.765062094116182312, 455.0000000000000568 ) ) ;
#53933=LINE ( 'NONE', #65239, #54106 ) ;
#53934=DIRECTION ( 'NONE',  ( 0.000000000000000000, 0.000000000000000000, 1.000000000000000000 ) ) ;
#53939=CARTESIAN_POINT ( 'NONE',  ( -10.73351654964669599, -1.690483450353341910, 455.0000000000000568 ) ) ;
#53946=DIRECTION ( 'NONE',  ( -1.000000000000000000, 0.000000000000000000, 0.000000000000000000 ) ) ;
#53957=CARTESIAN_POINT ( 'NONE',  ( 11.78648345035340661, 7.593516549646560421, 455.0000000000000568 ) ) ;
#53965=FACE_OUTER_BOUND ( 'NONE', #32526, .T. ) ;
#53968=CYLINDRICAL_SURFACE ( 'NONE', #9366, 0.1999999999999987899 ) ;
#53988=DIRECTION ( 'NONE',  ( -1.836970198721029934E-16, 1.836970198721036344E-16, -1.000000000000000000 ) ) ;
#53992=CARTESIAN_POINT ( 'NONE',  ( 9.955011587777235604, -2.765062094116182312, 455.0000000000000568 ) ) ;
#53995=CYLINDRICAL_SURFACE ( 'NONE', #39440, 0.5999999999999998668 ) ;
#54006=ADVANCED_FACE ( 'NONE', ( #44974 ), #66545, .T. ) ;
#54011=ORIENTED_EDGE ( 'NONE', *, *, #40317, .F. ) ;
#54012=FACE_OUTER_BOUND ( 'NONE', #35383, .T. ) ;
#54016=CARTESIAN_POINT ( 'NONE',  ( -4.383466043307859827, 8.393516549646589553, 455.0000000000000568 ) ) ;
#54020=CARTESIAN_POINT ( 'NONE',  ( 6.006483450353379716, -6.006483450353490738, 455.0000000000000568 ) ) ;
#54023=CARTESIAN_POINT ( 'NONE',  ( -8.593516549646697200, -4.396432944014498467, 195.0000000000000284 ) ) ;
#54027=PRODUCT_CONTEXT ( 'NONE', #28643, 'mechanical' ) ;
#54031=DIRECTION ( 'NONE',  ( -1.000000000000000000, 0.000000000000000000, 0.000000000000000000 ) ) ;
#54037=ORIENTED_EDGE ( 'NONE', *, *, #55732, .F. ) ;
#54042=DIRECTION ( 'NONE',  ( -0.000000000000000000, 3.673940397442059868E-16, -1.000000000000000000 ) ) ;
#54061=LINE ( 'NONE', #5956, #55057 ) ;
#54081=CARTESIAN_POINT ( 'NONE',  ( -4.727349090213463612, 7.798499376343949407, 455.0000000000000568 ) ) ;
#54082=ORIENTED_EDGE ( 'NONE', *, *, #54841, .T. ) ;
#54083=DIRECTION ( 'NONE',  ( 3.614007241618349165E-15, 1.000000000000000000, 0.000000000000000000 ) ) ;
#54086=EDGE_CURVE ( 'NONE', #35382, #26427, #25522, .T. ) ;
#54091=CARTESIAN_POINT ( 'NONE',  ( -8.393516549646712122, 5.655420232009161552, 455.0000000000000568 ) ) ;
#54094=DIRECTION ( 'NONE',  ( 0.7071067811865474617, 0.7071067811865474617, 2.597868168706479611E-16 ) ) ;
#54097=ORIENTED_EDGE ( 'NONE', *, *, #60291, .T. ) ;
#54098=DIRECTION ( 'NONE',  ( 1.000000000000000000, -3.491481338843133750E-15, -1.836970198721036590E-16 ) ) ;
#54106=VECTOR ( 'NONE', #43990, 1000.000000000000000 ) ;
#54108=EDGE_CURVE ( 'NONE', #28277, #56701, #51693, .T. ) ;
#54125=CIRCLE ( 'NONE', #69908, 2.204799999999997429 ) ;
#54128=DIRECTION ( 'NONE',  ( -0.000000000000000000, 0.000000000000000000, -1.000000000000000000 ) ) ;
#54132=EDGE_LOOP ( 'NONE', ( #53321, #62261, #3580, #39803 ) ) ;
#54137=CARTESIAN_POINT ( 'NONE',  ( -11.29351654964668583, 8.513516549646642062, 455.0000000000000568 ) ) ;
#54143=VERTEX_POINT ( 'NONE', #67246 ) ;
#54151=ORIENTED_EDGE ( 'NONE', *, *, #66098, .T. ) ;
#54152=PLANE ( 'NONE',  #57991 ) ;
#54184=CARTESIAN_POINT ( 'NONE',  ( -9.791916549646712653, 10.19191654964664018, 455.0000000000000568 ) ) ;
#54190=CARTESIAN_POINT ( 'NONE',  ( 11.32648345035337734, -7.806483450353395526, 195.0000000000000284 ) ) ;
#54198=CIRCLE ( 'NONE', #23675, 1.399999999999999245 ) ;
#54203=EDGE_CURVE ( 'NONE', #37838, #51193, #59436, .T. ) ;
#54204=DIRECTION ( 'NONE',  ( -1.000000000000000000, 2.135044278125299371E-15, 0.000000000000000000 ) ) ;
#54205=LINE ( 'NONE', #812, #423 ) ;
#54208=ORIENTED_EDGE ( 'NONE', *, *, #14695, .T. ) ;
#54209=ORIENTED_EDGE ( 'NONE', *, *, #41518, .T. ) ;
#54215=FACE_OUTER_BOUND ( 'NONE', #3841, .T. ) ;
#54219=AXIS2_PLACEMENT_3D ( 'NONE', #66023, #650, #48741 ) ;
#54220=CARTESIAN_POINT ( 'NONE',  ( -10.08346604330797369, -9.106483450353383802, 455.0000000000000568 ) ) ;
#54222=DIRECTION ( 'NONE',  ( 0.6414496315691565753, -0.7671651518153006499, -2.818519042764004597E-16 ) ) ;
#54225=DIRECTION ( 'NONE',  ( -1.836970198721029934E-16, -1.836970198721010706E-16, 1.000000000000000000 ) ) ;
#54229=AXIS2_PLACEMENT_3D ( 'NONE', #36488, #42140, #58062 ) ;
#54240=EDGE_CURVE ( 'NONE', #15827, #8176, #10303, .T. ) ;
#54252=CARTESIAN_POINT ( 'NONE',  ( 7.428221114745003462, -3.606483450353490827, 455.0000000000000568 ) ) ;
#54255=ORIENTED_EDGE ( 'NONE', *, *, #39808, .F. ) ;
#54256=AXIS2_PLACEMENT_3D ( 'NONE', #10284, #53428, #4979 ) ;
#54258=EDGE_LOOP ( 'NONE', ( #25197, #8694, #45483, #2892 ) ) ;
#54260=AXIS2_PLACEMENT_3D ( 'NONE', #45429, #41178, #18562 ) ;
#54267=DIRECTION ( 'NONE',  ( -2.135044278125299371E-15, 1.000000000000000000, -0.000000000000000000 ) ) ;
#54272=AXIS2_PLACEMENT_3D ( 'NONE', #33662, #29047, #49919 ) ;
#54277=EDGE_LOOP ( 'NONE', ( #62273, #27991, #62923, #44067 ) ) ;
#54282=VERTEX_POINT ( 'NONE', #32215 ) ;
#54297=EDGE_CURVE ( 'NONE', #41637, #53484, #37185, .T. ) ;
#54298=VECTOR ( 'NONE', #27766, 1000.000000000000000 ) ;
#54301=DIRECTION ( 'NONE',  ( -0.000000000000000000, 3.673940397442059868E-16, -1.000000000000000000 ) ) ;
#54302=VECTOR ( 'NONE', #28275, 1000.000000000000000 ) ;
#54303=DIRECTION ( 'NONE',  ( 0.000000000000000000, 0.000000000000000000, -1.000000000000000000 ) ) ;
#54308=DIRECTION ( 'NONE',  ( 1.000000000000000000, -1.047444401652940164E-14, 0.000000000000000000 ) ) ;
#54316=VECTOR ( 'NONE', #56321, 1000.000000000000000 ) ;
#54328=CYLINDRICAL_SURFACE ( 'NONE', #51312, 0.1999999999999992339 ) ;
#54335=EDGE_CURVE ( 'NONE', #8176, #20324, #7960, .T. ) ;
#54336=FACE_OUTER_BOUND ( 'NONE', #20256, .T. ) ;
#54340=CYLINDRICAL_SURFACE ( 'NONE', #69938, 0.1999999999999987899 ) ;
#54346=EDGE_LOOP ( 'NONE', ( #14497, #63315, #58712, #51007 ) ) ;
#54369=DIRECTION ( 'NONE',  ( 0.6414496315691469164, -0.7671651518153088656, -2.587583378555128790E-16 ) ) ;
#54370=ORIENTED_EDGE ( 'NONE', *, *, #54086, .T. ) ;
#54373=CARTESIAN_POINT ( 'NONE',  ( -8.693516549646711056, 11.11351654964659730, 455.0000000000000568 ) ) ;
#54381=ORIENTED_EDGE ( 'NONE', *, *, #57084, .F. ) ;
#54387=VERTEX_POINT ( 'NONE', #49855 ) ;
#54390=CARTESIAN_POINT ( 'NONE',  ( -11.29351654964668583, 8.513516549646642062, 195.0000000000000284 ) ) ;
#54397=ORIENTED_EDGE ( 'NONE', *, *, #35120, .F. ) ;
#54399=DIRECTION ( 'NONE',  ( -1.000000000000000000, 0.000000000000000000, 0.000000000000000000 ) ) ;
#54418=CARTESIAN_POINT ( 'NONE',  ( 4.186483450353337687, -11.78648345035347589, 455.0000000000000568 ) ) ;
#54431=LINE ( 'NONE', #41486, #23104 ) ;
#54432=CARTESIAN_POINT ( 'NONE',  ( -8.393516549646722780, -5.668387132715892562, 195.0000000000000284 ) ) ;
#54438=CARTESIAN_POINT ( 'NONE',  ( 9.955011587777235604, -2.765062094116086833, 195.0000000000000284 ) ) ;
#54443=LINE ( 'NONE', #65054, #41383 ) ;
#54445=CARTESIAN_POINT ( 'NONE',  ( 11.08848345035334404, -9.804883450353433005, 195.0000000000000284 ) ) ;
#54451=ORIENTED_EDGE ( 'NONE', *, *, #50409, .T. ) ;
#54461=CARTESIAN_POINT ( 'NONE',  ( 7.272650909786598561, -4.201500623656122535, 455.0000000000000568 ) ) ;
#54469=DIRECTION ( 'NONE',  ( -0.000000000000000000, 3.673940397442059868E-16, -1.000000000000000000 ) ) ;
#54474=LINE ( 'NONE', #21936, #23800 ) ;
#54475=EDGE_CURVE ( 'NONE', #23831, #52876, #57249, .T. ) ;
#54477=ORIENTED_EDGE ( 'NONE', *, *, #32612, .T. ) ;
#54479=ORIENTED_EDGE ( 'NONE', *, *, #57962, .F. ) ;
#54490=ORIENTED_EDGE ( 'NONE', *, *, #1712, .F. ) ;
#54500=CARTESIAN_POINT ( 'NONE',  ( 10.20488345035345290, 9.791916549646566992, 455.0000000000000568 ) ) ;
#54501=CARTESIAN_POINT ( 'NONE',  ( 11.12648345035337627, -9.106483450353492159, 455.0000000000000568 ) ) ;
#54504=CYLINDRICAL_SURFACE ( 'NONE', #31205, 0.2000000000000005107 ) ;
#54509=LINE ( 'NONE', #6062, #19170 ) ;
#54513=EDGE_LOOP ( 'NONE', ( #13278, #43532, #17208, #44561 ) ) ;
#54514=VERTEX_POINT ( 'NONE', #51603 ) ;
#54524=DIRECTION ( 'NONE',  ( -0.000000000000000000, -0.000000000000000000, -1.000000000000000000 ) ) ;
#54530=DIRECTION ( 'NONE',  ( -1.836970198721029934E-16, 1.836970198721036344E-16, -1.000000000000000000 ) ) ;
#54539=AXIS2_PLACEMENT_3D ( 'NONE', #3513, #25427, #40977 ) ;
#54544=EDGE_LOOP ( 'NONE', ( #39758, #31438, #57300, #50516 ) ) ;
#54548=CARTESIAN_POINT ( 'NONE',  ( -11.99351654964679526, -7.826483450353362237, 455.0000000000000568 ) ) ;
#54550=DIRECTION ( 'NONE',  ( -3.717264591378874374E-15, -1.000000000000000000, 0.000000000000000000 ) ) ;
#54554=EDGE_LOOP ( 'NONE', ( #46526, #10142, #58454, #25916 ) ) ;
#54565=ORIENTED_EDGE ( 'NONE', *, *, #24968, .T. ) ;
#54568=CARTESIAN_POINT ( 'NONE',  ( -5.993516549646711766, 5.993516549646603409, 455.0000000000000568 ) ) ;
#54569=CARTESIAN_POINT ( 'NONE',  ( 11.34648345035330053, 1.077516549646569066, 195.0000000000000284 ) ) ;
#54578=CARTESIAN_POINT ( 'NONE',  ( -4.173516549646837603, -11.78648345035344214, 455.0000000000000568 ) ) ;
#54580=CARTESIAN_POINT ( 'NONE',  ( 9.417013320880721849, 1.853252480934663771, 195.0000000000000284 ) ) ;
#54589=EDGE_CURVE ( 'NONE', #51166, #49441, #32870, .T. ) ;
#54594=ORIENTED_EDGE ( 'NONE', *, *, #3862, .F. ) ;
#54598=CARTESIAN_POINT ( 'NONE',  ( 11.12648345035340647, 7.793516549646564151, 455.0000000000000568 ) ) ;
#54622=EDGE_CURVE ( 'NONE', #35173, #40737, #27229, .T. ) ;
#54628=CIRCLE ( 'NONE', #2511, 0.1999999999999987899 ) ;
#54639=EDGE_CURVE ( 'NONE', #28757, #55545, #15917, .T. ) ;
#54662=CIRCLE ( 'NONE', #24165, 0.5999999999999998668 ) ;
#54671=DIRECTION ( 'NONE',  ( -1.053224967557347660E-14, -1.000000000000000000, 0.000000000000000000 ) ) ;
#54674=VECTOR ( 'NONE', #54301, 1000.000000000000000 ) ;
#54675=CARTESIAN_POINT ( 'NONE',  ( 10.09643294401454661, -2.906483450353491094, 455.0000000000000568 ) ) ;
#54677=DIRECTION ( 'NONE',  ( -1.836970198721029934E-16, 1.836970198721036344E-16, -1.000000000000000000 ) ) ;
#54679=VECTOR ( 'NONE', #14512, 1000.000000000000000 ) ;
#54689=LINE ( 'NONE', #49718, #36379 ) ;
#54700=VERTEX_POINT ( 'NONE', #10555 ) ;
#54702=CARTESIAN_POINT ( 'NONE',  ( 11.19368345035340440, 11.18071654964654904, 455.0000000000000568 ) ) ;
#54705=ORIENTED_EDGE ( 'NONE', *, *, #45179, .F. ) ;
#54709=FACE_OUTER_BOUND ( 'NONE', #50961, .T. ) ;
#54715=DIRECTION ( 'NONE',  ( -0.000000000000000000, 1.000000000000000000, -0.000000000000000000 ) ) ;
#54718=EDGE_CURVE ( 'NONE', #29457, #60260, #1266, .T. ) ;
#54725=CARTESIAN_POINT ( 'NONE',  ( -11.11351654964669500, -4.206483450353289300, 195.0000000000000284 ) ) ;
#54726=EDGE_CURVE ( 'NONE', #65820, #19320, #24938, .T. ) ;
#54728=ADVANCED_FACE ( 'NONE', ( #39492 ), #12611, .F. ) ;
#54730=FACE_OUTER_BOUND ( 'NONE', #39272, .T. ) ;
#54736=CARTESIAN_POINT ( 'NONE',  ( 4.201500623656052369, 4.727349090213339267, 455.0000000000000568 ) ) ;
#54739=LINE ( 'NONE', #60365, #65824 ) ;
#54742=CARTESIAN_POINT ( 'NONE',  ( 3.006483450353369502, -7.428221114745093168, 455.0000000000000568 ) ) ;
#54744=DIRECTION ( 'NONE',  ( 0.000000000000000000, -3.673940397442059868E-16, 1.000000000000000000 ) ) ;
#54746=DIRECTION ( 'NONE',  ( 1.836970198721029934E-16, 1.836970198721010706E-16, -1.000000000000000000 ) ) ;
#54752=VECTOR ( 'NONE', #69430, 1000.000000000000000 ) ;
#54756=CARTESIAN_POINT ( 'NONE',  ( -9.404046420174113408, -1.866219381641437636, 455.0000000000000568 ) ) ;
#54772=CARTESIAN_POINT ( 'NONE',  ( -5.993516549646751734, -8.211283450353379365, 195.0000000000000284 ) ) ;
#54775=DIRECTION ( 'NONE',  ( -7.457533623526253657E-15, -1.000000000000000000, -1.836970198721024757E-16 ) ) ;
#54779=LINE ( 'NONE', #27910, #23417 ) ;
#54785=CARTESIAN_POINT ( 'NONE',  ( -7.798499376344157241, -7.272650909786626983, 455.0000000000000568 ) ) ;
#54787=LINE ( 'NONE', #54445, #8407 ) ;
#54799=LINE ( 'NONE', #54461, #39149 ) ;
#54801=CIRCLE ( 'NONE', #17486, 0.1999999999999987899 ) ;
#54803=DIRECTION ( 'NONE',  ( -1.000000000000000000, 6.308085367188447236E-15, 0.000000000000000000 ) ) ;
#54813=DIRECTION ( 'NONE',  ( -0.6414496315691494699, -0.7671651518153064231, 0.000000000000000000 ) ) ;
#54817=DIRECTION ( 'NONE',  ( -0.7671651518153106419, -0.6414496315691445849, 0.000000000000000000 ) ) ;
#54821=AXIS2_PLACEMENT_3D ( 'NONE', #27039, #47899, #69474 ) ;
#54829=VERTEX_POINT ( 'NONE', #11921 ) ;
#54834=ORIENTED_EDGE ( 'NONE', *, *, #68755, .T. ) ;
#54836=DIRECTION ( 'NONE',  ( 1.836970198721029934E-16, -1.836970198721036344E-16, 1.000000000000000000 ) ) ;
#54840=VERTEX_POINT ( 'NONE', #28202 ) ;
#54841=EDGE_CURVE ( 'NONE', #4035, #58797, #5777, .T. ) ;
#54847=LINE ( 'NONE', #49538, #13926 ) ;
#54850=VERTEX_POINT ( 'NONE', #11239 ) ;
#54858=CARTESIAN_POINT ( 'NONE',  ( -4.188533722949370208, -4.740315990920148437, 195.0000000000000284 ) ) ;
#54865=VERTEX_POINT ( 'NONE', #52128 ) ;
#54870=DIRECTION ( 'NONE',  ( 0.000000000000000000, -1.000000000000000000, -3.673940397442059868E-16 ) ) ;
#54881=DIRECTION ( 'NONE',  ( 1.000000000000000000, 0.000000000000000000, 0.000000000000000000 ) ) ;
#54883=EDGE_CURVE ( 'NONE', #13109, #17390, #36208, .T. ) ;
#54892=AXIS2_PLACEMENT_3D ( 'NONE', #55445, #33526, #50128 ) ;
#54898=FACE_OUTER_BOUND ( 'NONE', #32581, .T. ) ;
#54908=DIRECTION ( 'NONE',  ( 1.836970198721029934E-16, 1.836970198721010706E-16, -1.000000000000000000 ) ) ;
#54923=ORIENTED_EDGE ( 'NONE', *, *, #46290, .T. ) ;
#54942=ORIENTED_EDGE ( 'NONE', *, *, #33238, .T. ) ;
#54946=ORIENTED_EDGE ( 'NONE', *, *, #6405, .F. ) ;
#54950=CARTESIAN_POINT ( 'NONE',  ( 4.186483450353337687, -11.78648345035337996, 195.0000000000000284 ) ) ;
#54951=EDGE_CURVE ( 'NONE', #48961, #53340, #25261, .T. ) ;
#54958=ORIENTED_EDGE ( 'NONE', *, *, #39358, .F. ) ;
#54967=EDGE_LOOP ( 'NONE', ( #34640, #34733, #48234, #57580 ) ) ;
#54972=ORIENTED_EDGE ( 'NONE', *, *, #41350, .T. ) ;
#54978=AXIS2_PLACEMENT_3D ( 'NONE', #13025, #50530, #2087 ) ;
#54983=AXIS2_PLACEMENT_3D ( 'NONE', #4317, #42472, #36835 ) ;
#54986=ORIENTED_EDGE ( 'NONE', *, *, #10969, .T. ) ;
#54999=ADVANCED_FACE ( 'NONE', ( #11089 ), #64161, .F. ) ;
#55000=ORIENTED_EDGE ( 'NONE', *, *, #674, .T. ) ;
#55004=ORIENTED_EDGE ( 'NONE', *, *, #11393, .F. ) ;
#55009=AXIS2_PLACEMENT_3D ( 'NONE', #66470, #19078, #61495 ) ;
#55010=ORIENTED_EDGE ( 'NONE', *, *, #50558, .F. ) ;
#55016=DIRECTION ( 'NONE',  ( -1.000000000000000000, 6.308085367188447236E-15, 0.000000000000000000 ) ) ;
#55024=VERTEX_POINT ( 'NONE', #27695 ) ;
#55025=CARTESIAN_POINT ( 'NONE',  ( -7.813516549646789322, -11.78648345035335865, 195.0000000000000284 ) ) ;
#55026=DIRECTION ( 'NONE',  ( 7.665540703601096574E-15, 1.000000000000000000, -0.000000000000000000 ) ) ;
#55027=AXIS2_PLACEMENT_3D ( 'NONE', #41595, #9073, #30640 ) ;
#55036=FACE_OUTER_BOUND ( 'NONE', #68352, .T. ) ;
#55043=EDGE_CURVE ( 'NONE', #27624, #35699, #15705, .T. ) ;
#55044=DIRECTION ( 'NONE',  ( -1.836970198721029934E-16, 1.836970198721036344E-16, -1.000000000000000000 ) ) ;
#55045=CARTESIAN_POINT ( 'NONE',  ( 4.406483450353335662, -11.78648345035347766, 455.0000000000000568 ) ) ;
#55048=ORIENTED_EDGE ( 'NONE', *, *, #25417, .F. ) ;
#55052=DIRECTION ( 'NONE',  ( -0.000000000000000000, -0.000000000000000000, -1.000000000000000000 ) ) ;
#55056=DIRECTION ( 'NONE',  ( 0.000000000000000000, 1.000000000000000000, 0.000000000000000000 ) ) ;
#55057=VECTOR ( 'NONE', #27523, 1000.000000000000000 ) ;
#55061=CARTESIAN_POINT ( 'NONE',  ( -1.677516549646676625, 10.73351654964656987, 455.0000000000000568 ) ) ;
#55067=CARTESIAN_POINT ( 'NONE',  ( 7.616533956692244089, 8.393516549646575342, 455.0000000000000568 ) ) ;
#55077=EDGE_CURVE ( 'NONE', #4323, #52471, #850, .T. ) ;
#55090=FACE_OUTER_BOUND ( 'NONE', #34678, .T. ) ;
#55091=CARTESIAN_POINT ( 'NONE',  ( -11.31351654964679021, -7.806483450353372433, 455.0000000000000568 ) ) ;
#55092=DIRECTION ( 'NONE',  ( -1.836970198721029934E-16, 1.836970198721036344E-16, -1.000000000000000000 ) ) ;
#55098=CARTESIAN_POINT ( 'NONE',  ( 2.290483450353350658, -9.841277389592708147, 195.0000000000000284 ) ) ;
#55102=ORIENTED_EDGE ( 'NONE', *, *, #47143, .T. ) ;
#55109=DIRECTION ( 'NONE',  ( -0.7671651518153087546, -0.6414496315691469164, 2.309356642089053889E-17 ) ) ;
#55111=EDGE_CURVE ( 'NONE', #19113, #62883, #3548, .T. ) ;
#55114=EDGE_CURVE ( 'NONE', #22946, #8396, #33003, .T. ) ;
#55116=ADVANCED_FACE ( 'NONE', ( #4746 ), #49276, .T. ) ;
#55118=CARTESIAN_POINT ( 'NONE',  ( 4.396432944014527777, -8.406483450353384512, 195.0000000000000284 ) ) ;
#55139=LINE ( 'NONE', #13014, #48955 ) ;
#55141=ORIENTED_EDGE ( 'NONE', *, *, #6936, .T. ) ;
#55147=PLANE ( 'NONE',  #54978 ) ;
#55155=AXIS2_PLACEMENT_3D ( 'NONE', #39364, #55979, #55629 ) ;
#55159=CARTESIAN_POINT ( 'NONE',  ( 4.396432944014526889, -8.606483450353382025, 195.0000000000000284 ) ) ;
#55167=CARTESIAN_POINT ( 'NONE',  ( 7.826483450353421745, 11.77351654964657257, 455.0000000000000568 ) ) ;
#55170=ADVANCED_FACE ( 'NONE', ( #39674 ), #17777, .T. ) ;
#55187=FACE_OUTER_BOUND ( 'NONE', #68090, .T. ) ;
#55190=VERTEX_POINT ( 'NONE', #17423 ) ;
#55193=VERTEX_POINT ( 'NONE', #11764 ) ;
#55208=AXIS2_PLACEMENT_3D ( 'NONE', #11373, #32610, #49554 ) ;
#55231=LINE ( 'NONE', #17743, #42207 ) ;
#55232=DIRECTION ( 'NONE',  ( 1.000000000000000000, -2.309061475090597584E-14, 1.836970198720987533E-16 ) ) ;
#55234=EDGE_CURVE ( 'NONE', #26006, #42528, #23771, .T. ) ;
#55237=CARTESIAN_POINT ( 'NONE',  ( 9.106483450353415776, 10.08346604330773744, 455.0000000000000568 ) ) ;
#55242=ORIENTED_EDGE ( 'NONE', *, *, #51590, .T. ) ;
#55245=DIRECTION ( 'NONE',  ( -0.000000000000000000, 3.673940397442059868E-16, -1.000000000000000000 ) ) ;
#55248=DIRECTION ( 'NONE',  ( 0.000000000000000000, -3.673940397442059868E-16, 1.000000000000000000 ) ) ;
#55253=DIRECTION ( 'NONE',  ( 0.000000000000000000, 0.000000000000000000, 1.000000000000000000 ) ) ;
#55269=ORIENTED_EDGE ( 'NONE', *, *, #10867, .F. ) ;
#55277=DIRECTION ( 'NONE',  ( 0.000000000000000000, 3.673940397442059868E-16, -1.000000000000000000 ) ) ;
#55279=ORIENTED_EDGE ( 'NONE', *, *, #20762, .F. ) ;
#55290=ORIENTED_EDGE ( 'NONE', *, *, #6487, .T. ) ;
#55299=ORIENTED_EDGE ( 'NONE', *, *, #26051, .T. ) ;
#55304=ORIENTED_EDGE ( 'NONE', *, *, #17695, .F. ) ;
#55307=CARTESIAN_POINT ( 'NONE',  ( -9.293516549646779978, -10.92648345035333790, 195.0000000000000284 ) ) ;
#55310=CARTESIAN_POINT ( 'NONE',  ( -7.259684009079930611, 4.188533722949235205, 195.0000000000000284 ) ) ;
#55319=ORIENTED_EDGE ( 'NONE', *, *, #20762, .T. ) ;
#55321=EDGE_CURVE ( 'NONE', #64507, #40247, #48772, .T. ) ;
#55325=CARTESIAN_POINT ( 'NONE',  ( 11.78648345035335865, 7.813516549646607245, 195.0000000000000284 ) ) ;
#55326=ORIENTED_EDGE ( 'NONE', *, *, #68697, .T. ) ;
#55348=DIRECTION ( 'NONE',  ( 1.156482317317870187E-14, 1.000000000000000000, 0.000000000000000000 ) ) ;
#55355=DIRECTION ( 'NONE',  ( -9.973078850062113474E-15, -1.000000000000000000, 0.000000000000000000 ) ) ;
#55356=VECTOR ( 'NONE', #1601, 1000.000000000000114 ) ;
#55372=EDGE_CURVE ( 'NONE', #38597, #37495, #58915, .T. ) ;
#55380=AXIS2_PLACEMENT_3D ( 'NONE', #54702, #27477, #65656 ) ;
#55385=VERTEX_POINT ( 'NONE', #64749 ) ;
#55398=AXIS2_PLACEMENT_3D ( 'NONE', #64057, #43158, #53096 ) ;
#55400=DIRECTION ( 'NONE',  ( -0.6414496315691645689, -0.7671651518152939886, -2.587583378555115478E-16 ) ) ;
#55401=AXIS2_PLACEMENT_3D ( 'NONE', #17665, #60440, #27933 ) ;
#55402=CARTESIAN_POINT ( 'NONE',  ( -1.677516549646676625, 10.73351654964656987, 455.0000000000000568 ) ) ;
#55410=EDGE_CURVE ( 'NONE', #5119, #37252, #53803, .T. ) ;
#55417=EDGE_CURVE ( 'NONE', #5044, #8876, #42127, .T. ) ;
#55422=CARTESIAN_POINT ( 'NONE',  ( 9.106483450353415776, 10.08346604330773744, 455.0000000000000568 ) ) ;
#55430=DIRECTION ( 'NONE',  ( 0.000000000000000000, 3.673940397442059868E-16, -1.000000000000000000 ) ) ;
#55434=DIRECTION ( 'NONE',  ( 7.304098846218132892E-15, 1.000000000000000000, 3.673940397442059868E-16 ) ) ;
#55438=DIRECTION ( 'NONE',  ( 1.062171939662868407E-14, 1.000000000000000000, 0.000000000000000000 ) ) ;
#55442=DIRECTION ( 'NONE',  ( 0.6414496315691367023, -0.7671651518153173033, -2.309356642089295169E-17 ) ) ;
#55443=LINE ( 'NONE', #32833, #63390 ) ;
#55444=ORIENTED_EDGE ( 'NONE', *, *, #41811, .F. ) ;
#55445=CARTESIAN_POINT ( 'NONE',  ( -5.993516549646711766, 5.993516549646603409, 455.0000000000000568 ) ) ;
#55447=DIRECTION ( 'NONE',  ( 1.836970198721029934E-16, 1.836970198721010706E-16, -1.000000000000000000 ) ) ;
#55450=AXIS2_PLACEMENT_3D ( 'NONE', #25064, #14095, #35653 ) ;
#55451=EDGE_LOOP ( 'NONE', ( #6849, #35642, #39738, #58805 ) ) ;
#55455=ORIENTED_EDGE ( 'NONE', *, *, #33888, .T. ) ;
#55463=CIRCLE ( 'NONE', #35102, 1.399999999999998579 ) ;
#55482=DIRECTION ( 'NONE',  ( -1.836970198721029934E-16, 1.836970198721036344E-16, -1.000000000000000000 ) ) ;
#55488=LINE ( 'NONE', #65746, #48357 ) ;
#55494=ORIENTED_EDGE ( 'NONE', *, *, #53805, .T. ) ;
#55495=DIRECTION ( 'NONE',  ( -4.268512490100335178E-15, -1.000000000000000000, 0.000000000000000000 ) ) ;
#55500=AXIS2_PLACEMENT_3D ( 'NONE', #41852, #36549, #57061 ) ;
#55513=CLOSED_SHELL ( 'NONE', ( #35854, #60717, #24937, #45102, #46698, #40465, #38997, #57922, #39214, #65176, #8075, #42743, #37745, #33897, #4018, #27986, #9883, #26630, #6812, #28146, #61498, #25790, #27167, #65600, #8640, #31646, #18184, #52388, #39944, #43058, #52029, #35763, #53769, #55703, #47, #50207, #41239, #23387, #38733, #40149, #46656, #66360, #62659, #22694, #40319, #47056, #22816, #3318, #20346, #29735, #11738, #69556, #65611, #67384, #66118, #49650, #65160, #33391, #25969, #39192, #52739, #28764, #28143, #41770, #43833, #27408, #33936, #39671, #54006, #6168, #1297, #58560, #29775, #21916, #21192, #21604, #43883, #55595, #40894, #58105, #27716, #37693, #11122, #42227, #24556, #66836, #63962, #56192, #1976, #153, #50252, #36501, #57033, #13344, #49671, #45826, #38337, #119, #67411, #45490, #58822, #32288, #57694, #25022, #61328, #16938, #11164, #25660, #54999, #55170, #4751, #24359, #68436, #41706, #35109, #19380, #33086, #32119, #44311, #48915, #51430, #30395, #19962, #14528, #53676, #44026, #58461, #675, #21677, #49160, #64708, #44458, #64190, #18959, #39990, #24450, #43485, #36055, #29896, #16389, #8626, #61360, #15518, #2422, #32115, #5701, #22407, #32643, #1034, #49519, #12210, #51842, #64223, #7224, #62165, #23395, #28549, #42306, #69841, #25700, #59958, #43909, #63192, #59331, #58135, #37020, #50952, #67457, #50531, #59822, #54728, #8475, #57402, #45500, #28425, #30393, #56763, #39888, #52706, #41417, #66961, #29413, #46705, #45354, #11728, #51855, #45835, #25905, #8479, #50831, #50871, #44009, #23737, #56078, #50552, #17220, #49871, #51009, #14635, #10950, #11305, #62219, #48078, #63601, #9535, #3851, #44276, #280, #36259, #43682, #27761, #56615, #237, #69638, #33191, #61951, #1622, #39984, #5046, #62349, #17363, #55116, #17420, #22377, #8308, #22475, #16547, #26294, #62795, #18900, #29453, #45775, #37485, #32808, #31258, #19697, #47059, #26806, #7896, #48868, #33551, #35212, #27101, #20452, #14979, #41186, #20160, #52931, #4369, #15605, #18606, #17880, #2983, #6874, #64238, #3860, #50997, #24999, #10517, #39515, #59725, #26104, #22267, #63482, #53627, #10165, #17586, #62605, #68923, #28490, #64292, #69157, #68661, #67405, #12136, #17583, #20716, #15232, #590, #12750, #1305, #3447, #25176, #67712, #17821, #6057, #63095, #68526, #55588, #2329, #69716, #22614, #8877, #11195, #36975, #36668, #2895, #56154, #13285, #15941, #17370, #47523, #21652, #20630, #5786, #33686, #63087, #59064, #68827, #29258, #38421, #19257, #11854, #41377, #8559, #6418, #27237, #6080, #67692, #5738, #13535, #40008, #31118, #33649, #69355, #31947, #24271, #44611, #21085, #62683, #62886, #11257, #6268, #38013, #67247, #45323, #3087, #31909, #17452, #61051, #59578, #3035, #46827, #4300, #9516, #44443, #43934, #29687, #28050, #17069, #36097, #47205, #42840, #40248, #66187, #58293, #40724, #46577, #21770, #6419, #19075, #37397, #3796, #35893, #24635, #40492, #4745, #3618, #28499, #1691, #48880, #58732 ) ) ;
#55515=CARTESIAN_POINT ( 'NONE',  ( 11.12648345035337982, -7.806483450353490561, 455.0000000000000568 ) ) ;
#55523=DIRECTION ( 'NONE',  ( 0.000000000000000000, 1.000000000000000000, 0.000000000000000000 ) ) ;
#55524=AXIS2_PLACEMENT_3D ( 'NONE', #51613, #40988, #19427 ) ;
#55526=DIRECTION ( 'NONE',  ( 1.836970198721029934E-16, -1.836970198721036344E-16, 1.000000000000000000 ) ) ;
#55527=CARTESIAN_POINT ( 'NONE',  ( -10.19191654964685156, -9.804883450353383267, 455.0000000000000568 ) ) ;
#55533=DIRECTION ( 'NONE',  ( 0.000000000000000000, -1.000000000000000000, -3.673940397442059868E-16 ) ) ;
#55535=VECTOR ( 'NONE', #52013, 1000.000000000000000 ) ;
#55536=DIRECTION ( 'NONE',  ( 1.836970198721029934E-16, 1.836970198721010706E-16, -1.000000000000000000 ) ) ;
#55545=VERTEX_POINT ( 'NONE', #45238 ) ;
#55563=AXIS2_PLACEMENT_3D ( 'NONE', #43103, #4598, #32513 ) ;
#55564=EDGE_CURVE ( 'NONE', #17797, #1336, #2463, .T. ) ;
#55566=VECTOR ( 'NONE', #27549, 1000.000000000000000 ) ;
#55579=VERTEX_POINT ( 'NONE', #1422 ) ;
#55588=ADVANCED_FACE ( 'NONE', ( #28294 ), #39253, .F. ) ;
#55591=LINE ( 'NONE', #69857, #39449 ) ;
#55595=ADVANCED_FACE ( 'NONE', ( #12357 ), #33937, .T. ) ;
#55598=CARTESIAN_POINT ( 'NONE',  ( -11.47551654964667733, 11.07551654964660237, 455.0000000000000568 ) ) ;
#55602=LINE ( 'NONE', #17774, #42292 ) ;
#55610=CARTESIAN_POINT ( 'NONE',  ( 9.106483450353380249, -11.12648345035348640, 455.0000000000000568 ) ) ;
#55612=AXIS2_PLACEMENT_3D ( 'NONE', #22430, #65226, #58875 ) ;
#55614=DIRECTION ( 'NONE',  ( 1.000000000000000000, 0.000000000000000000, 0.000000000000000000 ) ) ;
#55621=DIRECTION ( 'NONE',  ( 0.7671651518153105309, 0.6414496315691445849, 2.356647714346206145E-16 ) ) ;
#55623=DIRECTION ( 'NONE',  ( -1.000000000000000000, 0.000000000000000000, 0.000000000000000000 ) ) ;
#55624=AXIS2_PLACEMENT_3D ( 'NONE', #37439, #10557, #26478 ) ;
#55626=VERTEX_POINT ( 'NONE', #23342 ) ;
#55629=DIRECTION ( 'NONE',  ( -4.336808689942043768E-15, -1.000000000000000000, 0.000000000000000000 ) ) ;
#55637=CARTESIAN_POINT ( 'NONE',  ( -2.693516549646827851, -10.92648345035345692, 455.0000000000000568 ) ) ;
#55643=DIRECTION ( 'NONE',  ( 1.000000000000000000, 0.000000000000000000, -0.000000000000000000 ) ) ;
#55644=VECTOR ( 'NONE', #21778, 1000.000000000000000 ) ;
#55648=ORIENTED_EDGE ( 'NONE', *, *, #33808, .F. ) ;
#55662=AXIS2_PLACEMENT_3D ( 'NONE', #18143, #24154, #39708 ) ;
#55670=DIRECTION ( 'NONE',  ( 1.836970198721029934E-16, -1.836970198721036344E-16, 1.000000000000000000 ) ) ;
#55674=EDGE_CURVE ( 'NONE', #24680, #19296, #37472, .T. ) ;
#55679=AXIS2_PLACEMENT_3D ( 'NONE', #32887, #65419, #55495 ) ;
#55685=VECTOR ( 'NONE', #4424, 1000.000000000000000 ) ;
#55688=PLANE ( 'NONE',  #59902 ) ;
#55693=CARTESIAN_POINT ( 'NONE',  ( 12.00648345035338060, -4.186483450353492231, 455.0000000000000568 ) ) ;
#55698=CARTESIAN_POINT ( 'NONE',  ( -10.08346604330797369, -9.106483450353383802, 455.0000000000000568 ) ) ;
#55700=PLANE ( 'NONE',  #38905 ) ;
#55702=CARTESIAN_POINT ( 'NONE',  ( -11.99351654964679526, -7.826483450353362237, 455.0000000000000568 ) ) ;
#55703=ADVANCED_FACE ( 'NONE', ( #63270 ), #20133, .T. ) ;
#55708=EDGE_CURVE ( 'NONE', #15805, #35336, #52312, .T. ) ;
#55715=CIRCLE ( 'NONE', #2617, 0.4000000000000010214 ) ;
#55717=FACE_OUTER_BOUND ( 'NONE', #21926, .T. ) ;
#55719=EDGE_CURVE ( 'NONE', #38741, #57915, #2462, .T. ) ;
#55724=AXIS2_PLACEMENT_3D ( 'NONE', #39639, #7812, #2172 ) ;
#55729=CARTESIAN_POINT ( 'NONE',  ( -2.893516549646830249, -11.12648345035345621, 455.0000000000000568 ) ) ;
#55730=DIRECTION ( 'NONE',  ( 0.7071067811865550112, 0.7071067811865401342, 2.597868168706466299E-16 ) ) ;
#55732=EDGE_CURVE ( 'NONE', #69020, #61169, #45589, .T. ) ;
#55751=CARTESIAN_POINT ( 'NONE',  ( -5.993516549646776603, -6.006483450353426790, 455.0000000000000568 ) ) ;
#55753=LINE ( 'NONE', #28867, #68800 ) ;
#55756=FACE_OUTER_BOUND ( 'NONE', #15908, .T. ) ;
#55759=EDGE_LOOP ( 'NONE', ( #44178, #18500, #886, #33351 ) ) ;
#55763=DIRECTION ( 'NONE',  ( 0.000000000000000000, -1.000000000000000000, 0.000000000000000000 ) ) ;
#55767=VECTOR ( 'NONE', #9648, 1000.000000000000000 ) ;
#55776=LINE ( 'NONE', #33853, #8163 ) ;
#55777=AXIS2_PLACEMENT_3D ( 'NONE', #19543, #9298, #20948 ) ;
#55785=CARTESIAN_POINT ( 'NONE',  ( -10.19191654964671301, 10.19191654964664018, 455.0000000000000568 ) ) ;
#55793=ORIENTED_EDGE ( 'NONE', *, *, #463, .T. ) ;
#55797=EDGE_CURVE ( 'NONE', #19307, #14977, #47351, .T. ) ;
#55808=ORIENTED_EDGE ( 'NONE', *, *, #27451, .T. ) ;
#55811=VECTOR ( 'NONE', #69190, 1000.000000000000000 ) ;
#55812=AXIS2_PLACEMENT_3D ( 'NONE', #1815, #6766, #29375 ) ;
#55822=ORIENTED_EDGE ( 'NONE', *, *, #34361, .F. ) ;
#55825=CARTESIAN_POINT ( 'NONE',  ( -7.813516549646711162, 11.77351654964660277, 195.0000000000000284 ) ) ;
#55833=ORIENTED_EDGE ( 'NONE', *, *, #2811, .F. ) ;
#55839=CARTESIAN_POINT ( 'NONE',  ( 12.00648345035337883, -11.19368345035347900, 455.0000000000000568 ) ) ;
#55841=VECTOR ( 'NONE', #13444, 1000.000000000000000 ) ;
#55846=ORIENTED_EDGE ( 'NONE', *, *, #16410, .F. ) ;
#55858=ORIENTED_EDGE ( 'NONE', *, *, #37854, .F. ) ;
#55867=FACE_OUTER_BOUND ( 'NONE', #46061, .T. ) ;
#55869=LINE ( 'NONE', #33273, #39102 ) ;
#55870=LINE ( 'NONE', #24034, #59456 ) ;
#55877=CARTESIAN_POINT ( 'NONE',  ( -1.077516549646825750, -10.74648345035347852, 455.0000000000000568 ) ) ;
#55878=ORIENTED_EDGE ( 'NONE', *, *, #39294, .F. ) ;
#55886=VERTEX_POINT ( 'NONE', #42395 ) ;
#55894=CARTESIAN_POINT ( 'NONE',  ( 7.272650909786598561, -7.811466277050860718, 455.0000000000000568 ) ) ;
#55896=DIRECTION ( 'NONE',  ( -0.000000000000000000, 3.673940397442059868E-16, -1.000000000000000000 ) ) ;
#55902=VERTEX_POINT ( 'NONE', #59357 ) ;
#55907=VECTOR ( 'NONE', #21405, 1000.000000000000000 ) ;
#55909=AXIS2_PLACEMENT_3D ( 'NONE', #57750, #36176, #52457 ) ;
#55912=DIRECTION ( 'NONE',  ( 3.614007241618349165E-15, 1.000000000000000000, 0.000000000000000000 ) ) ;
#55916=VECTOR ( 'NONE', #56332, 1000.000000000000000 ) ;
#55918=CARTESIAN_POINT ( 'NONE',  ( 2.706483450353343478, -10.92648345035346225, 455.0000000000000568 ) ) ;
#55924=ORIENTED_EDGE ( 'NONE', *, *, #47210, .F. ) ;
#55932=EDGE_CURVE ( 'NONE', #40401, #10374, #7319, .T. ) ;
#55938=EDGE_CURVE ( 'NONE', #48072, #34099, #55776, .T. ) ;
#55940=CARTESIAN_POINT ( 'NONE',  ( -9.404046420174067222, -1.866219381641389674, 195.0000000000000284 ) ) ;
#55955=LINE ( 'NONE', #22740, #5121 ) ;
#55956=AXIS2_PLACEMENT_3D ( 'NONE', #60620, #34781, #7904 ) ;
#55961=ORIENTED_EDGE ( 'NONE', *, *, #30576, .T. ) ;
#55963=CARTESIAN_POINT ( 'NONE',  ( -4.173516549646666185, 11.99351654964658920, 455.0000000000000568 ) ) ;
#55965=VECTOR ( 'NONE', #2744, 1000.000000000000000 ) ;
#55971=CARTESIAN_POINT ( 'NONE',  ( 7.757955312929505354, 8.452095193409313367, 195.0000000000000284 ) ) ;
#55977=ORIENTED_EDGE ( 'NONE', *, *, #51853, .T. ) ;
#55979=DIRECTION ( 'NONE',  ( 1.836970198721029934E-16, -1.836970198721036344E-16, 1.000000000000000000 ) ) ;
#55981=EDGE_CURVE ( 'NONE', #1978, #4035, #17248, .T. ) ;
#55982=CARTESIAN_POINT ( 'NONE',  ( 10.74648345035330443, 1.677516549646577371, 195.0000000000000284 ) ) ;
#55986=DIRECTION ( 'NONE',  ( 0.000000000000000000, 0.000000000000000000, 1.000000000000000000 ) ) ;
#55990=ORIENTED_EDGE ( 'NONE', *, *, #46302, .T. ) ;
#55996=LINE ( 'NONE', #66257, #14615 ) ;
#55999=ORIENTED_EDGE ( 'NONE', *, *, #49754, .F. ) ;
#56003=VERTEX_POINT ( 'NONE', #12273 ) ;
#56019=ORIENTED_EDGE ( 'NONE', *, *, #63931, .F. ) ;
#56020=CIRCLE ( 'NONE', #69560, 0.3999999999999993006 ) ;
#56023=DIRECTION ( 'NONE',  ( 3.717264591378874374E-15, 1.000000000000000000, 0.000000000000000000 ) ) ;
#56033=EDGE_LOOP ( 'NONE', ( #37633, #968, #15579, #20936 ) ) ;
#56062=PLANE ( 'NONE',  #23636 ) ;
#56078=ADVANCED_FACE ( 'NONE', ( #65364 ), #22570, .F. ) ;
#56079=DIRECTION ( 'NONE',  ( -0.000000000000000000, -0.000000000000000000, -1.000000000000000000 ) ) ;
#56085=DIRECTION ( 'NONE',  ( -0.000000000000000000, -0.000000000000000000, -1.000000000000000000 ) ) ;
#56090=DIRECTION ( 'NONE',  ( -0.000000000000000000, -0.000000000000000000, -1.000000000000000000 ) ) ;
#56095=ORIENTED_EDGE ( 'NONE', *, *, #21775, .F. ) ;
#56101=VECTOR ( 'NONE', #51956, 1000.000000000000000 ) ;
#56103=CARTESIAN_POINT ( 'NONE',  ( -11.07551654964682086, -10.20488345035337296, 455.0000000000000568 ) ) ;
#56114=CIRCLE ( 'NONE', #67382, 0.1999999999999996503 ) ;
#56120=EDGE_CURVE ( 'NONE', #44833, #24433, #53373, .T. ) ;
#56123=CARTESIAN_POINT ( 'NONE',  ( 10.20488345035338007, -11.48848345035339769, 195.0000000000000284 ) ) ;
#56129=EDGE_CURVE ( 'NONE', #24615, #5610, #47704, .T. ) ;
#56130=CARTESIAN_POINT ( 'NONE',  ( 4.186483450353376767, 11.99351654964663716, 195.0000000000000284 ) ) ;
#56137=ORIENTED_EDGE ( 'NONE', *, *, #48642, .F. ) ;
#56141=DIRECTION ( 'NONE',  ( 0.7671651518152985405, 0.6414496315691592399, -2.309356642088639737E-17 ) ) ;
#56142=CARTESIAN_POINT ( 'NONE',  ( -4.734785091273957747, 5.380658396643156038, 195.0000000000000284 ) ) ;
#56148=VERTEX_POINT ( 'NONE', #56130 ) ;
#56154=ADVANCED_FACE ( 'NONE', ( #3091 ), #30308, .F. ) ;
#56164=EDGE_CURVE ( 'NONE', #55385, #62302, #45861, .T. ) ;
#56176=ORIENTED_EDGE ( 'NONE', *, *, #5620, .F. ) ;
#56181=CARTESIAN_POINT ( 'NONE',  ( -11.77351654964679106, -7.606483450353366038, 455.0000000000000568 ) ) ;
#56184=ORIENTED_EDGE ( 'NONE', *, *, #1572, .F. ) ;
#56191=ORIENTED_EDGE ( 'NONE', *, *, #52239, .F. ) ;
#56192=ADVANCED_FACE ( 'NONE', ( #3433 ), #9084, .T. ) ;
#56193=CARTESIAN_POINT ( 'NONE',  ( -7.252248008019509307, -5.393625297349935011, 455.0000000000000568 ) ) ;
#56213=VECTOR ( 'NONE', #25953, 1000.000000000000000 ) ;
#56223=VERTEX_POINT ( 'NONE', #48321 ) ;
#56237=DIRECTION ( 'NONE',  ( 1.836970198721029934E-16, 1.836970198721010706E-16, -1.000000000000000000 ) ) ;
#56242=EDGE_CURVE ( 'NONE', #46696, #62134, #16135, .T. ) ;
#56245=CARTESIAN_POINT ( 'NONE',  ( 6.006483450353379716, -4.606483450353492159, 455.0000000000000568 ) ) ;
#56265=DIRECTION ( 'NONE',  ( 1.000000000000000000, 0.000000000000000000, 0.000000000000000000 ) ) ;
#56269=CARTESIAN_POINT ( 'NONE',  ( 5.393625297349938563, 7.252248008019325454, 455.0000000000000568 ) ) ;
#56275=LINE ( 'NONE', #24093, #64502 ) ;
#56289=DIRECTION ( 'NONE',  ( 0.000000000000000000, 1.000000000000000000, 0.000000000000000000 ) ) ;
#56291=CARTESIAN_POINT ( 'NONE',  ( -9.093516549646782465, -11.12648345035334252, 195.0000000000000284 ) ) ;
#56297=FACE_OUTER_BOUND ( 'NONE', #28773, .T. ) ;
#56300=ORIENTED_EDGE ( 'NONE', *, *, #50299, .F. ) ;
#56302=ORIENTED_EDGE ( 'NONE', *, *, #3793, .F. ) ;
#56314=DIRECTION ( 'NONE',  ( -1.047444401652940007E-14, -1.000000000000000000, -1.836970198721029934E-16 ) ) ;
#56316=DIRECTION ( 'NONE',  ( -1.836970198721029934E-16, 1.836970198721036344E-16, -1.000000000000000000 ) ) ;
#56318=LINE ( 'NONE', #40033, #27266 ) ;
#56321=DIRECTION ( 'NONE',  ( 0.000000000000000000, 1.000000000000000000, 3.673940397442059868E-16 ) ) ;
#56323=ORIENTED_EDGE ( 'NONE', *, *, #47844, .T. ) ;
#56326=CARTESIAN_POINT ( 'NONE',  ( 4.201500623656039934, 7.259684009079806266, 455.0000000000000568 ) ) ;
#56331=EDGE_CURVE ( 'NONE', #40323, #63752, #65289, .T. ) ;
#56332=DIRECTION ( 'NONE',  ( -1.836970198721029934E-16, 1.836970198721036344E-16, -1.000000000000000000 ) ) ;
#56339=CARTESIAN_POINT ( 'NONE',  ( -11.77351654964670935, 7.813516549646603693, 455.0000000000000568 ) ) ;
#56344=ORIENTED_EDGE ( 'NONE', *, *, #9643, .F. ) ;
#56351=VECTOR ( 'NONE', #10661, 1000.000000000000000 ) ;
#56354=LINE ( 'NONE', #61288, #13036 ) ;
#56381=VERTEX_POINT ( 'NONE', #60658 ) ;
#56390=LINE ( 'NONE', #29866, #35303 ) ;
#56394=DIRECTION ( 'NONE',  ( 0.7071067811865530128, 0.7071067811865421326, 0.000000000000000000 ) ) ;
#56405=CARTESIAN_POINT ( 'NONE',  ( 10.92648345035337520, -9.106483450353492159, 455.0000000000000568 ) ) ;
#56415=ORIENTED_EDGE ( 'NONE', *, *, #5312, .T. ) ;
#56418=VECTOR ( 'NONE', #63018, 1000.000000000000000 ) ;
#56419=DIRECTION ( 'NONE',  ( -0.000000000000000000, -0.000000000000000000, -1.000000000000000000 ) ) ;
#56424=AXIS2_PLACEMENT_3D ( 'NONE', #54023, #5572, #37062 ) ;
#56425=DIRECTION ( 'NONE',  ( -1.836970198721029934E-16, -1.836970198721010706E-16, 1.000000000000000000 ) ) ;
#56427=ORIENTED_EDGE ( 'NONE', *, *, #14313, .T. ) ;
#56435=VECTOR ( 'NONE', #68802, 1000.000000000000000 ) ;
#56438=CYLINDRICAL_SURFACE ( 'NONE', #2166, 0.3999999999999993006 ) ;
#56442=EDGE_CURVE ( 'NONE', #14977, #41272, #33442, .T. ) ;
#56446=EDGE_CURVE ( 'NONE', #9593, #4203, #38403, .T. ) ;
#56450=ORIENTED_EDGE ( 'NONE', *, *, #12049, .F. ) ;
#56455=EDGE_CURVE ( 'NONE', #51358, #19035, #44373, .T. ) ;
#56456=CARTESIAN_POINT ( 'NONE',  ( 4.186483450353335023, -12.00648345035347830, 455.0000000000000568 ) ) ;
#56460=EDGE_CURVE ( 'NONE', #20566, #58112, #32742, .T. ) ;
#56463=LINE ( 'NONE', #30302, #68895 ) ;
#56475=VERTEX_POINT ( 'NONE', #6222 ) ;
#56480=CARTESIAN_POINT ( 'NONE',  ( -11.77351654964670935, 4.173516549646604901, 195.0000000000000284 ) ) ;
#56485=CARTESIAN_POINT ( 'NONE',  ( -7.415254214038336400, 3.593516549646603497, 455.0000000000000568 ) ) ;
#56488=FACE_OUTER_BOUND ( 'NONE', #64547, .T. ) ;
#56494=ORIENTED_EDGE ( 'NONE', *, *, #12865, .T. ) ;
#56496=CARTESIAN_POINT ( 'NONE',  ( 1.090483450353338268, -11.34648345035345329, 455.0000000000000568 ) ) ;
#56515=EDGE_CURVE ( 'NONE', #40339, #43425, #51083, .T. ) ;
#56520=ORIENTED_EDGE ( 'NONE', *, *, #59986, .T. ) ;
#56532=CARTESIAN_POINT ( 'NONE',  ( 7.811466277050774565, 7.259684009079793832, 455.0000000000000568 ) ) ;
#56538=ORIENTED_EDGE ( 'NONE', *, *, #18779, .F. ) ;
#56551=VECTOR ( 'NONE', #6873, 1000.000000000000000 ) ;
#56567=VECTOR ( 'NONE', #1881, 1000.000000000000000 ) ;
#56584=ORIENTED_EDGE ( 'NONE', *, *, #23791, .F. ) ;
#56588=CARTESIAN_POINT ( 'NONE',  ( 8.406483450353359643, 7.603567055985454459, 195.0000000000000284 ) ) ;
#56592=EDGE_CURVE ( 'NONE', #45555, #24615, #56390, .T. ) ;
#56601=ORIENTED_EDGE ( 'NONE', *, *, #46210, .T. ) ;
#56608=VERTEX_POINT ( 'NONE', #13952 ) ;
#56615=ADVANCED_FACE ( 'NONE', ( #12888 ), #41879, .F. ) ;
#56624=CARTESIAN_POINT ( 'NONE',  ( 1.690483450353370998, 10.73351654964664270, 195.0000000000000284 ) ) ;
#56637=VERTEX_POINT ( 'NONE', #4761 ) ;
#56639=CARTESIAN_POINT ( 'NONE',  ( 7.852485183456931139, -3.430747519065322937, 195.0000000000000284 ) ) ;
#56668=ORIENTED_EDGE ( 'NONE', *, *, #19345, .F. ) ;
#56669=CARTESIAN_POINT ( 'NONE',  ( 8.406483450353379183, -4.396432944014657451, 455.0000000000000568 ) ) ;
#56670=ORIENTED_EDGE ( 'NONE', *, *, #36602, .T. ) ;
#56675=DIRECTION ( 'NONE',  ( 0.7071067811865475727, 0.7071067811865475727, 2.597868168706480597E-16 ) ) ;
#56689=EDGE_CURVE ( 'NONE', #43025, #58272, #52497, .T. ) ;
#56701=VERTEX_POINT ( 'NONE', #63454 ) ;
#56704=VECTOR ( 'NONE', #46990, 1000.000000000000114 ) ;
#56706=ORIENTED_EDGE ( 'NONE', *, *, #66098, .F. ) ;
#56708=CARTESIAN_POINT ( 'NONE',  ( -11.11351654964674118, -4.206483450353336373, 455.0000000000000568 ) ) ;
#56709=CARTESIAN_POINT ( 'NONE',  ( 11.19368345035340440, 11.18071654964654904, 455.0000000000000568 ) ) ;
#56715=CARTESIAN_POINT ( 'NONE',  ( -9.791916549646819234, -11.08848345035330496, 195.0000000000000284 ) ) ;
#56718=LINE ( 'NONE', #46456, #66625 ) ;
#56727=CARTESIAN_POINT ( 'NONE',  ( -10.19191654964671301, 11.47551654964660450, 455.0000000000000568 ) ) ;
#56729=LINE ( 'NONE', #45768, #33084 ) ;
#56735=EDGE_LOOP ( 'NONE', ( #56520, #22680, #41723, #63065 ) ) ;
#56745=CARTESIAN_POINT ( 'NONE',  ( 7.272650909786598561, -4.201500623656122535, 455.0000000000000568 ) ) ;
#56749=ORIENTED_EDGE ( 'NONE', *, *, #52733, .T. ) ;
#56754=DIRECTION ( 'NONE',  ( -0.000000000000000000, 3.673940397442059868E-16, -1.000000000000000000 ) ) ;
#56763=ADVANCED_FACE ( 'NONE', ( #10408 ), #5104, .F. ) ;
#56766=DIRECTION ( 'NONE',  ( -0.7671651518153105309, -0.6414496315691445849, 0.000000000000000000 ) ) ;
#56768=EDGE_CURVE ( 'NONE', #43371, #2424, #54847, .T. ) ;
#56769=ORIENTED_EDGE ( 'NONE', *, *, #41295, .T. ) ;
#56776=EDGE_LOOP ( 'NONE', ( #33463, #4871, #36088, #31701 ) ) ;
#56780=LINE ( 'NONE', #17906, #34432 ) ;
#56795=ORIENTED_EDGE ( 'NONE', *, *, #15059, .F. ) ;
#56800=EDGE_CURVE ( 'NONE', #53367, #35322, #28306, .T. ) ;
#56801=EDGE_CURVE ( 'NONE', #20952, #8722, #32016, .T. ) ;
#56810=AXIS2_PLACEMENT_3D ( 'NONE', #60587, #18483, #13189 ) ;
#56816=ORIENTED_EDGE ( 'NONE', *, *, #53594, .F. ) ;
#56830=DIRECTION ( 'NONE',  ( -8.339399738404099512E-15, -1.000000000000000000, 0.000000000000000000 ) ) ;
#56831=LINE ( 'NONE', #56485, #5141 ) ;
#56833=CARTESIAN_POINT ( 'NONE',  ( 4.406483450353420928, 11.77351654964658501, 455.0000000000000568 ) ) ;
#56836=DIRECTION ( 'NONE',  ( 0.000000000000000000, 0.000000000000000000, 1.000000000000000000 ) ) ;
#56843=DIRECTION ( 'NONE',  ( -1.000000000000000000, 0.000000000000000000, 0.000000000000000000 ) ) ;
#56854=EDGE_CURVE ( 'NONE', #37495, #20667, #38921, .T. ) ;
#56858=EDGE_CURVE ( 'NONE', #14886, #50762, #61510, .T. ) ;
#56859=DIRECTION ( 'NONE',  ( 0.000000000000000000, 1.000000000000000000, 0.000000000000000000 ) ) ;
#56862=CARTESIAN_POINT ( 'NONE',  ( -4.188533722949417282, -4.740315990920195510, 455.0000000000000568 ) ) ;
#56864=AXIS2_PLACEMENT_3D ( 'NONE', #34840, #40143, #62407 ) ;
#56865=LINE ( 'NONE', #68547, #45218 ) ;
#56867=VERTEX_POINT ( 'NONE', #7078 ) ;
#56869=DIRECTION ( 'NONE',  ( -1.836970198721029934E-16, -1.836970198721010706E-16, 1.000000000000000000 ) ) ;
#56872=ORIENTED_EDGE ( 'NONE', *, *, #4847, .F. ) ;
#56888=CARTESIAN_POINT ( 'NONE',  ( 2.906483450353342324, -11.12648345035336916, 195.0000000000000284 ) ) ;
#56897=ORIENTED_EDGE ( 'NONE', *, *, #60194, .T. ) ;
#56900=DIRECTION ( 'NONE',  ( 4.336808689942043768E-15, 1.000000000000000000, 0.000000000000000000 ) ) ;
#56914=EDGE_CURVE ( 'NONE', #55902, #39228, #55715, .T. ) ;
#56918=AXIS2_PLACEMENT_3D ( 'NONE', #481, #37272, #22043 ) ;
#56922=CARTESIAN_POINT ( 'NONE',  ( 7.826483450353374671, 11.77351654964661876, 195.0000000000000284 ) ) ;
#56924=VERTEX_POINT ( 'NONE', #4251 ) ;
#56927=VERTEX_POINT ( 'NONE', #61883 ) ;
#56939=VERTEX_POINT ( 'NONE', #67543 ) ;
#56955=ORIENTED_EDGE ( 'NONE', *, *, #28965, .F. ) ;
#56961=CARTESIAN_POINT ( 'NONE',  ( -9.404046420174124066, 1.853252480934674651, 455.0000000000000568 ) ) ;
#56963=VERTEX_POINT ( 'NONE', #67887 ) ;
#56964=ORIENTED_EDGE ( 'NONE', *, *, #67563, .T. ) ;
#56970=CARTESIAN_POINT ( 'NONE',  ( 10.20488345035338185, -10.20488345035352928, 455.0000000000000568 ) ) ;
#56979=ORIENTED_EDGE ( 'NONE', *, *, #63702, .T. ) ;
#57000=AXIS2_PLACEMENT_3D ( 'NONE', #15213, #27217, #33874 ) ;
#57008=EDGE_CURVE ( 'NONE', #5664, #57882, #30759, .T. ) ;
#57019=CYLINDRICAL_SURFACE ( 'NONE', #68743, 2.204799999999997873 ) ;
#57023=EDGE_CURVE ( 'NONE', #41828, #35896, #54628, .T. ) ;
#57024=CARTESIAN_POINT ( 'NONE',  ( -9.828310488886053520, 1.677516549646603794, 455.0000000000000568 ) ) ;
#57032=DIRECTION ( 'NONE',  ( 0.7071067811865446862, 0.7071067811865503483, 0.000000000000000000 ) ) ;
#57033=ADVANCED_FACE ( 'NONE', ( #57973 ), #9541, .F. ) ;
#57036=VECTOR ( 'NONE', #566, 1000.000000000000000 ) ;
#57040=ORIENTED_EDGE ( 'NONE', *, *, #53604, .T. ) ;
#57043=ORIENTED_EDGE ( 'NONE', *, *, #58635, .F. ) ;
#57046=ORIENTED_EDGE ( 'NONE', *, *, #32561, .F. ) ;
#57051=ORIENTED_EDGE ( 'NONE', *, *, #24205, .F. ) ;
#57061=DIRECTION ( 'NONE',  ( -1.062171939662868407E-14, -1.000000000000000000, 0.000000000000000000 ) ) ;
#57066=CARTESIAN_POINT ( 'NONE',  ( -4.393516549646835578, -11.78648345035344214, 455.0000000000000568 ) ) ;
#57070=VECTOR ( 'NONE', #46783, 1000.000000000000000 ) ;
#57071=CARTESIAN_POINT ( 'NONE',  ( 6.006483450353401921, 5.993516549646582092, 455.0000000000000568 ) ) ;
#57072=DIRECTION ( 'NONE',  ( -0.000000000000000000, -0.000000000000000000, -1.000000000000000000 ) ) ;
#57084=EDGE_CURVE ( 'NONE', #41334, #27705, #23958, .T. ) ;
#57092=( GEOMETRIC_REPRESENTATION_CONTEXT ( 3 ) GLOBAL_UNCERTAINTY_ASSIGNED_CONTEXT ( ( #32374 ) ) GLOBAL_UNIT_ASSIGNED_CONTEXT ( ( #37190, #42823, #22647 ) ) REPRESENTATION_CONTEXT ( 'NONE', 'WORKASPACE' ) );
#57093=LINE ( 'NONE', #46480, #35820 ) ;
#57095=VERTEX_POINT ( 'NONE', #64334 ) ;
#57120=CYLINDRICAL_SURFACE ( 'NONE', #21094, 0.1999999999999987899 ) ;
#57123=AXIS2_PLACEMENT_3D ( 'NONE', #22138, #44034, #16485 ) ;
#57132=ORIENTED_EDGE ( 'NONE', *, *, #42496, .T. ) ;
#57133=ORIENTED_EDGE ( 'NONE', *, *, #17825, .F. ) ;
#57138=ORIENTED_EDGE ( 'NONE', *, *, #45135, .T. ) ;
#57146=DIRECTION ( 'NONE',  ( -1.000000000000000000, 0.000000000000000000, 0.000000000000000000 ) ) ;
#57156=CARTESIAN_POINT ( 'NONE',  ( -6.606374702650169795, 7.252248008019353875, 455.0000000000000568 ) ) ;
#57165=DIRECTION ( 'NONE',  ( -1.836970198721029934E-16, 1.836970198721036344E-16, -1.000000000000000000 ) ) ;
#57172=AXIS2_PLACEMENT_3D ( 'NONE', #32885, #37848, #59415 ) ;
#57177=VECTOR ( 'NONE', #46682, 1000.000000000000000 ) ;
#57181=CARTESIAN_POINT ( 'NONE',  ( 10.09643294401457858, 9.093516549646567526, 455.0000000000000568 ) ) ;
#57183=DIRECTION ( 'NONE',  ( 8.673617379884087537E-15, 1.000000000000000000, 0.000000000000000000 ) ) ;
#57184=DIRECTION ( 'NONE',  ( -0.000000000000000000, 3.673940397442059868E-16, -1.000000000000000000 ) ) ;
#57196=DIRECTION ( 'NONE',  ( 0.000000000000000000, 1.000000000000000000, 0.000000000000000000 ) ) ;
#57198=CARTESIAN_POINT ( 'NONE',  ( -6.606374702650211539, -7.265214908726115972, 195.0000000000000284 ) ) ;
#57200=ORIENTED_EDGE ( 'NONE', *, *, #18591, .T. ) ;
#57201=DIRECTION ( 'NONE',  ( 1.000000000000000000, -5.120954910632640039E-15, 0.000000000000000000 ) ) ;
#57203=ORIENTED_EDGE ( 'NONE', *, *, #47635, .T. ) ;
#57204=DIRECTION ( 'NONE',  ( 0.000000000000000000, 3.673940397442059868E-16, -1.000000000000000000 ) ) ;
#57206=FACE_OUTER_BOUND ( 'NONE', #35607, .T. ) ;
#57217=VECTOR ( 'NONE', #28750, 1000.000000000000000 ) ;
#57229=ORIENTED_EDGE ( 'NONE', *, *, #51079, .F. ) ;
#57238=ORIENTED_EDGE ( 'NONE', *, *, #69160, .F. ) ;
#57243=EDGE_LOOP ( 'NONE', ( #35364, #60678, #51849, #17747 ) ) ;
#57249=LINE ( 'NONE', #3512, #33905 ) ;
#57252=LINE ( 'NONE', #36745, #52757 ) ;
#57255=CARTESIAN_POINT ( 'NONE',  ( -11.07551654964667520, 10.19191654964664018, 455.0000000000000568 ) ) ;
#57258=DIRECTION ( 'NONE',  ( 1.836970198721029934E-16, -1.836970198721036344E-16, 1.000000000000000000 ) ) ;
#57262=CARTESIAN_POINT ( 'NONE',  ( -4.188533722949374649, -7.272650909786617213, 195.0000000000000284 ) ) ;
#57300=ORIENTED_EDGE ( 'NONE', *, *, #58023, .T. ) ;
#57304=ORIENTED_EDGE ( 'NONE', *, *, #28406, .F. ) ;
#57308=ORIENTED_EDGE ( 'NONE', *, *, #12776, .F. ) ;
#57314=ORIENTED_EDGE ( 'NONE', *, *, #31555, .F. ) ;
#57331=VECTOR ( 'NONE', #55730, 1000.000000000000114 ) ;
#57332=PLANE ( 'NONE',  #1339 ) ;
#57343=DIRECTION ( 'NONE',  ( -1.000000000000000000, 0.000000000000000000, 0.000000000000000000 ) ) ;
#57347=EDGE_CURVE ( 'NONE', #33281, #62698, #49462, .T. ) ;
#57355=EDGE_CURVE ( 'NONE', #34574, #3676, #18645, .T. ) ;
#57357=ORIENTED_EDGE ( 'NONE', *, *, #30829, .F. ) ;
#57362=CARTESIAN_POINT ( 'NONE',  ( 7.826483450353421745, 11.99351654964657499, 455.0000000000000568 ) ) ;
#57367=ORIENTED_EDGE ( 'NONE', *, *, #10025, .T. ) ;
#57371=EDGE_LOOP ( 'NONE', ( #593, #34532, #28090, #11815 ) ) ;
#57383=ORIENTED_EDGE ( 'NONE', *, *, #59855, .F. ) ;
#57386=ORIENTED_EDGE ( 'NONE', *, *, #54297, .T. ) ;
#57391=LINE ( 'NONE', #29816, #10553 ) ;
#57392=VERTEX_POINT ( 'NONE', #67089 ) ;
#57395=CYLINDRICAL_SURFACE ( 'NONE', #62132, 0.1999999999999992339 ) ;
#57397=ORIENTED_EDGE ( 'NONE', *, *, #8631, .F. ) ;
#57398=DIRECTION ( 'NONE',  ( -0.000000000000000000, 3.673940397442059868E-16, -1.000000000000000000 ) ) ;
#57399=VERTEX_POINT ( 'NONE', #45517 ) ;
#57402=ADVANCED_FACE ( 'NONE', ( #19690 ), #67458, .F. ) ;
#57408=DIRECTION ( 'NONE',  ( 0.000000000000000000, -1.000000000000000000, 0.000000000000000000 ) ) ;
#57437=EDGE_CURVE ( 'NONE', #27985, #64753, #57806, .T. ) ;
#57445=DIRECTION ( 'NONE',  ( -0.000000000000000000, 3.673940397442059868E-16, -1.000000000000000000 ) ) ;
#57451=ORIENTED_EDGE ( 'NONE', *, *, #5068, .T. ) ;
#57452=LINE ( 'NONE', #30587, #6845 ) ;
#57453=ORIENTED_EDGE ( 'NONE', *, *, #9025, .T. ) ;
#57473=CARTESIAN_POINT ( 'NONE',  ( -11.77351654964674310, -4.406483450353321452, 455.0000000000000568 ) ) ;
#57477=EDGE_CURVE ( 'NONE', #43775, #24181, #30592, .T. ) ;
#57479=ORIENTED_EDGE ( 'NONE', *, *, #24756, .F. ) ;
#57480=VECTOR ( 'NONE', #40176, 1000.000000000000114 ) ;
#57482=CARTESIAN_POINT ( 'NONE',  ( -5.993516549646711766, 5.993516549646603409, 455.0000000000000568 ) ) ;
#57502=EDGE_LOOP ( 'NONE', ( #42338, #24354, #68811, #41367 ) ) ;
#57503=DIRECTION ( 'NONE',  ( 2.891205793294683355E-15, 1.000000000000000000, 0.000000000000000000 ) ) ;
#57510=CARTESIAN_POINT ( 'NONE',  ( 11.34648345035334671, 1.077516549646521327, 455.0000000000000568 ) ) ;
#57524=FACE_OUTER_BOUND ( 'NONE', #40747, .T. ) ;
#57528=LINE ( 'NONE', #35597, #19814 ) ;
#57531=LINE ( 'NONE', #40566, #62417 ) ;
#57533=VERTEX_POINT ( 'NONE', #41190 ) ;
#57537=CARTESIAN_POINT ( 'NONE',  ( 6.619341603356837744, -7.265214908726241205, 455.0000000000000568 ) ) ;
#57541=VECTOR ( 'NONE', #44351, 1000.000000000000000 ) ;
#57555=EDGE_LOOP ( 'NONE', ( #17290, #41089, #53887, #41803 ) ) ;
#57561=CARTESIAN_POINT ( 'NONE',  ( 7.606483450353380249, -11.78648345035339418, 195.0000000000000284 ) ) ;
#57567=EDGE_CURVE ( 'NONE', #41995, #61368, #58166, .T. ) ;
#57571=VECTOR ( 'NONE', #21131, 1000.000000000000000 ) ;
#57580=ORIENTED_EDGE ( 'NONE', *, *, #62136, .T. ) ;
#57585=VECTOR ( 'NONE', #30186, 1000.000000000000000 ) ;
#57591=VERTEX_POINT ( 'NONE', #59564 ) ;
#57598=CARTESIAN_POINT ( 'NONE',  ( -3.417780618358626565, 7.839518282750134404, 455.0000000000000568 ) ) ;
#57600=DIRECTION ( 'NONE',  ( 9.050731179009442381E-15, 1.000000000000000000, 3.673940397442060361E-16 ) ) ;
#57604=DIRECTION ( 'NONE',  ( 1.836970198721029934E-16, 1.836970198721010706E-16, -1.000000000000000000 ) ) ;
#57613=DIRECTION ( 'NONE',  ( -7.808916176531286882E-15, -1.000000000000000000, -3.673940397442059868E-16 ) ) ;
#57630=VECTOR ( 'NONE', #22487, 1000.000000000000000 ) ;
#57635=ORIENTED_EDGE ( 'NONE', *, *, #67950, .F. ) ;
#57641=LINE ( 'NONE', #5318, #28145 ) ;
#57642=CARTESIAN_POINT ( 'NONE',  ( 7.826483450353380000, -12.00648345035339659, 195.0000000000000284 ) ) ;
#57663=CARTESIAN_POINT ( 'NONE',  ( -8.393516549646712122, 7.603567055985436696, 195.0000000000000284 ) ) ;
#57674=CARTESIAN_POINT ( 'NONE',  ( 7.616533956692244089, 8.393516549646575342, 455.0000000000000568 ) ) ;
#57678=DIRECTION ( 'NONE',  ( 2.135044278125299371E-15, -1.000000000000000000, 0.000000000000000000 ) ) ;
#57694=ADVANCED_FACE ( 'NONE', ( #64186 ), #43291, .F. ) ;
#57698=DIRECTION ( 'NONE',  ( -0.7671651518153028704, -0.6414496315691537998, -2.587583378555113506E-16 ) ) ;
#57702=LINE ( 'NONE', #7593, #21046 ) ;
#57705=ORIENTED_EDGE ( 'NONE', *, *, #33031, .F. ) ;
#57722=DIRECTION ( 'NONE',  ( -1.836970198721029934E-16, 1.836970198721036344E-16, -1.000000000000000000 ) ) ;
#57724=DIRECTION ( 'NONE',  ( -0.000000000000000000, 0.000000000000000000, -1.000000000000000000 ) ) ;
#57734=ORIENTED_EDGE ( 'NONE', *, *, #48405, .T. ) ;
#57736=DIRECTION ( 'NONE',  ( 0.000000000000000000, 1.000000000000000000, 3.673940397442059868E-16 ) ) ;
#57741=ORIENTED_EDGE ( 'NONE', *, *, #52669, .T. ) ;
#57746=LINE ( 'NONE', #68722, #45167 ) ;
#57750=CARTESIAN_POINT ( 'NONE',  ( -10.08346604330787777, 9.093516549646603053, 455.0000000000000568 ) ) ;
#57753=DIRECTION ( 'NONE',  ( -1.836970198721029934E-16, 1.836970198721036344E-16, -1.000000000000000000 ) ) ;
#57759=ORIENTED_EDGE ( 'NONE', *, *, #6936, .F. ) ;
#57763=FACE_OUTER_BOUND ( 'NONE', #18807, .T. ) ;
#57768=DIRECTION ( 'NONE',  ( 0.000000000000000000, 3.673940397442059868E-16, -1.000000000000000000 ) ) ;
#57770=AXIS2_PLACEMENT_3D ( 'NONE', #12006, #22974, #27944 ) ;
#57786=ORIENTED_EDGE ( 'NONE', *, *, #50287, .F. ) ;
#57788=DIRECTION ( 'NONE',  ( -4.336808689942025625E-15, -1.000000000000000000, 0.000000000000000000 ) ) ;
#57791=DIRECTION ( 'NONE',  ( 1.836970198721029934E-16, 1.836970198721010706E-16, -1.000000000000000000 ) ) ;
#57794=VERTEX_POINT ( 'NONE', #17450 ) ;
#57804=LINE ( 'NONE', #4776, #51923 ) ;
#57806=LINE ( 'NONE', #4082, #36439 ) ;
#57812=ORIENTED_EDGE ( 'NONE', *, *, #7717, .F. ) ;
#57814=ORIENTED_EDGE ( 'NONE', *, *, #55708, .T. ) ;
#57816=AXIS2_PLACEMENT_3D ( 'NONE', #35667, #9163, #41328 ) ;
#57818=PLANE ( 'NONE',  #8906 ) ;
#57824=CARTESIAN_POINT ( 'NONE',  ( -11.18071654964677997, -12.00648345035332554, 195.0000000000000284 ) ) ;
#57826=ORIENTED_EDGE ( 'NONE', *, *, #32986, .T. ) ;
#57828=VECTOR ( 'NONE', #15737, 1000.000000000000000 ) ;
#57830=ORIENTED_EDGE ( 'NONE', *, *, #985, .T. ) ;
#57834=LINE ( 'NONE', #63504, #22055 ) ;
#57836=AXIS2_PLACEMENT_3D ( 'NONE', #56496, #51192, #57201 ) ;
#57840=PLANE ( 'NONE',  #38538 ) ;
#57844=EDGE_CURVE ( 'NONE', #26597, #587, #22902, .T. ) ;
#57857=EDGE_CURVE ( 'NONE', #69389, #31564, #61291, .T. ) ;
#57863=CARTESIAN_POINT ( 'NONE',  ( 7.826483450353374671, 11.99351654964662295, 195.0000000000000284 ) ) ;
#57875=CARTESIAN_POINT ( 'NONE',  ( 2.290483450353415495, 9.828310488885934504, 455.0000000000000568 ) ) ;
#57882=VERTEX_POINT ( 'NONE', #46760 ) ;
#57895=EDGE_CURVE ( 'NONE', #3872, #5817, #52078, .T. ) ;
#57907=AXIS2_PLACEMENT_3D ( 'NONE', #23742, #30451, #36094 ) ;
#57908=ORIENTED_EDGE ( 'NONE', *, *, #5494, .T. ) ;
#57911=LINE ( 'NONE', #63579, #9652 ) ;
#57915=VERTEX_POINT ( 'NONE', #41105 ) ;
#57922=ADVANCED_FACE ( 'NONE', ( #24856, #46414, #9295, #30860, #19541, #58078, #67991, #14253, #35806, #3642 ), #25207, .T. ) ;
#57930=DIRECTION ( 'NONE',  ( 0.000000000000000000, -3.673940397442059868E-16, 1.000000000000000000 ) ) ;
#57932=ORIENTED_EDGE ( 'NONE', *, *, #35332, .F. ) ;
#57934=AXIS2_PLACEMENT_3D ( 'NONE', #68340, #57724, #31230 ) ;
#57938=LINE ( 'NONE', #9507, #2707 ) ;
#57939=ORIENTED_EDGE ( 'NONE', *, *, #45179, .T. ) ;
#57941=DIRECTION ( 'NONE',  ( 1.836970198721029934E-16, -1.836970198721036344E-16, 1.000000000000000000 ) ) ;
#57950=LINE ( 'NONE', #42039, #23401 ) ;
#57951=DIRECTION ( 'NONE',  ( -0.6414496315691521344, -0.7671651518153043137, -2.309356642088964526E-17 ) ) ;
#57955=ORIENTED_EDGE ( 'NONE', *, *, #37497, .F. ) ;
#57956=CARTESIAN_POINT ( 'NONE',  ( -9.828310488886049967, -2.290483450353357320, 455.0000000000000568 ) ) ;
#57962=EDGE_CURVE ( 'NONE', #45972, #3676, #48179, .T. ) ;
#57964=VECTOR ( 'NONE', #14937, 1000.000000000000000 ) ;
#57965=VERTEX_POINT ( 'NONE', #10002 ) ;
#57970=EDGE_CURVE ( 'NONE', #26906, #40491, #69247, .T. ) ;
#57973=FACE_OUTER_BOUND ( 'NONE', #13456, .T. ) ;
#57981=DIRECTION ( 'NONE',  ( 1.000000000000000000, -3.491481338843133355E-15, -1.836970198721036344E-16 ) ) ;
#57983=DIRECTION ( 'NONE',  ( 1.000000000000000000, 0.000000000000000000, 0.000000000000000000 ) ) ;
#57991=AXIS2_PLACEMENT_3D ( 'NONE', #16675, #66127, #12359 ) ;
#57992=CIRCLE ( 'NONE', #27503, 0.4000000000000010214 ) ;
#57994=ORIENTED_EDGE ( 'NONE', *, *, #19011, .F. ) ;
#58007=CARTESIAN_POINT ( 'NONE',  ( -4.727349090213559535, -7.811466277050794993, 455.0000000000000568 ) ) ;
#58008=EDGE_CURVE ( 'NONE', #66944, #3209, #44343, .T. ) ;
#58017=ORIENTED_EDGE ( 'NONE', *, *, #20279, .F. ) ;
#58023=EDGE_CURVE ( 'NONE', #30559, #35173, #5405, .T. ) ;
#58028=ORIENTED_EDGE ( 'NONE', *, *, #7024, .T. ) ;
#58043=DIRECTION ( 'NONE',  ( -0.000000000000000000, -0.000000000000000000, -1.000000000000000000 ) ) ;
#58045=CARTESIAN_POINT ( 'NONE',  ( -7.793516549646712477, 11.31351654964660014, 455.0000000000000568 ) ) ;
#58046=AXIS2_PLACEMENT_3D ( 'NONE', #60229, #49961, #55623 ) ;
#58049=LINE ( 'NONE', #31196, #43302 ) ;
#58051=DIRECTION ( 'NONE',  ( 0.000000000000000000, -3.673940397442059868E-16, 1.000000000000000000 ) ) ;
#58052=EDGE_CURVE ( 'NONE', #66887, #67098, #68082, .T. ) ;
#58062=DIRECTION ( 'NONE',  ( 1.000000000000000000, 0.000000000000000000, 0.000000000000000000 ) ) ;
#58075=ORIENTED_EDGE ( 'NONE', *, *, #65055, .T. ) ;
#58077=CARTESIAN_POINT ( 'NONE',  ( -10.08346604330797547, -9.306483450353381315, 455.0000000000000568 ) ) ;
#58078=FACE_BOUND ( 'NONE', #40690, .T. ) ;
#58080=DIRECTION ( 'NONE',  ( 1.836970198721029934E-16, 1.836970198721010706E-16, -1.000000000000000000 ) ) ;
#58088=CARTESIAN_POINT ( 'NONE',  ( 12.00648345035338238, 4.173516549646515195, 455.0000000000000568 ) ) ;
#58105=ADVANCED_FACE ( 'NONE', ( #11036 ), #32613, .T. ) ;
#58108=LINE ( 'NONE', #59151, #27158 ) ;
#58110=PLANE ( 'NONE',  #61590 ) ;
#58112=VERTEX_POINT ( 'NONE', #48872 ) ;
#58115=CIRCLE ( 'NONE', #36654, 2.204799999999997429 ) ;
#58116=CARTESIAN_POINT ( 'NONE',  ( 9.306483450353379538, -10.09643294401456259, 195.0000000000000284 ) ) ;
#58126=CARTESIAN_POINT ( 'NONE',  ( 4.747751991980663000, 5.380658396643107189, 455.0000000000000568 ) ) ;
#58129=FACE_OUTER_BOUND ( 'NONE', #37039, .T. ) ;
#58135=ADVANCED_FACE ( 'NONE', ( #43554 ), #38266, .F. ) ;
#58138=VECTOR ( 'NONE', #13059, 1000.000000000000000 ) ;
#58155=LINE ( 'NONE', #58525, #2662 ) ;
#58166=LINE ( 'NONE', #31318, #64654 ) ;
#58170=CARTESIAN_POINT ( 'NONE',  ( 9.247904806590725002, 9.942044687070426434, 455.0000000000000568 ) ) ;
#58177=VERTEX_POINT ( 'NONE', #49556 ) ;
#58178=ORIENTED_EDGE ( 'NONE', *, *, #26718, .T. ) ;
#58185=ORIENTED_EDGE ( 'NONE', *, *, #31491, .F. ) ;
#58188=DIRECTION ( 'NONE',  ( 1.221996412923863792E-14, 1.000000000000000000, 1.836970198721013910E-16 ) ) ;
#58192=AXIS2_PLACEMENT_3D ( 'NONE', #55098, #54744, #6298 ) ;
#58195=CIRCLE ( 'NONE', #66046, 0.3999999999999993006 ) ;
#58204=CARTESIAN_POINT ( 'NONE',  ( -4.393516549646667713, 11.77351654964658856, 455.0000000000000568 ) ) ;
#58209=DIRECTION ( 'NONE',  ( 1.047444401652940007E-14, 1.000000000000000000, 1.836970198721029934E-16 ) ) ;
#58212=DIRECTION ( 'NONE',  ( 0.6414496315691537998, -0.7671651518153029814, -2.309356642088714309E-17 ) ) ;
#58215=EDGE_CURVE ( 'NONE', #9315, #35140, #61181, .T. ) ;
#58218=DIRECTION ( 'NONE',  ( 0.7071067811865401342, -0.7071067811865549002, 0.000000000000000000 ) ) ;
#58235=DIRECTION ( 'NONE',  ( 0.000000000000000000, 1.000000000000000000, 0.000000000000000000 ) ) ;
#58239=DIRECTION ( 'NONE',  ( -1.000000000000000000, 0.000000000000000000, 0.000000000000000000 ) ) ;
#58241=EDGE_CURVE ( 'NONE', #64033, #37901, #61528, .T. ) ;
#58242=VECTOR ( 'NONE', #39389, 1000.000000000000000 ) ;
#58244=VECTOR ( 'NONE', #43232, 1000.000000000000000 ) ;
#58248=ORIENTED_EDGE ( 'NONE', *, *, #28447, .T. ) ;
#58251=AXIS2_PLACEMENT_3D ( 'NONE', #67809, #51550, #30329 ) ;
#58258=ORIENTED_EDGE ( 'NONE', *, *, #59905, .F. ) ;
#58262=DIRECTION ( 'NONE',  ( 0.000000000000000000, 0.000000000000000000, 1.000000000000000000 ) ) ;
#58265=EDGE_CURVE ( 'NONE', #11613, #44153, #64268, .T. ) ;
#58266=ORIENTED_EDGE ( 'NONE', *, *, #48405, .F. ) ;
#58269=DIRECTION ( 'NONE',  ( 1.836970198721029934E-16, 1.836970198721010706E-16, -1.000000000000000000 ) ) ;
#58272=VERTEX_POINT ( 'NONE', #51287 ) ;
#58287=LINE ( 'NONE', #47668, #47091 ) ;
#58293=ADVANCED_FACE ( 'NONE', ( #62240 ), #40680, .T. ) ;
#58299=DIRECTION ( 'NONE',  ( -1.000000000000000000, 0.000000000000000000, 0.000000000000000000 ) ) ;
#58303=ORIENTED_EDGE ( 'NONE', *, *, #50949, .T. ) ;
#58309=AXIS2_PLACEMENT_3D ( 'NONE', #58451, #15658, #59132 ) ;
#58313=LINE ( 'NONE', #52299, #38085 ) ;
#58314=EDGE_CURVE ( 'NONE', #15685, #13374, #15819, .T. ) ;
#58317=VECTOR ( 'NONE', #11822, 1000.000000000000114 ) ;
#58323=CARTESIAN_POINT ( 'NONE',  ( -2.993516549646701108, 7.415254214038204061, 455.0000000000000568 ) ) ;
#58325=CIRCLE ( 'NONE', #34561, 2.204799999999999205 ) ;
#58326=LINE ( 'NONE', #62208, #51612 ) ;
#58335=ORIENTED_EDGE ( 'NONE', *, *, #14141, .T. ) ;
#58346=VERTEX_POINT ( 'NONE', #4867 ) ;
#58355=ORIENTED_EDGE ( 'NONE', *, *, #9189, .F. ) ;
#58356=ORIENTED_EDGE ( 'NONE', *, *, #27174, .T. ) ;
#58359=ORIENTED_EDGE ( 'NONE', *, *, #13200, .T. ) ;
#58363=CARTESIAN_POINT ( 'NONE',  ( -4.383466043307968185, -8.406483450353443132, 455.0000000000000568 ) ) ;
#58364=DIRECTION ( 'NONE',  ( 0.5000000000000019984, 0.8660254037844375974, 3.181725716174716554E-16 ) ) ;
#58374=VERTEX_POINT ( 'NONE', #48348 ) ;
#58385=ORIENTED_EDGE ( 'NONE', *, *, #54240, .T. ) ;
#58396=DIRECTION ( 'NONE',  ( 1.836970198721029934E-16, 1.836970198721010706E-16, -1.000000000000000000 ) ) ;
#58398=CARTESIAN_POINT ( 'NONE',  ( 11.32648345035337734, -7.806483450353490561, 455.0000000000000568 ) ) ;
#58399=AXIS2_PLACEMENT_3D ( 'NONE', #6958, #17225, #22885 ) ;
#58400=CARTESIAN_POINT ( 'NONE',  ( 11.48848345035334617, -11.08848345035349148, 455.0000000000000568 ) ) ;
#58401=DIRECTION ( 'NONE',  ( -0.6414496315691619044, -0.7671651518152962090, 0.000000000000000000 ) ) ;
#58408=EDGE_LOOP ( 'NONE', ( #30333, #41522, #9147, #39784 ) ) ;
#58420=VECTOR ( 'NONE', #52258, 1000.000000000000000 ) ;
#58430=FACE_OUTER_BOUND ( 'NONE', #60835, .T. ) ;
#58432=CARTESIAN_POINT ( 'NONE',  ( -11.31351654964674402, -4.406483450353330333, 455.0000000000000568 ) ) ;
#58443=ORIENTED_EDGE ( 'NONE', *, *, #1534, .F. ) ;
#58444=ORIENTED_EDGE ( 'NONE', *, *, #48773, .F. ) ;
#58448=VECTOR ( 'NONE', #51787, 1000.000000000000000 ) ;
#58451=CARTESIAN_POINT ( 'NONE',  ( -7.603567055985634759, -8.406483450353409381, 455.0000000000000568 ) ) ;
#58452=VERTEX_POINT ( 'NONE', #16168 ) ;
#58454=ORIENTED_EDGE ( 'NONE', *, *, #40940, .F. ) ;
#58461=ADVANCED_FACE ( 'NONE', ( #54012 ), #44402, .F. ) ;
#58462=VECTOR ( 'NONE', #37255, 1000.000000000000000 ) ;
#58465=ORIENTED_EDGE ( 'NONE', *, *, #36602, .F. ) ;
#58471=AXIS2_PLACEMENT_3D ( 'NONE', #17201, #33119, #55056 ) ;
#58483=ORIENTED_EDGE ( 'NONE', *, *, #65638, .T. ) ;
#58488=DIRECTION ( 'NONE',  ( -0.6414496315691565753, -0.7671651518153006499, 0.000000000000000000 ) ) ;
#58494=DIRECTION ( 'NONE',  ( -1.000000000000000000, 0.000000000000000000, 0.000000000000000000 ) ) ;
#58496=ORIENTED_EDGE ( 'NONE', *, *, #32201, .T. ) ;
#58498=ORIENTED_EDGE ( 'NONE', *, *, #17927, .T. ) ;
#58504=DIRECTION ( 'NONE',  ( 0.000000000000000000, 1.000000000000000000, 0.000000000000000000 ) ) ;
#58506=CARTESIAN_POINT ( 'NONE',  ( -9.942044687070568543, 2.752095193409294982, 195.0000000000000284 ) ) ;
#58518=DIRECTION ( 'NONE',  ( -4.121462285523434951E-16, -1.000000000000000000, -0.000000000000000000 ) ) ;
#58519=CARTESIAN_POINT ( 'NONE',  ( 9.106483450353380249, -10.09643294401465852, 455.0000000000000568 ) ) ;
#58525=CARTESIAN_POINT ( 'NONE',  ( 8.406483450353379183, -7.616533956692325802, 455.0000000000000568 ) ) ;
#58535=CARTESIAN_POINT ( 'NONE',  ( -9.234937905884020637, 9.942044687070460185, 455.0000000000000568 ) ) ;
#58549=VERTEX_POINT ( 'NONE', #18581 ) ;
#58550=ORIENTED_EDGE ( 'NONE', *, *, #1740, .F. ) ;
#58552=DIRECTION ( 'NONE',  ( 0.000000000000000000, 0.000000000000000000, -1.000000000000000000 ) ) ;
#58560=ADVANCED_FACE ( 'NONE', ( #50758 ), #17892, .F. ) ;
#58564=AXIS2_PLACEMENT_3D ( 'NONE', #29147, #2281, #66975 ) ;
#58576=PLANE ( 'NONE',  #21785 ) ;
#58580=DIRECTION ( 'NONE',  ( -3.491481338843133355E-15, -1.000000000000000000, -1.836970198721029934E-16 ) ) ;
#58586=EDGE_CURVE ( 'NONE', #37838, #27624, #2330, .T. ) ;
#58592=CYLINDRICAL_SURFACE ( 'NONE', #8552, 0.5999999999999989786 ) ;
#58595=CARTESIAN_POINT ( 'NONE',  ( -1.077516549646832189, -11.34648345035347994, 455.0000000000000568 ) ) ;
#58604=DIRECTION ( 'NONE',  ( 1.836970198721029934E-16, 1.836970198721010706E-16, -1.000000000000000000 ) ) ;
#58605=VECTOR ( 'NONE', #35856, 1000.000000000000000 ) ;
#58631=DIRECTION ( 'NONE',  ( -0.000000000000000000, 3.673940397442059868E-16, -1.000000000000000000 ) ) ;
#58635=EDGE_CURVE ( 'NONE', #68965, #37762, #57992, .T. ) ;
#58646=EDGE_CURVE ( 'NONE', #49618, #57533, #3040, .T. ) ;
#58647=VECTOR ( 'NONE', #19109, 1000.000000000000114 ) ;
#58650=CARTESIAN_POINT ( 'NONE',  ( 4.206483450353421638, 11.11351654964658486, 455.0000000000000568 ) ) ;
#58651=ORIENTED_EDGE ( 'NONE', *, *, #48308, .F. ) ;
#58652=LINE ( 'NONE', #22122, #54674 ) ;
#58654=CARTESIAN_POINT ( 'NONE',  ( 4.622483450353380263, -3.606483450353491271, 455.0000000000000568 ) ) ;
#58663=PLANE ( 'NONE',  #26003 ) ;
#58668=CARTESIAN_POINT ( 'NONE',  ( 6.006483450353379716, -6.006483450353490738, 455.0000000000000568 ) ) ;
#58670=CARTESIAN_POINT ( 'NONE',  ( 11.08848345035341687, 10.19191654964656379, 455.0000000000000568 ) ) ;
#58679=DIRECTION ( 'NONE',  ( 1.000000000000000000, -6.308085367188447236E-15, -2.317552966102676720E-30 ) ) ;
#58688=ORIENTED_EDGE ( 'NONE', *, *, #47210, .T. ) ;
#58691=LINE ( 'NONE', #20157, #62569 ) ;
#58693=DIRECTION ( 'NONE',  ( -1.000000000000000000, 3.903627567395476653E-15, 1.836970198721037083E-16 ) ) ;
#58694=ORIENTED_EDGE ( 'NONE', *, *, #62348, .T. ) ;
#58701=DIRECTION ( 'NONE',  ( 8.673617379884051249E-15, 1.000000000000000000, 0.000000000000000000 ) ) ;
#58711=LINE ( 'NONE', #16963, #47736 ) ;
#58712=ORIENTED_EDGE ( 'NONE', *, *, #52802, .F. ) ;
#58714=EDGE_LOOP ( 'NONE', ( #18669, #64687, #57635, #26848 ) ) ;
#58730=CYLINDRICAL_SURFACE ( 'NONE', #54256, 0.3999999999999993006 ) ;
#58732=ADVANCED_FACE ( 'NONE', ( #20683 ), #36251, .F. ) ;
#58737=ORIENTED_EDGE ( 'NONE', *, *, #6487, .F. ) ;
#58743=DIRECTION ( 'NONE',  ( 0.000000000000000000, -3.673940397442059868E-16, 1.000000000000000000 ) ) ;
#58746=CARTESIAN_POINT ( 'NONE',  ( -7.793516549646712477, 11.11351654964660085, 455.0000000000000568 ) ) ;
#58747=EDGE_LOOP ( 'NONE', ( #1809, #7588, #63314, #25949 ) ) ;
#58749=CIRCLE ( 'NONE', #36116, 1.399999999999999245 ) ;
#58751=ORIENTED_EDGE ( 'NONE', *, *, #2942, .T. ) ;
#58761=EDGE_CURVE ( 'NONE', #25574, #65042, #1548, .T. ) ;
#58763=LINE ( 'NONE', #10319, #20116 ) ;
#58793=DIRECTION ( 'NONE',  ( 0.000000000000000000, -3.673940397442059868E-16, 1.000000000000000000 ) ) ;
#58797=VERTEX_POINT ( 'NONE', #32353 ) ;
#58801=DIRECTION ( 'NONE',  ( -1.678252938371784572E-14, -1.000000000000000000, -1.836970198721041520E-16 ) ) ;
#58805=ORIENTED_EDGE ( 'NONE', *, *, #53279, .T. ) ;
#58807=ORIENTED_EDGE ( 'NONE', *, *, #38805, .F. ) ;
#58814=AXIS2_PLACEMENT_3D ( 'NONE', #6231, #12215, #23180 ) ;
#58816=DIRECTION ( 'NONE',  ( -1.836970198721029934E-16, 1.836970198721036344E-16, -1.000000000000000000 ) ) ;
#58817=EDGE_CURVE ( 'NONE', #37901, #11813, #16089, .T. ) ;
#58818=CARTESIAN_POINT ( 'NONE',  ( -11.31351654964671027, 4.393516549646604652, 455.0000000000000568 ) ) ;
#58819=VERTEX_POINT ( 'NONE', #43299 ) ;
#58820=ORIENTED_EDGE ( 'NONE', *, *, #51501, .T. ) ;
#58822=ADVANCED_FACE ( 'NONE', ( #37660 ), #59224, .F. ) ;
#58827=AXIS2_PLACEMENT_3D ( 'NONE', #59343, #53013, #43078 ) ;
#58834=DIRECTION ( 'NONE',  ( -8.802523127157697409E-15, -1.000000000000000000, -1.836970198721026976E-16 ) ) ;
#58847=AXIS2_PLACEMENT_3D ( 'NONE', #65511, #10718, #16035 ) ;
#58865=EDGE_CURVE ( 'NONE', #25048, #11040, #17124, .T. ) ;
#58866=CARTESIAN_POINT ( 'NONE',  ( 8.406483450353379183, -6.344579767990935260, 455.0000000000000568 ) ) ;
#58875=DIRECTION ( 'NONE',  ( 1.000000000000000000, -3.491481338843132961E-15, 0.000000000000000000 ) ) ;
#58876=VERTEX_POINT ( 'NONE', #21391 ) ;
#58894=LINE ( 'NONE', #31341, #5638 ) ;
#58906=CIRCLE ( 'NONE', #9234, 0.2000000000000005107 ) ;
#58907=DIRECTION ( 'NONE',  ( 1.836970198721029934E-16, 1.836970198721010706E-16, -1.000000000000000000 ) ) ;
#58912=DIRECTION ( 'NONE',  ( -1.836970198721029934E-16, 1.836970198721036344E-16, -1.000000000000000000 ) ) ;
#58915=CIRCLE ( 'NONE', #1365, 0.5999999999999989786 ) ;
#58920=CARTESIAN_POINT ( 'NONE',  ( -4.727349090213552429, -4.201500623656063915, 455.0000000000000568 ) ) ;
#58921=CARTESIAN_POINT ( 'NONE',  ( -7.259684009080030975, -7.811466277050769236, 455.0000000000000568 ) ) ;
#58924=EDGE_CURVE ( 'NONE', #53142, #40323, #33392, .T. ) ;
#58931=LINE ( 'NONE', #64936, #23096 ) ;
#58936=EDGE_CURVE ( 'NONE', #17426, #28515, #7546, .T. ) ;
#58939=VECTOR ( 'NONE', #10992, 1000.000000000000000 ) ;
#58946=CARTESIAN_POINT ( 'NONE',  ( -9.942044687070620057, -9.247904806590648619, 195.0000000000000284 ) ) ;
#58948=ORIENTED_EDGE ( 'NONE', *, *, #47876, .T. ) ;
#58950=CIRCLE ( 'NONE', #55563, 0.2000000000000005107 ) ;
#58954=LINE ( 'NONE', #52965, #41937 ) ;
#58957=CARTESIAN_POINT ( 'NONE',  ( -4.727349090213560423, -7.811466277050794993, 455.0000000000000568 ) ) ;
#58963=VECTOR ( 'NONE', #45953, 1000.000000000000000 ) ;
#58964=LINE ( 'NONE', #66289, #57541 ) ;
#58969=DIRECTION ( 'NONE',  ( 8.673617379884051249E-15, 1.000000000000000000, 0.000000000000000000 ) ) ;
#58970=CARTESIAN_POINT ( 'NONE',  ( -5.655420232009359616, -8.406483450353428921, 455.0000000000000568 ) ) ;
#58973=LINE ( 'NONE', #31058, #48680 ) ;
#58975=ORIENTED_EDGE ( 'NONE', *, *, #41917, .T. ) ;
#58977=EDGE_CURVE ( 'NONE', #23736, #42184, #29121, .T. ) ;
#58981=VERTEX_POINT ( 'NONE', #28413 ) ;
#58991=EDGE_LOOP ( 'NONE', ( #2888, #35811, #40659, #52007, #43386, #53590, #61389, #55444, #12689, #9728, #64865, #31818, #67787, #43861, #53846, #379, #40280 ) ) ;
#58993=AXIS2_PLACEMENT_3D ( 'NONE', #67204, #14159, #19807 ) ;
#58997=VECTOR ( 'NONE', #60930, 1000.000000000000000 ) ;
#59005=ORIENTED_EDGE ( 'NONE', *, *, #34807, .T. ) ;
#59016=DIRECTION ( 'NONE',  ( -0.000000000000000000, -0.000000000000000000, -1.000000000000000000 ) ) ;
#59017=LINE ( 'NONE', #11261, #36910 ) ;
#59018=DIRECTION ( 'NONE',  ( -0.7071067811865588970, -0.7071067811865361374, -2.597868168706466299E-16 ) ) ;
#59021=EDGE_CURVE ( 'NONE', #66347, #48590, #14006, .T. ) ;
#59025=EDGE_CURVE ( 'NONE', #6582, #63655, #34290, .T. ) ;
#59030=ORIENTED_EDGE ( 'NONE', *, *, #54718, .F. ) ;
#59040=EDGE_CURVE ( 'NONE', #25574, #57533, #23815, .T. ) ;
#59043=DIRECTION ( 'NONE',  ( -1.000000000000000000, 1.047444401652939849E-14, 0.000000000000000000 ) ) ;
#59053=VERTEX_POINT ( 'NONE', #44328 ) ;
#59056=AXIS2_PLACEMENT_3D ( 'NONE', #54184, #26604, #5742 ) ;
#59060=DIRECTION ( 'NONE',  ( 0.7071067811865451302, -0.7071067811865500152, 0.000000000000000000 ) ) ;
#59061=DIRECTION ( 'NONE',  ( 3.540573132209561620E-15, 1.000000000000000000, 0.000000000000000000 ) ) ;
#59064=ADVANCED_FACE ( 'NONE', ( #66940 ), #61985, .F. ) ;
#59065=CARTESIAN_POINT ( 'NONE',  ( -4.173516549646839380, -12.00648345035344811, 455.0000000000000568 ) ) ;
#59070=VECTOR ( 'NONE', #50869, 1000.000000000000000 ) ;
#59073=CARTESIAN_POINT ( 'NONE',  ( 10.92648345035337520, -9.106483450353398013, 195.0000000000000284 ) ) ;
#59081=CARTESIAN_POINT ( 'NONE',  ( 11.78648345035337819, -4.406483450353394282, 195.0000000000000284 ) ) ;
#59082=LINE ( 'NONE', #6383, #26755 ) ;
#59086=VECTOR ( 'NONE', #30355, 1000.000000000000000 ) ;
#59087=EDGE_LOOP ( 'NONE', ( #54082, #9865, #30207, #42038 ) ) ;
#59091=LINE ( 'NONE', #48488, #3938 ) ;
#59098=CARTESIAN_POINT ( 'NONE',  ( -6.606374702650164465, -4.747751991980617703, 195.0000000000000284 ) ) ;
#59099=EDGE_CURVE ( 'NONE', #63655, #56223, #24864, .T. ) ;
#59102=LINE ( 'NONE', #33614, #46193 ) ;
#59107=EDGE_CURVE ( 'NONE', #45635, #43736, #42169, .T. ) ;
#59109=ORIENTED_EDGE ( 'NONE', *, *, #16892, .F. ) ;
#59123=DIRECTION ( 'NONE',  ( 0.6414496315691539108, -0.7671651518153028704, -2.587583378555131256E-16 ) ) ;
#59124=ORIENTED_EDGE ( 'NONE', *, *, #32476, .F. ) ;
#59125=EDGE_CURVE ( 'NONE', #6262, #21629, #63754, .T. ) ;
#59128=CARTESIAN_POINT ( 'NONE',  ( 4.396432944014576627, 8.393516549646587777, 455.0000000000000568 ) ) ;
#59132=DIRECTION ( 'NONE',  ( -1.000000000000000000, 1.047444401652939849E-14, 0.000000000000000000 ) ) ;
#59136=EDGE_CURVE ( 'NONE', #14058, #13109, #41120, .T. ) ;
#59147=CARTESIAN_POINT ( 'NONE',  ( 4.406483450353335662, -11.78648345035347766, 455.0000000000000568 ) ) ;
#59151=CARTESIAN_POINT ( 'NONE',  ( -11.31351654964678843, -7.606483450353371367, 455.0000000000000568 ) ) ;
#59161=ORIENTED_EDGE ( 'NONE', *, *, #12131, .F. ) ;
#59162=DIRECTION ( 'NONE',  ( 1.000000000000000000, 0.000000000000000000, 0.000000000000000000 ) ) ;
#59167=LINE ( 'NONE', #53883, #59983 ) ;
#59168=LINE ( 'NONE', #54569, #41381 ) ;
#59171=VECTOR ( 'NONE', #51286, 1000.000000000000000 ) ;
#59172=AXIS2_PLACEMENT_3D ( 'NONE', #10368, #32279, #21674 ) ;
#59176=ORIENTED_EDGE ( 'NONE', *, *, #14967, .F. ) ;
#59179=EDGE_CURVE ( 'NONE', #11814, #41587, #19658, .T. ) ;
#59180=CARTESIAN_POINT ( 'NONE',  ( -7.603567055985545942, 8.593516549646603053, 195.0000000000000284 ) ) ;
#59181=AXIS2_PLACEMENT_3D ( 'NONE', #43558, #54530, #11378 ) ;
#59188=VERTEX_POINT ( 'NONE', #25932 ) ;
#59192=EDGE_CURVE ( 'NONE', #61399, #5119, #4371, .T. ) ;
#59207=LINE ( 'NONE', #64864, #46374 ) ;
#59215=ORIENTED_EDGE ( 'NONE', *, *, #31239, .T. ) ;
#59217=VECTOR ( 'NONE', #43539, 1000.000000000000000 ) ;
#59220=ORIENTED_EDGE ( 'NONE', *, *, #102, .T. ) ;
#59224=PLANE ( 'NONE',  #62562 ) ;
#59225=DIRECTION ( 'NONE',  ( -1.000000000000000000, -1.570596175624152093E-15, 0.000000000000000000 ) ) ;
#59227=EDGE_LOOP ( 'NONE', ( #8758, #25214, #19379, #51232 ) ) ;
#59230=EDGE_LOOP ( 'NONE', ( #67932, #15979, #59890, #4715 ) ) ;
#59237=VERTEX_POINT ( 'NONE', #47825 ) ;
#59240=DIRECTION ( 'NONE',  ( -0.7071067811865475727, -0.7071067811865475727, -2.597868168706480597E-16 ) ) ;
#59244=ORIENTED_EDGE ( 'NONE', *, *, #17816, .T. ) ;
#59250=ORIENTED_EDGE ( 'NONE', *, *, #9838, .F. ) ;
#59259=DIRECTION ( 'NONE',  ( -1.836970198721029934E-16, 1.836970198721036344E-16, -1.000000000000000000 ) ) ;
#59266=CARTESIAN_POINT ( 'NONE',  ( 9.247904806590689475, -9.955011587777253368, 195.0000000000000284 ) ) ;
#59277=LINE ( 'NONE', #9811, #14217 ) ;
#59288=EDGE_CURVE ( 'NONE', #12989, #11613, #99, .T. ) ;
#59294=ORIENTED_EDGE ( 'NONE', *, *, #26445, .T. ) ;
#59303=AXIS2_PLACEMENT_3D ( 'NONE', #35728, #36078, #30077 ) ;
#59312=ORIENTED_EDGE ( 'NONE', *, *, #15677, .F. ) ;
#59331=ADVANCED_FACE ( 'NONE', ( #6095 ), #805, .F. ) ;
#59332=EDGE_CURVE ( 'NONE', #2177, #64205, #23031, .T. ) ;
#59340=CARTESIAN_POINT ( 'NONE',  ( -8.393516549646712122, 4.383466043307770121, 195.0000000000000284 ) ) ;
#59343=CARTESIAN_POINT ( 'NONE',  ( -10.19191654964685689, -10.20488345035338362, 455.0000000000000568 ) ) ;
#59350=DIRECTION ( 'NONE',  ( -0.000000000000000000, 3.673940397442059868E-16, -1.000000000000000000 ) ) ;
#59357=CARTESIAN_POINT ( 'NONE',  ( -11.07551654964667520, 11.47551654964660450, 455.0000000000000568 ) ) ;
#59361=ORIENTED_EDGE ( 'NONE', *, *, #24613, .T. ) ;
#59371=EDGE_CURVE ( 'NONE', #69428, #56924, #49907, .T. ) ;
#59386=CARTESIAN_POINT ( 'NONE',  ( -10.91351654964670814, 9.093516549646603053, 455.0000000000000568 ) ) ;
#59387=ORIENTED_EDGE ( 'NONE', *, *, #59986, .F. ) ;
#59393=ORIENTED_EDGE ( 'NONE', *, *, #5654, .T. ) ;
#59396=FACE_OUTER_BOUND ( 'NONE', #37078, .T. ) ;
#59399=DIRECTION ( 'NONE',  ( 0.000000000000000000, -3.673940397442059868E-16, 1.000000000000000000 ) ) ;
#59401=VECTOR ( 'NONE', #34831, 1000.000000000000114 ) ;
#59405=CIRCLE ( 'NONE', #49215, 0.5999999999999989786 ) ;
#59410=VERTEX_POINT ( 'NONE', #66855 ) ;
#59415=DIRECTION ( 'NONE',  ( 1.000000000000000000, 0.000000000000000000, 0.000000000000000000 ) ) ;
#59420=VECTOR ( 'NONE', #10109, 1000.000000000000000 ) ;
#59424=VECTOR ( 'NONE', #46107, 1000.000000000000000 ) ;
#59431=EDGE_LOOP ( 'NONE', ( #55793, #6635, #13423, #975, #5217, #13179, #19559, #36513, #24875, #35113, #17389, #23036, #4601, #10221, #43136, #36787, #10824 ) ) ;
#59436=LINE ( 'NONE', #42819, #2320 ) ;
#59437=DIRECTION ( 'NONE',  ( 0.7671651518152939886, -0.6414496315691644579, -2.587583378555133721E-16 ) ) ;
#59438=VERTEX_POINT ( 'NONE', #50251 ) ;
#59454=VECTOR ( 'NONE', #58396, 1000.000000000000000 ) ;
#59456=VECTOR ( 'NONE', #63178, 1000.000000000000000 ) ;
#59459=ORIENTED_EDGE ( 'NONE', *, *, #23715, .T. ) ;
#59471=EDGE_LOOP ( 'NONE', ( #30488, #12266, #38418, #51507 ) ) ;
#59472=ORIENTED_EDGE ( 'NONE', *, *, #30524, .T. ) ;
#59474=ORIENTED_EDGE ( 'NONE', *, *, #10236, .F. ) ;
#59475=VERTEX_POINT ( 'NONE', #12406 ) ;
#59478=LINE ( 'NONE', #64784, #53531 ) ;
#59480=CARTESIAN_POINT ( 'NONE',  ( -9.791916549646867196, -11.08848345035335115, 455.0000000000000568 ) ) ;
#59483=CARTESIAN_POINT ( 'NONE',  ( 10.20488345035338185, -9.804883450353528929, 455.0000000000000568 ) ) ;
#59496=ORIENTED_EDGE ( 'NONE', *, *, #60423, .F. ) ;
#59497=DIRECTION ( 'NONE',  ( 0.000000000000000000, 3.673940397442059868E-16, -1.000000000000000000 ) ) ;
#59500=DIRECTION ( 'NONE',  ( -0.000000000000000000, 3.673940397442059868E-16, -1.000000000000000000 ) ) ;
#59503=AXIS2_PLACEMENT_3D ( 'NONE', #28884, #6970, #62105 ) ;
#59508=EDGE_CURVE ( 'NONE', #27839, #52379, #22695, .T. ) ;
#59516=ORIENTED_EDGE ( 'NONE', *, *, #2571, .T. ) ;
#59519=DIRECTION ( 'NONE',  ( -0.000000000000000000, -1.000000000000000000, -0.000000000000000000 ) ) ;
#59527=EDGE_CURVE ( 'NONE', #44836, #44460, #65994, .T. ) ;
#59538=ORIENTED_EDGE ( 'NONE', *, *, #11965, .F. ) ;
#59544=DIRECTION ( 'NONE',  ( -0.000000000000000000, -0.000000000000000000, -1.000000000000000000 ) ) ;
#59545=AXIS2_PLACEMENT_3D ( 'NONE', #57956, #35317, #3175 ) ;
#59551=FACE_OUTER_BOUND ( 'NONE', #52819, .T. ) ;
#59553=VECTOR ( 'NONE', #21088, 1000.000000000000000 ) ;
#59564=CARTESIAN_POINT ( 'NONE',  ( -11.99351654964674729, -7.826483450353316051, 195.0000000000000284 ) ) ;
#59567=VECTOR ( 'NONE', #58364, 999.9999999999998863 ) ;
#59571=ORIENTED_EDGE ( 'NONE', *, *, #26051, .F. ) ;
#59574=DIRECTION ( 'NONE',  ( -1.570596175624152093E-15, 1.000000000000000000, 3.673940397442060361E-16 ) ) ;
#59578=ADVANCED_FACE ( 'NONE', ( #19468 ), #24437, .F. ) ;
#59579=ORIENTED_EDGE ( 'NONE', *, *, #46648, .F. ) ;
#59581=CARTESIAN_POINT ( 'NONE',  ( 10.92648345035340895, 9.293516549646565039, 455.0000000000000568 ) ) ;
#59588=ORIENTED_EDGE ( 'NONE', *, *, #24599, .T. ) ;
#59597=VERTEX_POINT ( 'NONE', #58007 ) ;
#59598=EDGE_CURVE ( 'NONE', #52379, #20859, #9575, .T. ) ;
#59609=VECTOR ( 'NONE', #27592, 1000.000000000000000 ) ;
#59614=DIRECTION ( 'NONE',  ( -0.000000000000000000, -0.000000000000000000, -1.000000000000000000 ) ) ;
#59620=PLANE ( 'NONE',  #27675 ) ;
#59629=FACE_OUTER_BOUND ( 'NONE', #66194, .T. ) ;
#59631=CARTESIAN_POINT ( 'NONE',  ( 10.74648345035335240, 1.677516549646529409, 455.0000000000000568 ) ) ;
#59635=PLANE ( 'NONE',  #50853 ) ;
#59654=VECTOR ( 'NONE', #24673, 1000.000000000000000 ) ;
#59665=ORIENTED_EDGE ( 'NONE', *, *, #17982, .T. ) ;
#59667=EDGE_CURVE ( 'NONE', #34851, #64638, #46820, .T. ) ;
#59671=VERTEX_POINT ( 'NONE', #47744 ) ;
#59685=CARTESIAN_POINT ( 'NONE',  ( -2.693516549646827851, -10.92648345035345692, 455.0000000000000568 ) ) ;
#59690=CARTESIAN_POINT ( 'NONE',  ( -9.828310488886039309, -1.690483450353358119, 455.0000000000000568 ) ) ;
#59697=DIRECTION ( 'NONE',  ( 0.000000000000000000, 3.673940397442059868E-16, -1.000000000000000000 ) ) ;
#59705=CARTESIAN_POINT ( 'NONE',  ( 12.00648345035338060, -7.826483450353395988, 195.0000000000000284 ) ) ;
#59707=CARTESIAN_POINT ( 'NONE',  ( -11.11351654964671631, -2.906483450353335218, 455.0000000000000568 ) ) ;
#59709=ORIENTED_EDGE ( 'NONE', *, *, #20057, .F. ) ;
#59710=CARTESIAN_POINT ( 'NONE',  ( -2.752095193409374030, 9.942044687070435316, 455.0000000000000568 ) ) ;
#59725=ADVANCED_FACE ( 'NONE', ( #17644 ), #11978, .F. ) ;
#59726=EDGE_CURVE ( 'NONE', #49724, #3924, #23987, .T. ) ;
#59729=ORIENTED_EDGE ( 'NONE', *, *, #66103, .T. ) ;
#59733=FACE_OUTER_BOUND ( 'NONE', #51975, .T. ) ;
#59737=DIRECTION ( 'NONE',  ( -0.000000000000000000, -0.000000000000000000, -1.000000000000000000 ) ) ;
#59756=FACE_OUTER_BOUND ( 'NONE', #69828, .T. ) ;
#59761=CARTESIAN_POINT ( 'NONE',  ( -10.91351654964675610, -9.106483450353326958, 195.0000000000000284 ) ) ;
#59768=CARTESIAN_POINT ( 'NONE',  ( -11.47551654964667733, 11.07551654964660237, 455.0000000000000568 ) ) ;
#59772=CARTESIAN_POINT ( 'NONE',  ( -11.07551654964667520, 9.791916549646639822, 455.0000000000000568 ) ) ;
#59773=EDGE_LOOP ( 'NONE', ( #39537, #47222, #58248, #68156, #14089, #23531, #19452, #66185, #12733, #68164, #67298, #22453, #1524, #30409, #7005, #63226, #38358 ) ) ;
#59785=CARTESIAN_POINT ( 'NONE',  ( 8.406483450353379183, -6.344579767990839336, 195.0000000000000284 ) ) ;
#59800=AXIS2_PLACEMENT_3D ( 'NONE', #58363, #37481, #59043 ) ;
#59814=ORIENTED_EDGE ( 'NONE', *, *, #33339, .F. ) ;
#59822=ADVANCED_FACE ( 'NONE', ( #49491 ), #12665, .T. ) ;
#59826=CARTESIAN_POINT ( 'NONE',  ( 9.804883450353456098, 11.07551654964653132, 455.0000000000000568 ) ) ;
#59831=ORIENTED_EDGE ( 'NONE', *, *, #11252, .F. ) ;
#59835=DIRECTION ( 'NONE',  ( -3.016910393003147986E-15, 1.000000000000000000, 3.673940397442060361E-16 ) ) ;
#59849=LINE ( 'NONE', #64819, #21209 ) ;
#59855=EDGE_CURVE ( 'NONE', #23669, #33316, #3826, .T. ) ;
#59859=DIRECTION ( 'NONE',  ( -0.7071067811865530128, -0.7071067811865421326, 0.000000000000000000 ) ) ;
#59862=VECTOR ( 'NONE', #65029, 1000.000000000000000 ) ;
#59871=DIRECTION ( 'NONE',  ( -0.000000000000000000, -0.000000000000000000, -1.000000000000000000 ) ) ;
#59873=VECTOR ( 'NONE', #53247, 1000.000000000000000 ) ;
#59874=DIRECTION ( 'NONE',  ( 0.7071067811865514585, 0.7071067811865435759, -0.000000000000000000 ) ) ;
#59884=DIRECTION ( 'NONE',  ( -1.836970198721029934E-16, 1.836970198721036344E-16, -1.000000000000000000 ) ) ;
#59886=DIRECTION ( 'NONE',  ( 0.000000000000000000, 1.000000000000000000, 0.000000000000000000 ) ) ;
#59887=DIRECTION ( 'NONE',  ( -1.000000000000000000, 0.000000000000000000, 0.000000000000000000 ) ) ;
#59890=ORIENTED_EDGE ( 'NONE', *, *, #50607, .F. ) ;
#59895=AXIS2_PLACEMENT_3D ( 'NONE', #66655, #35515, #23526 ) ;
#59901=EDGE_CURVE ( 'NONE', #22220, #66935, #29639, .T. ) ;
#59902=AXIS2_PLACEMENT_3D ( 'NONE', #46733, #60980, #24828 ) ;
#59905=EDGE_CURVE ( 'NONE', #35824, #64638, #24698, .T. ) ;
#59906=VERTEX_POINT ( 'NONE', #24344 ) ;
#59908=VECTOR ( 'NONE', #65962, 1000.000000000000000 ) ;
#59914=EDGE_CURVE ( 'NONE', #47230, #53423, #36350, .T. ) ;
#59918=ORIENTED_EDGE ( 'NONE', *, *, #41295, .F. ) ;
#59924=EDGE_LOOP ( 'NONE', ( #42500, #1902, #46611, #2640 ) ) ;
#59934=PLANE ( 'NONE',  #28894 ) ;
#59936=VERTEX_POINT ( 'NONE', #62876 ) ;
#59939=AXIS2_PLACEMENT_3D ( 'NONE', #59768, #49161, #54128 ) ;
#59941=FACE_OUTER_BOUND ( 'NONE', #39931, .T. ) ;
#59953=CARTESIAN_POINT ( 'NONE',  ( -4.727349090213463612, 7.798499376343949407, 195.0000000000000284 ) ) ;
#59958=ADVANCED_FACE ( 'NONE', ( #67495 ), #9137, .F. ) ;
#59963=VERTEX_POINT ( 'NONE', #19382 ) ;
#59968=LINE ( 'NONE', #65624, #30900 ) ;
#59972=FACE_OUTER_BOUND ( 'NONE', #44493, .T. ) ;
#59976=PLANE ( 'NONE',  #25079 ) ;
#59979=ORIENTED_EDGE ( 'NONE', *, *, #36682, .F. ) ;
#59983=VECTOR ( 'NONE', #5446, 1000.000000000000000 ) ;
#59986=EDGE_CURVE ( 'NONE', #68597, #29795, #35637, .T. ) ;
#59991=CYLINDRICAL_SURFACE ( 'NONE', #64027, 2.204799999999997429 ) ;
#60002=EDGE_LOOP ( 'NONE', ( #69017, #64876, #51767, #35259 ) ) ;
#60011=FACE_OUTER_BOUND ( 'NONE', #46095, .T. ) ;
#60012=ORIENTED_EDGE ( 'NONE', *, *, #69892, .T. ) ;
#60013=EDGE_CURVE ( 'NONE', #56701, #67879, #3990, .T. ) ;
#60021=DIRECTION ( 'NONE',  ( -0.7071067811865500152, -0.7071067811865451302, 4.683861624749757595E-31 ) ) ;
#60025=DIRECTION ( 'NONE',  ( -0.000000000000000000, -0.000000000000000000, -1.000000000000000000 ) ) ;
#60030=CARTESIAN_POINT ( 'NONE',  ( -10.91351654964671525, -2.906483450353338771, 455.0000000000000568 ) ) ;
#60037=CARTESIAN_POINT ( 'NONE',  ( -5.993516549646776603, -6.006483450353426790, 455.0000000000000568 ) ) ;
#60039=DIRECTION ( 'NONE',  ( -0.000000000000000000, 3.673940397442059868E-16, -1.000000000000000000 ) ) ;
#60047=LINE ( 'NONE', #59710, #5170 ) ;
#60050=EDGE_CURVE ( 'NONE', #39788, #58819, #63587, .T. ) ;
#60064=DIRECTION ( 'NONE',  ( -0.000000000000000000, 3.673940397442059868E-16, -1.000000000000000000 ) ) ;
#60065=CARTESIAN_POINT ( 'NONE',  ( 10.09643294401454661, -9.306483450353491449, 455.0000000000000568 ) ) ;
#60071=VERTEX_POINT ( 'NONE', #43391 ) ;
#60078=DIRECTION ( 'NONE',  ( -1.836970198721029934E-16, 1.836970198721036344E-16, -1.000000000000000000 ) ) ;
#60087=VECTOR ( 'NONE', #11237, 1000.000000000000000 ) ;
#60089=EDGE_CURVE ( 'NONE', #23316, #24412, #64284, .T. ) ;
#60101=EDGE_CURVE ( 'NONE', #40247, #42678, #64621, .T. ) ;
#60106=DIRECTION ( 'NONE',  ( 1.836970198721029934E-16, 1.836970198721010706E-16, -1.000000000000000000 ) ) ;
#60128=CYLINDRICAL_SURFACE ( 'NONE', #11394, 2.204799999999997873 ) ;
#60132=CARTESIAN_POINT ( 'NONE',  ( 7.265214908726123078, -6.619341603356961201, 455.0000000000000568 ) ) ;
#60138=EDGE_LOOP ( 'NONE', ( #62763, #35582, #66776, #50021 ) ) ;
#60141=VERTEX_POINT ( 'NONE', #55067 ) ;
#60143=DIRECTION ( 'NONE',  ( 1.836970198721029934E-16, 1.836970198721010706E-16, -1.000000000000000000 ) ) ;
#60144=LINE ( 'NONE', #49206, #59217 ) ;
#60146=ORIENTED_EDGE ( 'NONE', *, *, #28258, .F. ) ;
#60148=LINE ( 'NONE', #21643, #19366 ) ;
#60153=CYLINDRICAL_SURFACE ( 'NONE', #55208, 1.399999999999998579 ) ;
#60156=CARTESIAN_POINT ( 'NONE',  ( 7.616533956692244978, 8.593516549646574632, 455.0000000000000568 ) ) ;
#60169=CIRCLE ( 'NONE', #55624, 0.1999999999999987899 ) ;
#60174=VERTEX_POINT ( 'NONE', #44416 ) ;
#60181=DIRECTION ( 'NONE',  ( -0.5000000000000068834, -0.8660254037844345998, 0.000000000000000000 ) ) ;
#60184=ORIENTED_EDGE ( 'NONE', *, *, #3710, .F. ) ;
#60192=CYLINDRICAL_SURFACE ( 'NONE', #28949, 0.1999999999999987899 ) ;
#60193=PLANE ( 'NONE',  #52120 ) ;
#60194=EDGE_CURVE ( 'NONE', #52241, #68881, #61996, .T. ) ;
#60204=CARTESIAN_POINT ( 'NONE',  ( -1.077516549646784449, -11.34648345035343198, 195.0000000000000284 ) ) ;
#60208=DIRECTION ( 'NONE',  ( -1.836970198721029934E-16, 1.836970198721036344E-16, -1.000000000000000000 ) ) ;
#60209=CIRCLE ( 'NONE', #29717, 0.1999999999999996503 ) ;
#60227=LINE ( 'NONE', #43635, #62816 ) ;
#60229=CARTESIAN_POINT ( 'NONE',  ( -4.193516549646673752, 11.31351654964658771, 455.0000000000000568 ) ) ;
#60230=DIRECTION ( 'NONE',  ( -1.836970198721029934E-16, 1.836970198721036344E-16, -1.000000000000000000 ) ) ;
#60242=LINE ( 'NONE', #28407, #43193 ) ;
#60244=ORIENTED_EDGE ( 'NONE', *, *, #50170, .T. ) ;
#60260=VERTEX_POINT ( 'NONE', #41495 ) ;
#60265=DIRECTION ( 'NONE',  ( 0.000000000000000000, -3.673940397442059868E-16, 1.000000000000000000 ) ) ;
#60271=LINE ( 'NONE', #49672, #54298 ) ;
#60274=EDGE_CURVE ( 'NONE', #19320, #62370, #15676, .T. ) ;
#60288=CARTESIAN_POINT ( 'NONE',  ( 6.006483450353379716, -6.006483450353490738, 455.0000000000000568 ) ) ;
#60289=FACE_OUTER_BOUND ( 'NONE', #49683, .T. ) ;
#60291=EDGE_CURVE ( 'NONE', #33734, #66887, #8603, .T. ) ;
#60294=AXIS2_PLACEMENT_3D ( 'NONE', #40056, #13201, #7884 ) ;
#60301=VECTOR ( 'NONE', #42233, 1000.000000000000114 ) ;
#60319=CARTESIAN_POINT ( 'NONE',  ( 7.606483450353373144, 11.31351654964662323, 195.0000000000000284 ) ) ;
#60320=ORIENTED_EDGE ( 'NONE', *, *, #14167, .T. ) ;
#60322=CYLINDRICAL_SURFACE ( 'NONE', #45295, 2.204799999999998761 ) ;
#60325=DIRECTION ( 'NONE',  ( -1.836970198721029934E-16, 1.836970198721036344E-16, -1.000000000000000000 ) ) ;
#60344=ORIENTED_EDGE ( 'NONE', *, *, #66314, .F. ) ;
#60347=AXIS2_PLACEMENT_3D ( 'NONE', #44622, #67255, #18810 ) ;
#60349=CYLINDRICAL_SURFACE ( 'NONE', #19994, 1.399999999999999245 ) ;
#60351=AXIS2_PLACEMENT_3D ( 'NONE', #36034, #57604, #47697 ) ;
#60355=EDGE_CURVE ( 'NONE', #13793, #47124, #42181, .T. ) ;
#60357=ORIENTED_EDGE ( 'NONE', *, *, #26431, .F. ) ;
#60365=CARTESIAN_POINT ( 'NONE',  ( 7.811466277050743479, 4.727349090213326832, 455.0000000000000568 ) ) ;
#60371=EDGE_CURVE ( 'NONE', #60571, #18478, #16404, .T. ) ;
#60379=DIRECTION ( 'NONE',  ( -0.000000000000000000, 3.673940397442059868E-16, -1.000000000000000000 ) ) ;
#60382=VERTEX_POINT ( 'NONE', #10707 ) ;
#60384=CARTESIAN_POINT ( 'NONE',  ( 4.740315990920143108, 4.188533722949256521, 195.0000000000000284 ) ) ;
#60386=DIRECTION ( 'NONE',  ( 1.000000000000000000, 2.135044278125301343E-15, -0.000000000000000000 ) ) ;
#60391=EDGE_LOOP ( 'NONE', ( #17383, #47254, #54594, #25761 ) ) ;
#60399=EDGE_CURVE ( 'NONE', #44650, #60071, #7388, .T. ) ;
#60400=CARTESIAN_POINT ( 'NONE',  ( -11.07551654964677290, -10.20488345035332500, 195.0000000000000284 ) ) ;
#60405=LINE ( 'NONE', #66057, #18150 ) ;
#60407=EDGE_CURVE ( 'NONE', #62060, #60909, #27330, .T. ) ;
#60411=VECTOR ( 'NONE', #30648, 1000.000000000000000 ) ;
#60420=ORIENTED_EDGE ( 'NONE', *, *, #68697, .F. ) ;
#60421=ORIENTED_EDGE ( 'NONE', *, *, #67789, .T. ) ;
#60423=EDGE_CURVE ( 'NONE', #18487, #31408, #32280, .T. ) ;
#60425=LINE ( 'NONE', #12323, #60749 ) ;
#60440=DIRECTION ( 'NONE',  ( 1.000000000000000000, -7.808916176531286882E-15, -2.868949260119708725E-30 ) ) ;
#60446=CARTESIAN_POINT ( 'NONE',  ( 4.396432944014527777, -8.406483450353478659, 455.0000000000000568 ) ) ;
#60452=ORIENTED_EDGE ( 'NONE', *, *, #57023, .F. ) ;
#60454=LINE ( 'NONE', #17675, #59609 ) ;
#60458=DIRECTION ( 'NONE',  ( -1.000000000000000000, 0.000000000000000000, 0.000000000000000000 ) ) ;
#60460=AXIS2_PLACEMENT_3D ( 'NONE', #19302, #45119, #18964 ) ;
#60467=CARTESIAN_POINT ( 'NONE',  ( 11.32648345035337734, -7.606483450353397124, 195.0000000000000284 ) ) ;
#60478=DIRECTION ( 'NONE',  ( 1.000000000000000000, 0.000000000000000000, 0.000000000000000000 ) ) ;
#60479=CARTESIAN_POINT ( 'NONE',  ( -6.331612867284154511, 8.393516549646601987, 195.0000000000000284 ) ) ;
#60483=CARTESIAN_POINT ( 'NONE',  ( -8.393516549646712122, 6.331612867284047041, 455.0000000000000568 ) ) ;
#60487=DIRECTION ( 'NONE',  ( -1.000000000000000000, 0.000000000000000000, 0.000000000000000000 ) ) ;
#60491=PLANE ( 'NONE',  #37765 ) ;
#60492=LINE ( 'NONE', #52246, #10355 ) ;
#60493=ORIENTED_EDGE ( 'NONE', *, *, #32241, .T. ) ;
#60494=ORIENTED_EDGE ( 'NONE', *, *, #53426, .T. ) ;
#60502=CARTESIAN_POINT ( 'NONE',  ( -9.791916549646712653, 10.19191654964664018, 455.0000000000000568 ) ) ;
#60503=CARTESIAN_POINT ( 'NONE',  ( -11.77351654964669336, -4.186483450353275515, 195.0000000000000284 ) ) ;
#60506=AXIS2_PLACEMENT_3D ( 'NONE', #52194, #30287, #51852 ) ;
#60508=VECTOR ( 'NONE', #44239, 1000.000000000000114 ) ;
#60509=PLANE ( 'NONE',  #41145 ) ;
#60510=DIRECTION ( 'NONE',  ( -0.000000000000000000, -0.000000000000000000, -1.000000000000000000 ) ) ;
#60529=EDGE_CURVE ( 'NONE', #9740, #12989, #33659, .T. ) ;
#60532=DIRECTION ( 'NONE',  ( -1.836970198721029934E-16, 1.836970198721036344E-16, -1.000000000000000000 ) ) ;
#60534=CARTESIAN_POINT ( 'NONE',  ( -6.606374702650259501, -7.265214908726163046, 455.0000000000000568 ) ) ;
#60535=AXIS2_PLACEMENT_3D ( 'NONE', #64838, #22044, #16048 ) ;
#60536=CARTESIAN_POINT ( 'NONE',  ( -10.19191654964671301, 9.791916549646639822, 455.0000000000000568 ) ) ;
#60539=CARTESIAN_POINT ( 'NONE',  ( -4.734785091273957747, 5.380658396643156038, 455.0000000000000568 ) ) ;
#60551=ORIENTED_EDGE ( 'NONE', *, *, #46094, .T. ) ;
#60564=ORIENTED_EDGE ( 'NONE', *, *, #3887, .T. ) ;
#60565=VECTOR ( 'NONE', #37509, 1000.000000000000000 ) ;
#60569=VERTEX_POINT ( 'NONE', #55918 ) ;
#60571=VERTEX_POINT ( 'NONE', #46005 ) ;
#60572=ORIENTED_EDGE ( 'NONE', *, *, #34163, .T. ) ;
#60579=CYLINDRICAL_SURFACE ( 'NONE', #39642, 0.3999999999999993006 ) ;
#60580=ORIENTED_EDGE ( 'NONE', *, *, #46564, .F. ) ;
#60582=EDGE_LOOP ( 'NONE', ( #47465, #68025, #11879, #60766 ) ) ;
#60587=CARTESIAN_POINT ( 'NONE',  ( -1.077516549646676092, 10.73351654964656454, 455.0000000000000568 ) ) ;
#60589=VECTOR ( 'NONE', #64747, 1000.000000000000000 ) ;
#60591=DIRECTION ( 'NONE',  ( -1.000000000000000000, 0.000000000000000000, 0.000000000000000000 ) ) ;
#60600=ORIENTED_EDGE ( 'NONE', *, *, #50287, .T. ) ;
#60601=DIRECTION ( 'NONE',  ( -0.5000000000000004441, 0.8660254037844383745, 3.181725716174720005E-16 ) ) ;
#60602=EDGE_CURVE ( 'NONE', #17661, #5817, #34686, .T. ) ;
#60612=CARTESIAN_POINT ( 'NONE',  ( 2.706483450353350584, -10.09643294401453595, 195.0000000000000284 ) ) ;
#60620=CARTESIAN_POINT ( 'NONE',  ( 7.826483450353380000, -12.00648345035349251, 455.0000000000000568 ) ) ;
#60621=ORIENTED_EDGE ( 'NONE', *, *, #59726, .T. ) ;
#60622=FACE_OUTER_BOUND ( 'NONE', #28481, .T. ) ;
#60637=ORIENTED_EDGE ( 'NONE', *, *, #33808, .T. ) ;
#60644=ORIENTED_EDGE ( 'NONE', *, *, #31555, .T. ) ;
#60658=CARTESIAN_POINT ( 'NONE',  ( -7.603567055985545942, 8.393516549646601987, 195.0000000000000284 ) ) ;
#60662=CARTESIAN_POINT ( 'NONE',  ( 11.48848345035334617, -10.20488345035352928, 455.0000000000000568 ) ) ;
#60665=DIRECTION ( 'NONE',  ( -0.000000000000000000, -0.000000000000000000, -1.000000000000000000 ) ) ;
#60666=PLANE ( 'NONE',  #40137 ) ;
#60672=DIRECTION ( 'NONE',  ( 0.000000000000000000, 1.000000000000000000, 0.000000000000000000 ) ) ;
#60676=ORIENTED_EDGE ( 'NONE', *, *, #10519, .T. ) ;
#60678=ORIENTED_EDGE ( 'NONE', *, *, #26974, .F. ) ;
#60680=CARTESIAN_POINT ( 'NONE',  ( -2.693516549646827851, -10.92648345035345692, 455.0000000000000568 ) ) ;
#60683=FACE_OUTER_BOUND ( 'NONE', #18382, .T. ) ;
#60695=VECTOR ( 'NONE', #49364, 1000.000000000000000 ) ;
#60705=EDGE_LOOP ( 'NONE', ( #4753, #5463, #38993, #49151 ) ) ;
#60709=DIRECTION ( 'NONE',  ( -0.6414496315691698980, -0.7671651518152895477, -2.587583378555116957E-16 ) ) ;
#60713=DIRECTION ( 'NONE',  ( -1.836970198721029934E-16, 1.836970198721036344E-16, -1.000000000000000000 ) ) ;
#60717=ADVANCED_FACE ( 'NONE', ( #30797 ), #35742, .F. ) ;
#60723=CARTESIAN_POINT ( 'NONE',  ( 9.306483450353379538, -10.92648345035348534, 455.0000000000000568 ) ) ;
#60724=EDGE_LOOP ( 'NONE', ( #30432, #7742, #3223, #61188 ) ) ;
#60727=DIRECTION ( 'NONE',  ( 1.836970198721029934E-16, 1.836970198721010706E-16, -1.000000000000000000 ) ) ;
#60729=DIRECTION ( 'NONE',  ( -1.000000000000000000, 0.000000000000000000, 0.000000000000000000 ) ) ;
#60735=ORIENTED_EDGE ( 'NONE', *, *, #5356, .F. ) ;
#60736=CARTESIAN_POINT ( 'NONE',  ( 1.090483450353343819, -10.74648345035335772, 195.0000000000000284 ) ) ;
#60748=CARTESIAN_POINT ( 'NONE',  ( -11.31351654964679021, -7.806483450353372433, 455.0000000000000568 ) ) ;
#60749=VECTOR ( 'NONE', #43834, 1000.000000000000000 ) ;
#60751=LINE ( 'NONE', #23274, #42350 ) ;
#60757=EDGE_LOOP ( 'NONE', ( #3494, #25217, #50780, #36976 ) ) ;
#60761=CARTESIAN_POINT ( 'NONE',  ( -7.603567055985637424, -8.606483450353410447, 455.0000000000000568 ) ) ;
#60762=CARTESIAN_POINT ( 'NONE',  ( 7.811466277050743479, 4.727349090213326832, 455.0000000000000568 ) ) ;
#60766=ORIENTED_EDGE ( 'NONE', *, *, #45631, .T. ) ;
#60773=EDGE_LOOP ( 'NONE', ( #2208, #58266, #49117, #17194 ) ) ;
#60778=DIRECTION ( 'NONE',  ( -1.000000000000000000, -0.000000000000000000, -0.000000000000000000 ) ) ;
#60784=FACE_OUTER_BOUND ( 'NONE', #60391, .T. ) ;
#60786=ORIENTED_EDGE ( 'NONE', *, *, #33339, .T. ) ;
#60792=DIRECTION ( 'NONE',  ( 8.728482790395504563E-15, 1.000000000000000000, 3.673940397442059868E-16 ) ) ;
#60793=CARTESIAN_POINT ( 'NONE',  ( -9.942044687070568543, 2.752095193409294982, 455.0000000000000568 ) ) ;
#60796=PLANE ( 'NONE',  #9789 ) ;
#60806=DIRECTION ( 'NONE',  ( 1.836970198721029934E-16, 1.836970198721010706E-16, -1.000000000000000000 ) ) ;
#60808=VECTOR ( 'NONE', #42570, 1000.000000000000000 ) ;
#60810=ORIENTED_EDGE ( 'NONE', *, *, #39808, .T. ) ;
#60812=DIRECTION ( 'NONE',  ( 1.000000000000000000, -8.339399738404102667E-15, 0.000000000000000000 ) ) ;
#60822=DIRECTION ( 'NONE',  ( -1.000000000000000000, 8.339399738404101090E-15, -1.836970198721014896E-16 ) ) ;
#60830=DIRECTION ( 'NONE',  ( 0.6414496315691526895, 0.7671651518153038696, 2.587583378555111534E-16 ) ) ;
#60833=CARTESIAN_POINT ( 'NONE',  ( 7.811466277050727491, 7.259684009079840905, 195.0000000000000284 ) ) ;
#60835=EDGE_LOOP ( 'NONE', ( #42319, #9759, #49331, #9757 ) ) ;
#60838=ORIENTED_EDGE ( 'NONE', *, *, #47993, .T. ) ;
#60848=VERTEX_POINT ( 'NONE', #43482 ) ;
#60857=CIRCLE ( 'NONE', #30387, 0.1999999999999987899 ) ;
#60870=DIRECTION ( 'NONE',  ( 0.000000000000000000, -1.000000000000000000, 0.000000000000000000 ) ) ;
#60875=CARTESIAN_POINT ( 'NONE',  ( -11.99351654964674374, -4.186483450353318148, 455.0000000000000568 ) ) ;
#60876=DIRECTION ( 'NONE',  ( -0.000000000000000000, 3.673940397442059868E-16, -1.000000000000000000 ) ) ;
#60878=PLANE ( 'NONE',  #50709 ) ;
#60888=VERTEX_POINT ( 'NONE', #11644 ) ;
#60900=DIRECTION ( 'NONE',  ( 1.047444401652939849E-14, 1.000000000000000000, 0.000000000000000000 ) ) ;
#60901=EDGE_CURVE ( 'NONE', #58346, #17426, #19931, .T. ) ;
#60905=ORIENTED_EDGE ( 'NONE', *, *, #5604, .T. ) ;
#60909=VERTEX_POINT ( 'NONE', #10618 ) ;
#60927=ORIENTED_EDGE ( 'NONE', *, *, #38462, .F. ) ;
#60929=EDGE_CURVE ( 'NONE', #64997, #3474, #8616, .T. ) ;
#60930=DIRECTION ( 'NONE',  ( -8.802523127157697409E-15, -1.000000000000000000, -1.836970198721026976E-16 ) ) ;
#60932=ORIENTED_EDGE ( 'NONE', *, *, #53528, .F. ) ;
#60933=ORIENTED_EDGE ( 'NONE', *, *, #16792, .F. ) ;
#60936=DIRECTION ( 'NONE',  ( 0.7671651518152985405, 0.6414496315691592399, -2.309356642088639737E-17 ) ) ;
#60938=CIRCLE ( 'NONE', #14673, 0.5999999999999989786 ) ;
#60943=ORIENTED_EDGE ( 'NONE', *, *, #24346, .T. ) ;
#60948=ORIENTED_EDGE ( 'NONE', *, *, #37064, .T. ) ;
#60949=VECTOR ( 'NONE', #20491, 1000.000000000000114 ) ;
#60954=CARTESIAN_POINT ( 'NONE',  ( 11.78648345035337819, -7.606483450353493936, 455.0000000000000568 ) ) ;
#60956=CYLINDRICAL_SURFACE ( 'NONE', #20028, 0.5999999999999998668 ) ;
#60972=DIRECTION ( 'NONE',  ( -2.891205793294683355E-15, -1.000000000000000000, 0.000000000000000000 ) ) ;
#60980=DIRECTION ( 'NONE',  ( 0.7671651518153173033, 0.6414496315691367023, 2.587583378555109069E-16 ) ) ;
#60982=DIRECTION ( 'NONE',  ( -1.047444401652939849E-14, -1.000000000000000000, 0.000000000000000000 ) ) ;
#60987=DIRECTION ( 'NONE',  ( 0.000000000000000000, -3.673940397442059868E-16, 1.000000000000000000 ) ) ;
#60995=DIRECTION ( 'NONE',  ( -1.836970198721029934E-16, 1.836970198721036344E-16, -1.000000000000000000 ) ) ;
#60997=DIRECTION ( 'NONE',  ( 0.000000000000000000, 3.673940397442059868E-16, -1.000000000000000000 ) ) ;
#61008=EDGE_LOOP ( 'NONE', ( #46361, #58017, #52551, #33012 ) ) ;
#61014=DIRECTION ( 'NONE',  ( 1.000000000000000000, 0.000000000000000000, 0.000000000000000000 ) ) ;
#61019=ORIENTED_EDGE ( 'NONE', *, *, #9945, .T. ) ;
#61025=ORIENTED_EDGE ( 'NONE', *, *, #63656, .T. ) ;
#61032=CARTESIAN_POINT ( 'NONE',  ( 4.206483450353343478, -11.12648345035347575, 455.0000000000000568 ) ) ;
#61041=VECTOR ( 'NONE', #16423, 1000.000000000000000 ) ;
#61051=ADVANCED_FACE ( 'NONE', ( #44511 ), #50532, .F. ) ;
#61061=DIRECTION ( 'NONE',  ( -1.836970198721029934E-16, 1.836970198721036344E-16, -1.000000000000000000 ) ) ;
#61063=VECTOR ( 'NONE', #27148, 1000.000000000000000 ) ;
#61074=CARTESIAN_POINT ( 'NONE',  ( -10.08346604330787777, 9.293516549646602343, 455.0000000000000568 ) ) ;
#61076=AXIS2_PLACEMENT_3D ( 'NONE', #50976, #50278, #2883 ) ;
#61079=VECTOR ( 'NONE', #66536, 1000.000000000000000 ) ;
#61082=EDGE_LOOP ( 'NONE', ( #46149, #37540, #15993, #15480 ) ) ;
#61086=VECTOR ( 'NONE', #18230, 1000.000000000000000 ) ;
#61087=CARTESIAN_POINT ( 'NONE',  ( -7.813516549646836395, -11.78648345035340661, 455.0000000000000568 ) ) ;
#61091=LINE ( 'NONE', #44483, #64607 ) ;
#61102=CARTESIAN_POINT ( 'NONE',  ( -10.91351654964670814, 9.093516549646603053, 195.0000000000000284 ) ) ;
#61126=VECTOR ( 'NONE', #16649, 1000.000000000000000 ) ;
#61130=DIRECTION ( 'NONE',  ( 1.000000000000000000, -1.047444401652940007E-14, 1.836970198721010706E-16 ) ) ;
#61131=VERTEX_POINT ( 'NONE', #24352 ) ;
#61132=PLANE ( 'NONE',  #16716 ) ;
#61134=DIRECTION ( 'NONE',  ( -0.000000000000000000, -0.000000000000000000, -1.000000000000000000 ) ) ;
#61144=DIRECTION ( 'NONE',  ( 4.121462285523434458E-16, 1.000000000000000000, 0.000000000000000000 ) ) ;
#61167=PLANE ( 'NONE',  #67775 ) ;
#61169=VERTEX_POINT ( 'NONE', #46965 ) ;
#61172=DIRECTION ( 'NONE',  ( -0.7071067811865474617, 0.7071067811865474617, -0.000000000000000000 ) ) ;
#61177=CYLINDRICAL_SURFACE ( 'NONE', #65714, 0.1999999999999996503 ) ;
#61178=ORIENTED_EDGE ( 'NONE', *, *, #7188, .F. ) ;
#61181=LINE ( 'NONE', #12739, #6009 ) ;
#61188=ORIENTED_EDGE ( 'NONE', *, *, #9838, .T. ) ;
#61194=CARTESIAN_POINT ( 'NONE',  ( -7.415254214038309755, -3.606483450353353160, 195.0000000000000284 ) ) ;
#61197=VERTEX_POINT ( 'NONE', #3840 ) ;
#61204=ORIENTED_EDGE ( 'NONE', *, *, #15147, .F. ) ;
#61207=DIRECTION ( 'NONE',  ( 1.000000000000000000, 0.000000000000000000, 0.000000000000000000 ) ) ;
#61208=ORIENTED_EDGE ( 'NONE', *, *, #37152, .T. ) ;
#61209=DIRECTION ( 'NONE',  ( -1.836970198721029934E-16, 1.836970198721036344E-16, -1.000000000000000000 ) ) ;
#61210=CARTESIAN_POINT ( 'NONE',  ( 12.00648345035338060, -4.186483450353396307, 195.0000000000000284 ) ) ;
#61235=VECTOR ( 'NONE', #23465, 1000.000000000000000 ) ;
#61237=CARTESIAN_POINT ( 'NONE',  ( -8.593516549646711411, 7.603567055985436696, 455.0000000000000568 ) ) ;
#61244=EDGE_LOOP ( 'NONE', ( #35035, #23824, #49882, #30764 ) ) ;
#61249=ORIENTED_EDGE ( 'NONE', *, *, #41609, .T. ) ;
#61255=DIRECTION ( 'NONE',  ( -1.836970198721029934E-16, 1.836970198721036344E-16, -1.000000000000000000 ) ) ;
#61257=CYLINDRICAL_SURFACE ( 'NONE', #14798, 1.399999999999999245 ) ;
#61263=EDGE_CURVE ( 'NONE', #26074, #19113, #32470, .T. ) ;
#61268=ORIENTED_EDGE ( 'NONE', *, *, #50607, .T. ) ;
#61274=EDGE_CURVE ( 'NONE', #64371, #5737, #32109, .T. ) ;
#61276=ORIENTED_EDGE ( 'NONE', *, *, #4287, .T. ) ;
#61283=ORIENTED_EDGE ( 'NONE', *, *, #15769, .T. ) ;
#61288=CARTESIAN_POINT ( 'NONE',  ( 10.92648345035337343, -2.706483450353395437, 195.0000000000000284 ) ) ;
#61291=CIRCLE ( 'NONE', #55662, 1.399999999999998579 ) ;
#61297=EDGE_CURVE ( 'NONE', #59237, #22525, #58287, .T. ) ;
#61302=DIRECTION ( 'NONE',  ( -1.000000000000000000, 0.000000000000000000, 0.000000000000000000 ) ) ;
#61327=CARTESIAN_POINT ( 'NONE',  ( 6.344579767990853547, 8.393516549646580671, 455.0000000000000568 ) ) ;
#61328=ADVANCED_FACE ( 'NONE', ( #15598 ), #42794, .F. ) ;
#61337=LINE ( 'NONE', #12895, #19209 ) ;
#61339=CYLINDRICAL_SURFACE ( 'NONE', #4908, 0.1999999999999987899 ) ;
#61342=CARTESIAN_POINT ( 'NONE',  ( 12.00648345035341968, 11.18071654964654726, 455.0000000000000568 ) ) ;
#61343=ORIENTED_EDGE ( 'NONE', *, *, #44487, .T. ) ;
#61352=ORIENTED_EDGE ( 'NONE', *, *, #13761, .T. ) ;
#61360=ADVANCED_FACE ( 'NONE', ( #59756 ), #5339, .F. ) ;
#61368=VERTEX_POINT ( 'NONE', #10976 ) ;
#61389=ORIENTED_EDGE ( 'NONE', *, *, #16062, .F. ) ;
#61399=VERTEX_POINT ( 'NONE', #64039 ) ;
#61402=EDGE_CURVE ( 'NONE', #26427, #59671, #69666, .T. ) ;
#61404=CARTESIAN_POINT ( 'NONE',  ( 11.48848345035342078, 11.07551654964652599, 455.0000000000000568 ) ) ;
#61411=ORIENTED_EDGE ( 'NONE', *, *, #24633, .F. ) ;
#61412=DIRECTION ( 'NONE',  ( 0.000000000000000000, 1.000000000000000000, 0.000000000000000000 ) ) ;
#61413=LINE ( 'NONE', #39846, #48699 ) ;
#61420=ORIENTED_EDGE ( 'NONE', *, *, #30749, .T. ) ;
#61423=CARTESIAN_POINT ( 'NONE',  ( -9.404046420174124066, 1.853252480934674873, 455.0000000000000568 ) ) ;
#61427=AXIS2_PLACEMENT_3D ( 'NONE', #25450, #8830, #3535 ) ;
#61429=FACE_OUTER_BOUND ( 'NONE', #44667, .T. ) ;
#61436=LINE ( 'NONE', #2751, #41722 ) ;
#61442=EDGE_CURVE ( 'NONE', #14683, #23727, #54799, .T. ) ;
#61445=CARTESIAN_POINT ( 'NONE',  ( 11.32648345035337734, -7.606483450353492159, 455.0000000000000568 ) ) ;
#61454=EDGE_CURVE ( 'NONE', #13193, #45555, #21093, .T. ) ;
#61457=EDGE_CURVE ( 'NONE', #16734, #15307, #8672, .T. ) ;
#61459=CARTESIAN_POINT ( 'NONE',  ( 10.20488345035338007, -11.08848345035349325, 455.0000000000000568 ) ) ;
#61467=CARTESIAN_POINT ( 'NONE',  ( 2.906483450353420039, 10.91351654964658913, 455.0000000000000568 ) ) ;
#61475=DIRECTION ( 'NONE',  ( -0.000000000000000000, -0.000000000000000000, -1.000000000000000000 ) ) ;
#61486=VERTEX_POINT ( 'NONE', #39221 ) ;
#61488=DIRECTION ( 'NONE',  ( -1.000000000000000000, 3.016910393003147986E-15, 0.000000000000000000 ) ) ;
#61493=VECTOR ( 'NONE', #1419, 1000.000000000000000 ) ;
#61495=DIRECTION ( 'NONE',  ( 0.000000000000000000, 1.000000000000000000, 0.000000000000000000 ) ) ;
#61496=EDGE_CURVE ( 'NONE', #55024, #29674, #53874, .T. ) ;
#61497=CARTESIAN_POINT ( 'NONE',  ( -4.193516549646831848, -11.12648345035344377, 455.0000000000000568 ) ) ;
#61498=ADVANCED_FACE ( 'NONE', ( #60784 ), #55147, .F. ) ;
#61510=LINE ( 'NONE', #22666, #37668 ) ;
#61526=CARTESIAN_POINT ( 'NONE',  ( 4.396432944014577515, 8.593516549646585290, 455.0000000000000568 ) ) ;
#61527=LINE ( 'NONE', #55894, #41082 ) ;
#61528=LINE ( 'NONE', #23714, #11636 ) ;
#61546=AXIS2_PLACEMENT_3D ( 'NONE', #47739, #25837, #68964 ) ;
#61550=AXIS2_PLACEMENT_3D ( 'NONE', #3995, #68706, #14595 ) ;
#61553=EDGE_LOOP ( 'NONE', ( #56300, #3576, #63762, #1285 ) ) ;
#61559=AXIS2_PLACEMENT_3D ( 'NONE', #46471, #68048, #35872 ) ;
#61561=LINE ( 'NONE', #41407, #4639 ) ;
#61562=DIRECTION ( 'NONE',  ( 1.000000000000000000, 0.000000000000000000, 0.000000000000000000 ) ) ;
#61565=ORIENTED_EDGE ( 'NONE', *, *, #67090, .F. ) ;
#61569=CARTESIAN_POINT ( 'NONE',  ( 4.186483450353423841, 11.99351654964658742, 455.0000000000000568 ) ) ;
#61576=ORIENTED_EDGE ( 'NONE', *, *, #36596, .T. ) ;
#61578=CARTESIAN_POINT ( 'NONE',  ( 4.622483450353394474, 3.593516549646586622, 455.0000000000000568 ) ) ;
#61579=CIRCLE ( 'NONE', #16442, 1.399999999999998579 ) ;
#61587=VECTOR ( 'NONE', #6910, 1000.000000000000000 ) ;
#61588=DIRECTION ( 'NONE',  ( -0.000000000000000000, -0.000000000000000000, -1.000000000000000000 ) ) ;
#61590=AXIS2_PLACEMENT_3D ( 'NONE', #9678, #31260, #52832 ) ;
#61592=VECTOR ( 'NONE', #56265, 1000.000000000000000 ) ;
#61605=DIRECTION ( 'NONE',  ( -0.7071067811865401342, 0.7071067811865550112, 0.000000000000000000 ) ) ;
#61612=DIRECTION ( 'NONE',  ( -1.079558018506126467E-14, -1.000000000000000000, 0.000000000000000000 ) ) ;
#61621=AXIS2_PLACEMENT_3D ( 'NONE', #11582, #651, #32491 ) ;
#61622=DIRECTION ( 'NONE',  ( 1.000000000000000000, 0.000000000000000000, 0.000000000000000000 ) ) ;
#61626=ORIENTED_EDGE ( 'NONE', *, *, #30749, .F. ) ;
#61642=AXIS2_PLACEMENT_3D ( 'NONE', #56405, #56754, #2318 ) ;
#61647=AXIS2_PLACEMENT_3D ( 'NONE', #11106, #161, #11782 ) ;
#61650=PLANE ( 'NONE',  #55956 ) ;
#61660=DIRECTION ( 'NONE',  ( -0.000000000000000000, -0.000000000000000000, -1.000000000000000000 ) ) ;
#61666=FACE_OUTER_BOUND ( 'NONE', #17364, .T. ) ;
#61675=EDGE_LOOP ( 'NONE', ( #57040, #30055, #40920, #65414 ) ) ;
#61678=DIRECTION ( 'NONE',  ( 1.836970198721029934E-16, 1.836970198721010706E-16, -1.000000000000000000 ) ) ;
#61679=EDGE_CURVE ( 'NONE', #44259, #39509, #53918, .T. ) ;
#61686=DIRECTION ( 'NONE',  ( 0.000000000000000000, 1.000000000000000000, 0.000000000000000000 ) ) ;
#61694=DIRECTION ( 'NONE',  ( 0.000000000000000000, -3.673940397442059868E-16, 1.000000000000000000 ) ) ;
#61695=AXIS2_PLACEMENT_3D ( 'NONE', #32898, #34260, #11657 ) ;
#61733=ORIENTED_EDGE ( 'NONE', *, *, #12911, .T. ) ;
#61734=ORIENTED_EDGE ( 'NONE', *, *, #12125, .T. ) ;
#61751=VECTOR ( 'NONE', #47331, 1000.000000000000000 ) ;
#61763=VECTOR ( 'NONE', #47420, 1000.000000000000000 ) ;
#61774=EDGE_CURVE ( 'NONE', #1311, #50458, #11145, .T. ) ;
#61791=LINE ( 'NONE', #46565, #45196 ) ;
#61795=LINE ( 'NONE', #62133, #69542 ) ;
#61806=VECTOR ( 'NONE', #26384, 1000.000000000000000 ) ;
#61820=VERTEX_POINT ( 'NONE', #64901 ) ;
#61835=VECTOR ( 'NONE', #8008, 1000.000000000000000 ) ;
#61839=EDGE_LOOP ( 'NONE', ( #18522, #4790, #1813, #48779 ) ) ;
#61848=CARTESIAN_POINT ( 'NONE',  ( -11.11351654964674118, -4.206483450353336373, 455.0000000000000568 ) ) ;
#61860=DIRECTION ( 'NONE',  ( 1.000000000000000000, 0.000000000000000000, 0.000000000000000000 ) ) ;
#61883=CARTESIAN_POINT ( 'NONE',  ( -9.234937905884079257, -9.955011587777201854, 195.0000000000000284 ) ) ;
#61885=DIRECTION ( 'NONE',  ( -0.7071067811865446862, -0.7071067811865503483, 0.000000000000000000 ) ) ;
#61887=ORIENTED_EDGE ( 'NONE', *, *, #26224, .T. ) ;
#61903=EDGE_LOOP ( 'NONE', ( #16193, #8293, #69726, #6728 ) ) ;
#61906=ORIENTED_EDGE ( 'NONE', *, *, #27658, .F. ) ;
#61918=ORIENTED_EDGE ( 'NONE', *, *, #64922, .F. ) ;
#61924=LINE ( 'NONE', #3235, #29447 ) ;
#61938=ORIENTED_EDGE ( 'NONE', *, *, #32681, .T. ) ;
#61946=CARTESIAN_POINT ( 'NONE',  ( -5.993516549646776603, -6.006483450353426790, 455.0000000000000568 ) ) ;
#61951=ADVANCED_FACE ( 'NONE', ( #68023 ), #60956, .F. ) ;
#61958=ORIENTED_EDGE ( 'NONE', *, *, #49443, .F. ) ;
#61962=DIRECTION ( 'NONE',  ( 0.000000000000000000, 3.673940397442059868E-16, -1.000000000000000000 ) ) ;
#61970=CARTESIAN_POINT ( 'NONE',  ( 12.00648345035338238, 4.173516549646515195, 455.0000000000000568 ) ) ;
#61978=VECTOR ( 'NONE', #14909, 1000.000000000000000 ) ;
#61982=ORIENTED_EDGE ( 'NONE', *, *, #31010, .T. ) ;
#61984=FACE_OUTER_BOUND ( 'NONE', #39390, .T. ) ;
#61985=PLANE ( 'NONE',  #60294 ) ;
#61992=EDGE_CURVE ( 'NONE', #31845, #46179, #7911, .T. ) ;
#61995=EDGE_LOOP ( 'NONE', ( #69605, #27952, #26027, #5975 ) ) ;
#61996=LINE ( 'NONE', #12241, #1743 ) ;
#62000=FACE_OUTER_BOUND ( 'NONE', #60757, .T. ) ;
#62016=ORIENTED_EDGE ( 'NONE', *, *, #59527, .T. ) ;
#62021=VERTEX_POINT ( 'NONE', #29487 ) ;
#62027=LINE ( 'NONE', #14312, #31349 ) ;
#62033=PLANE ( 'NONE',  #43957 ) ;
#62034=CARTESIAN_POINT ( 'NONE',  ( 8.606483450353334064, 4.383466043307767457, 195.0000000000000284 ) ) ;
#62039=PLANE ( 'NONE',  #20838 ) ;
#62049=CYLINDRICAL_SURFACE ( 'NONE', #3489, 0.5999999999999989786 ) ;
#62050=ORIENTED_EDGE ( 'NONE', *, *, #50368, .F. ) ;
#62055=ORIENTED_EDGE ( 'NONE', *, *, #44666, .T. ) ;
#62057=ORIENTED_EDGE ( 'NONE', *, *, #56689, .T. ) ;
#62060=VERTEX_POINT ( 'NONE', #35844 ) ;
#62061=VERTEX_POINT ( 'NONE', #48211 ) ;
#62067=EDGE_LOOP ( 'NONE', ( #45158, #50522, #28856, #68203 ) ) ;
#62069=LINE ( 'NONE', #22862, #48219 ) ;
#62076=FACE_OUTER_BOUND ( 'NONE', #29630, .T. ) ;
#62080=CIRCLE ( 'NONE', #42922, 2.204799999999997429 ) ;
#62081=ORIENTED_EDGE ( 'NONE', *, *, #21340, .T. ) ;
#62083=EDGE_CURVE ( 'NONE', #8462, #28622, #10377, .T. ) ;
#62084=CARTESIAN_POINT ( 'NONE',  ( 10.74648345035337904, -1.690483450353490680, 455.0000000000000568 ) ) ;
#62086=EDGE_CURVE ( 'NONE', #44680, #56867, #41142, .T. ) ;
#62089=AXIS2_PLACEMENT_3D ( 'NONE', #11175, #43715, #234 ) ;
#62095=VERTEX_POINT ( 'NONE', #26639 ) ;
#62105=DIRECTION ( 'NONE',  ( 1.000000000000000000, 0.000000000000000000, 0.000000000000000000 ) ) ;
#62111=EDGE_CURVE ( 'NONE', #20447, #325, #13251, .T. ) ;
#62113=CARTESIAN_POINT ( 'NONE',  ( 9.106483450353380249, -10.92648345035339297, 195.0000000000000284 ) ) ;
#62124=CARTESIAN_POINT ( 'NONE',  ( -8.393516549646712122, 6.331612867284047041, 195.0000000000000284 ) ) ;
#62125=EDGE_CURVE ( 'NONE', #40441, #58819, #19933, .T. ) ;
#62132=AXIS2_PLACEMENT_3D ( 'NONE', #25226, #19915, #41490 ) ;
#62133=CARTESIAN_POINT ( 'NONE',  ( -4.383466043307968185, -8.406483450353443132, 455.0000000000000568 ) ) ;
#62134=VERTEX_POINT ( 'NONE', #36915 ) ;
#62136=EDGE_CURVE ( 'NONE', #6331, #59936, #5071, .T. ) ;
#62141=ORIENTED_EDGE ( 'NONE', *, *, #1543, .T. ) ;
#62145=ORIENTED_EDGE ( 'NONE', *, *, #65693, .F. ) ;
#62147=LINE ( 'NONE', #13371, #22595 ) ;
#62148=CARTESIAN_POINT ( 'NONE',  ( -10.91351654964680584, -9.106483450353376696, 455.0000000000000568 ) ) ;
#62165=ADVANCED_FACE ( 'NONE', ( #52467 ), #53181, .F. ) ;
#62173=EDGE_CURVE ( 'NONE', #59597, #14943, #46015, .T. ) ;
#62192=EDGE_CURVE ( 'NONE', #29982, #15138, #59849, .T. ) ;
#62195=EDGE_CURVE ( 'NONE', #3591, #3786, #42894, .T. ) ;
#62202=EDGE_CURVE ( 'NONE', #5389, #39722, #16371, .T. ) ;
#62208=CARTESIAN_POINT ( 'NONE',  ( 10.92648345035337343, -2.706483450353490916, 455.0000000000000568 ) ) ;
#62214=CARTESIAN_POINT ( 'NONE',  ( -9.942044687070668019, -9.247904806590694804, 455.0000000000000568 ) ) ;
#62219=ADVANCED_FACE ( 'NONE', ( #54215 ), #21683, .F. ) ;
#62240=FACE_OUTER_BOUND ( 'NONE', #37846, .T. ) ;
#62243=DIRECTION ( 'NONE',  ( 1.836970198721029934E-16, -1.836970198721036344E-16, 1.000000000000000000 ) ) ;
#62254=VECTOR ( 'NONE', #19142, 1000.000000000000000 ) ;
#62261=ORIENTED_EDGE ( 'NONE', *, *, #51347, .F. ) ;
#62273=ORIENTED_EDGE ( 'NONE', *, *, #60089, .F. ) ;
#62292=CYLINDRICAL_SURFACE ( 'NONE', #11152, 0.5999999999999998668 ) ;
#62293=ORIENTED_EDGE ( 'NONE', *, *, #36677, .T. ) ;
#62295=PLANE ( 'NONE',  #63290 ) ;
#62296=ORIENTED_EDGE ( 'NONE', *, *, #37793, .F. ) ;
#62299=EDGE_CURVE ( 'NONE', #65403, #3828, #15563, .T. ) ;
#62302=VERTEX_POINT ( 'NONE', #65510 ) ;
#62303=CARTESIAN_POINT ( 'NONE',  ( 7.826483450353380000, -11.78648345035349010, 455.0000000000000568 ) ) ;
#62307=PLANE ( 'NONE',  #18860 ) ;
#62322=CARTESIAN_POINT ( 'NONE',  ( -11.77351654964670935, 4.173516549646604901, 195.0000000000000284 ) ) ;
#62331=DIRECTION ( 'NONE',  ( -0.000000000000000000, 0.000000000000000000, -1.000000000000000000 ) ) ;
#62334=CARTESIAN_POINT ( 'NONE',  ( 8.606483450353380249, -7.616533956692325802, 455.0000000000000568 ) ) ;
#62348=EDGE_CURVE ( 'NONE', #49054, #39974, #42638, .T. ) ;
#62349=ADVANCED_FACE ( 'NONE', ( #40708 ), #29053, .F. ) ;
#62352=ORIENTED_EDGE ( 'NONE', *, *, #11192, .T. ) ;
#62357=CIRCLE ( 'NONE', #58993, 0.4000000000000010214 ) ;
#62362=VECTOR ( 'NONE', #27388, 1000.000000000000000 ) ;
#62363=DIRECTION ( 'NONE',  ( 8.339399738404099512E-15, 1.000000000000000000, 1.836970198721025990E-16 ) ) ;
#62366=DIRECTION ( 'NONE',  ( 0.7071067811865474617, 0.7071067811865474617, 2.597868168706479611E-16 ) ) ;
#62370=VERTEX_POINT ( 'NONE', #46017 ) ;
#62380=FACE_OUTER_BOUND ( 'NONE', #49404, .T. ) ;
#62383=EDGE_CURVE ( 'NONE', #36022, #47486, #13836, .T. ) ;
#62390=DIRECTION ( 'NONE',  ( -2.891205793294675467E-15, -1.000000000000000000, 0.000000000000000000 ) ) ;
#62399=LINE ( 'NONE', #20672, #41309 ) ;
#62402=LINE ( 'NONE', #1974, #6986 ) ;
#62403=ORIENTED_EDGE ( 'NONE', *, *, #57023, .T. ) ;
#62407=DIRECTION ( 'NONE',  ( -1.000000000000000000, 1.671920889371702657E-15, 0.000000000000000000 ) ) ;
#62416=VERTEX_POINT ( 'NONE', #2182 ) ;
#62417=VECTOR ( 'NONE', #52231, 1000.000000000000114 ) ;
#62429=EDGE_CURVE ( 'NONE', #62021, #58452, #12424, .T. ) ;
#62456=AXIS2_PLACEMENT_3D ( 'NONE', #14660, #6737, #45600 ) ;
#62459=ORIENTED_EDGE ( 'NONE', *, *, #56129, .F. ) ;
#62462=CARTESIAN_POINT ( 'NONE',  ( -1.077516549646670541, 11.33351654964656596, 455.0000000000000568 ) ) ;
#62464=CARTESIAN_POINT ( 'NONE',  ( -9.093516549646771807, -10.09643294401451286, 195.0000000000000284 ) ) ;
#62475=CARTESIAN_POINT ( 'NONE',  ( -4.393516549646667713, 11.77351654964658856, 455.0000000000000568 ) ) ;
#62477=CARTESIAN_POINT ( 'NONE',  ( -4.727349090213461835, 4.188533722949259186, 455.0000000000000568 ) ) ;
#62487=ORIENTED_EDGE ( 'NONE', *, *, #48517, .F. ) ;
#62489=DIRECTION ( 'NONE',  ( -1.836970198721029934E-16, 1.836970198721036344E-16, -1.000000000000000000 ) ) ;
#62494=FACE_OUTER_BOUND ( 'NONE', #59087, .T. ) ;
#62500=EDGE_LOOP ( 'NONE', ( #54972, #33469, #46501, #52094 ) ) ;
#62513=EDGE_CURVE ( 'NONE', #20566, #49587, #14538, .T. ) ;
#62523=CIRCLE ( 'NONE', #51225, 1.399999999999998579 ) ;
#62528=EDGE_LOOP ( 'NONE', ( #51918, #50965, #4492, #31949 ) ) ;
#62531=LINE ( 'NONE', #39910, #40464 ) ;
#62540=CARTESIAN_POINT ( 'NONE',  ( 12.00648345035340903, 7.813516549646560172, 455.0000000000000568 ) ) ;
#62542=DIRECTION ( 'NONE',  ( 1.000000000000000000, -1.047444401652940007E-14, 1.836970198721010706E-16 ) ) ;
#62551=CARTESIAN_POINT ( 'NONE',  ( 4.206483450353374565, 11.31351654964663034, 195.0000000000000284 ) ) ;
#62553=AXIS2_PLACEMENT_3D ( 'NONE', #54756, #59018, #5290 ) ;
#62554=ORIENTED_EDGE ( 'NONE', *, *, #37452, .T. ) ;
#62562=AXIS2_PLACEMENT_3D ( 'NONE', #6530, #16437, #27394 ) ;
#62565=EDGE_LOOP ( 'NONE', ( #55299, #51376, #57357, #49326 ) ) ;
#62569=VECTOR ( 'NONE', #4606, 1000.000000000000000 ) ;
#62573=EDGE_CURVE ( 'NONE', #27098, #12341, #45908, .T. ) ;
#62580=DIRECTION ( 'NONE',  ( 0.000000000000000000, 1.000000000000000000, 0.000000000000000000 ) ) ;
#62585=VERTEX_POINT ( 'NONE', #47762 ) ;
#62601=DIRECTION ( 'NONE',  ( -1.836970198721029934E-16, 1.836970198721036344E-16, -1.000000000000000000 ) ) ;
#62602=EDGE_CURVE ( 'NONE', #51028, #62370, #3588, .T. ) ;
#62605=ADVANCED_FACE ( 'NONE', ( #64388 ), #16646, .T. ) ;
#62607=DIRECTION ( 'NONE',  ( -0.000000000000000000, 3.673940397442059868E-16, -1.000000000000000000 ) ) ;
#62617=VECTOR ( 'NONE', #58801, 1000.000000000000000 ) ;
#62621=ORIENTED_EDGE ( 'NONE', *, *, #27658, .T. ) ;
#62622=ORIENTED_EDGE ( 'NONE', *, *, #9607, .T. ) ;
#62644=EDGE_LOOP ( 'NONE', ( #53832, #7280, #31338, #23488 ) ) ;
#62659=ADVANCED_FACE ( 'NONE', ( #21254 ), #32202, .F. ) ;
#62667=ORIENTED_EDGE ( 'NONE', *, *, #13835, .T. ) ;
#62677=VECTOR ( 'NONE', #37063, 999.9999999999998863 ) ;
#62679=CARTESIAN_POINT ( 'NONE',  ( -5.993516549646711766, 5.993516549646603409, 455.0000000000000568 ) ) ;
#62680=ORIENTED_EDGE ( 'NONE', *, *, #62086, .F. ) ;
#62683=ADVANCED_FACE ( 'NONE', ( #64725 ), #37513, .F. ) ;
#62684=VECTOR ( 'NONE', #14960, 1000.000000000000000 ) ;
#62698=VERTEX_POINT ( 'NONE', #16281 ) ;
#62703=ORIENTED_EDGE ( 'NONE', *, *, #62125, .T. ) ;
#62705=CARTESIAN_POINT ( 'NONE',  ( 11.19368345035340973, 11.99351654964656433, 455.0000000000000568 ) ) ;
#62708=CARTESIAN_POINT ( 'NONE',  ( 1.690483450353344352, -10.74648345035336128, 195.0000000000000284 ) ) ;
#62711=ORIENTED_EDGE ( 'NONE', *, *, #30879, .F. ) ;
#62713=AXIS2_PLACEMENT_3D ( 'NONE', #11949, #5977, #54083 ) ;
#62723=CARTESIAN_POINT ( 'NONE',  ( -6.331612867284154511, 8.393516549646601987, 455.0000000000000568 ) ) ;
#62736=VECTOR ( 'NONE', #21534, 1000.000000000000114 ) ;
#62741=CARTESIAN_POINT ( 'NONE',  ( 9.417013320880792904, -1.866219381641466279, 195.0000000000000284 ) ) ;
#62746=ORIENTED_EDGE ( 'NONE', *, *, #43622, .T. ) ;
#62748=CYLINDRICAL_SURFACE ( 'NONE', #59895, 0.8128000000000145109 ) ;
#62761=CARTESIAN_POINT ( 'NONE',  ( -3.593516549646712299, 4.609516549646604844, 455.0000000000000568 ) ) ;
#62763=ORIENTED_EDGE ( 'NONE', *, *, #28447, .F. ) ;
#62771=CARTESIAN_POINT ( 'NONE',  ( 7.826483450353380000, -11.78648345035349010, 455.0000000000000568 ) ) ;
#62776=CIRCLE ( 'NONE', #53766, 1.399999999999999245 ) ;
#62792=VERTEX_POINT ( 'NONE', #56193 ) ;
#62795=ADVANCED_FACE ( 'NONE', ( #6701 ), #50539, .F. ) ;
#62797=DIRECTION ( 'NONE',  ( 1.000000000000000000, 3.016910393003147986E-15, 0.000000000000000000 ) ) ;
#62801=ORIENTED_EDGE ( 'NONE', *, *, #29321, .F. ) ;
#62809=CARTESIAN_POINT ( 'NONE',  ( 11.78648345035340661, 7.593516549646560421, 455.0000000000000568 ) ) ;
#62816=VECTOR ( 'NONE', #64859, 1000.000000000000000 ) ;
#62828=DIRECTION ( 'NONE',  ( 1.000000000000000000, 0.000000000000000000, 0.000000000000000000 ) ) ;
#62829=DIRECTION ( 'NONE',  ( 0.000000000000000000, 3.673940397442059868E-16, -1.000000000000000000 ) ) ;
#62830=DIRECTION ( 'NONE',  ( -1.000000000000000000, 0.000000000000000000, 0.000000000000000000 ) ) ;
#62840=CARTESIAN_POINT ( 'NONE',  ( 8.406483450353404052, 6.331612867284015955, 455.0000000000000568 ) ) ;
#62843=EDGE_CURVE ( 'NONE', #54850, #59438, #2443, .T. ) ;
#62844=VERTEX_POINT ( 'NONE', #55839 ) ;
#62861=LINE ( 'NONE', #9830, #13554 ) ;
#62863=CYLINDRICAL_SURFACE ( 'NONE', #41180, 0.5999999999999998668 ) ;
#62864=CIRCLE ( 'NONE', #64003, 1.399999999999999245 ) ;
#62870=LINE ( 'NONE', #29990, #15034 ) ;
#62871=ORIENTED_EDGE ( 'NONE', *, *, #53675, .T. ) ;
#62876=CARTESIAN_POINT ( 'NONE',  ( 8.465062094116026614, 4.242044687070459119, 195.0000000000000284 ) ) ;
#62879=CIRCLE ( 'NONE', #38067, 0.5999999999999998668 ) ;
#62883=VERTEX_POINT ( 'NONE', #67144 ) ;
#62886=ADVANCED_FACE ( 'NONE', ( #8085 ), #3502, .F. ) ;
#62889=AXIS2_PLACEMENT_3D ( 'NONE', #14438, #20084, #3476 ) ;
#62894=VECTOR ( 'NONE', #16196, 1000.000000000000000 ) ;
#62895=DIRECTION ( 'NONE',  ( -1.836970198721029934E-16, -1.836970198721010706E-16, 1.000000000000000000 ) ) ;
#62896=DIRECTION ( 'NONE',  ( 0.7671651518152998728, -0.6414496315691575745, 2.309356642088859447E-17 ) ) ;
#62910=FACE_OUTER_BOUND ( 'NONE', #48526, .T. ) ;
#62922=LINE ( 'NONE', #35685, #53214 ) ;
#62923=ORIENTED_EDGE ( 'NONE', *, *, #7721, .T. ) ;
#62937=ORIENTED_EDGE ( 'NONE', *, *, #22335, .F. ) ;
#62944=EDGE_CURVE ( 'NONE', #44953, #35986, #52653, .T. ) ;
#62951=DIRECTION ( 'NONE',  ( 0.000000000000000000, 3.673940397442059868E-16, -1.000000000000000000 ) ) ;
#62958=CARTESIAN_POINT ( 'NONE',  ( -5.993516549646799696, -8.211283450353425550, 455.0000000000000568 ) ) ;
#62967=ORIENTED_EDGE ( 'NONE', *, *, #26898, .T. ) ;
#62968=DIRECTION ( 'NONE',  ( -1.000000000000000000, 0.000000000000000000, 0.000000000000000000 ) ) ;
#62970=VERTEX_POINT ( 'NONE', #40965 ) ;
#62977=CIRCLE ( 'NONE', #11045, 0.1999999999999987899 ) ;
#62996=EDGE_CURVE ( 'NONE', #13374, #5297, #51942, .T. ) ;
#62998=ORIENTED_EDGE ( 'NONE', *, *, #22736, .F. ) ;
#62999=LINE ( 'NONE', #51697, #16853 ) ;
#63003=VECTOR ( 'NONE', #68825, 1000.000000000000000 ) ;
#63016=ORIENTED_EDGE ( 'NONE', *, *, #28183, .T. ) ;
#63018=DIRECTION ( 'NONE',  ( 1.047444401652940007E-14, 1.000000000000000000, 1.836970198721029934E-16 ) ) ;
#63026=LINE ( 'NONE', #14582, #41934 ) ;
#63040=CARTESIAN_POINT ( 'NONE',  ( -11.11351654964670743, 2.893516549646604208, 455.0000000000000568 ) ) ;
#63048=CARTESIAN_POINT ( 'NONE',  ( -2.752095193409373586, 9.942044687070435316, 195.0000000000000284 ) ) ;
#63061=EDGE_LOOP ( 'NONE', ( #25178, #40221, #32165, #68391 ) ) ;
#63065=ORIENTED_EDGE ( 'NONE', *, *, #25872, .T. ) ;
#63066=EDGE_CURVE ( 'NONE', #26162, #64793, #42372, .T. ) ;
#63070=CARTESIAN_POINT ( 'NONE',  ( -10.19191654964680893, -10.20488345035333566, 195.0000000000000284 ) ) ;
#63071=ORIENTED_EDGE ( 'NONE', *, *, #1543, .F. ) ;
#63073=CARTESIAN_POINT ( 'NONE',  ( 11.08848345035334404, -11.08848345035349148, 455.0000000000000568 ) ) ;
#63087=ADVANCED_FACE ( 'NONE', ( #54730 ), #49069, .F. ) ;
#63095=ADVANCED_FACE ( 'NONE', ( #26827 ), #43410, .F. ) ;
#63097=CIRCLE ( 'NONE', #26973, 0.1999999999999987899 ) ;
#63107=CARTESIAN_POINT ( 'NONE',  ( -11.11351654964679270, -7.806483450353373321, 455.0000000000000568 ) ) ;
#63112=ORIENTED_EDGE ( 'NONE', *, *, #38624, .F. ) ;
#63118=DIRECTION ( 'NONE',  ( -1.836970198721029934E-16, 1.836970198721036344E-16, -1.000000000000000000 ) ) ;
#63122=ORIENTED_EDGE ( 'NONE', *, *, #1835, .F. ) ;
#63128=VECTOR ( 'NONE', #431, 1000.000000000000000 ) ;
#63131=ORIENTED_EDGE ( 'NONE', *, *, #16058, .F. ) ;
#63132=FACE_OUTER_BOUND ( 'NONE', #61244, .T. ) ;
#63134=CARTESIAN_POINT ( 'NONE',  ( 7.265214908726139065, 5.380658396643097419, 455.0000000000000568 ) ) ;
#63135=ORIENTED_EDGE ( 'NONE', *, *, #4432, .F. ) ;
#63140=CARTESIAN_POINT ( 'NONE',  ( 11.08848345035342042, 11.47551654964652812, 455.0000000000000568 ) ) ;
#63147=CARTESIAN_POINT ( 'NONE',  ( 9.955011587777175208, 2.752095193409277663, 195.0000000000000284 ) ) ;
#63157=ORIENTED_EDGE ( 'NONE', *, *, #32569, .T. ) ;
#63173=AXIS2_PLACEMENT_3D ( 'NONE', #10594, #20166, #58701 ) ;
#63174=CARTESIAN_POINT ( 'NONE',  ( 12.00648345035338060, -4.186483450353492231, 455.0000000000000568 ) ) ;
#63178=DIRECTION ( 'NONE',  ( 1.836970198721029934E-16, 1.836970198721010706E-16, -1.000000000000000000 ) ) ;
#63187=PLANE ( 'NONE',  #37801 ) ;
#63192=ADVANCED_FACE ( 'NONE', ( #28870 ), #45480, .F. ) ;
#63196=VERTEX_POINT ( 'NONE', #22886 ) ;
#63198=DIRECTION ( 'NONE',  ( 8.673617379884013384E-15, 1.000000000000000000, 0.000000000000000000 ) ) ;
#63201=ORIENTED_EDGE ( 'NONE', *, *, #68472, .T. ) ;
#63202=DIRECTION ( 'NONE',  ( 0.000000000000000000, 0.000000000000000000, 1.000000000000000000 ) ) ;
#63208=FACE_OUTER_BOUND ( 'NONE', #33721, .T. ) ;
#63216=CARTESIAN_POINT ( 'NONE',  ( 3.606483450353406006, 7.415254214038213831, 455.0000000000000568 ) ) ;
#63219=ORIENTED_EDGE ( 'NONE', *, *, #47515, .T. ) ;
#63224=VECTOR ( 'NONE', #49727, 1000.000000000000000 ) ;
#63226=ORIENTED_EDGE ( 'NONE', *, *, #42312, .T. ) ;
#63227=EDGE_CURVE ( 'NONE', #32424, #13109, #45131, .T. ) ;
#63229=CIRCLE ( 'NONE', #4542, 0.1999999999999987899 ) ;
#63233=AXIS2_PLACEMENT_3D ( 'NONE', #63870, #15775, #57503 ) ;
#63239=AXIS2_PLACEMENT_3D ( 'NONE', #2046, #19004, #18292 ) ;
#63251=DIRECTION ( 'NONE',  ( 3.614007241618349165E-15, 1.000000000000000000, 0.000000000000000000 ) ) ;
#63256=AXIS2_PLACEMENT_3D ( 'NONE', #11753, #33338, #27686 ) ;
#63268=DIRECTION ( 'NONE',  ( 3.540573132209561620E-15, 1.000000000000000000, 0.000000000000000000 ) ) ;
#63270=FACE_OUTER_BOUND ( 'NONE', #13526, .T. ) ;
#63290=AXIS2_PLACEMENT_3D ( 'NONE', #66304, #17862, #13863 ) ;
#63296=CARTESIAN_POINT ( 'NONE',  ( -5.993516549646711766, 5.993516549646603409, 455.0000000000000568 ) ) ;
#63297=ORIENTED_EDGE ( 'NONE', *, *, #7030, .T. ) ;
#63301=ORIENTED_EDGE ( 'NONE', *, *, #55417, .T. ) ;
#63314=ORIENTED_EDGE ( 'NONE', *, *, #8478, .F. ) ;
#63315=ORIENTED_EDGE ( 'NONE', *, *, #50611, .F. ) ;
#63323=EDGE_LOOP ( 'NONE', ( #44136, #5372, #3634, #5009 ) ) ;
#63327=VECTOR ( 'NONE', #62896, 999.9999999999998863 ) ;
#63329=EDGE_CURVE ( 'NONE', #35173, #43873, #40532, .T. ) ;
#63330=CIRCLE ( 'NONE', #32844, 1.399999999999998579 ) ;
#63334=EDGE_CURVE ( 'NONE', #31845, #13045, #46186, .T. ) ;
#63338=ORIENTED_EDGE ( 'NONE', *, *, #54622, .T. ) ;
#63339=VECTOR ( 'NONE', #26579, 1000.000000000000000 ) ;
#63340=DIRECTION ( 'NONE',  ( -1.000000000000000000, 0.000000000000000000, 0.000000000000000000 ) ) ;
#63345=PRODUCT_DEFINITION ( 'UNKNOWN', '', #9905, #11961 ) ;
#63364=FACE_OUTER_BOUND ( 'NONE', #12169, .T. ) ;
#63365=EDGE_LOOP ( 'NONE', ( #23423, #38274, #53353, #39296 ) ) ;
#63368=DIRECTION ( 'NONE',  ( -1.000000000000000000, 0.000000000000000000, 0.000000000000000000 ) ) ;
#63370=VECTOR ( 'NONE', #14367, 1000.000000000000000 ) ;
#63371=LINE ( 'NONE', #8560, #1122 ) ;
#63373=EDGE_LOOP ( 'NONE', ( #29124, #56176, #48904, #22935 ) ) ;
#63380=ORIENTED_EDGE ( 'NONE', *, *, #38896, .T. ) ;
#63381=ORIENTED_EDGE ( 'NONE', *, *, #24123, .F. ) ;
#63384=ORIENTED_EDGE ( 'NONE', *, *, #58817, .F. ) ;
#63390=VECTOR ( 'NONE', #60379, 1000.000000000000000 ) ;
#63391=FACE_OUTER_BOUND ( 'NONE', #41593, .T. ) ;
#63394=DIRECTION ( 'NONE',  ( -0.000000000000000000, -1.000000000000000000, -0.000000000000000000 ) ) ;
#63415=ORIENTED_EDGE ( 'NONE', *, *, #62429, .F. ) ;
#63440=CARTESIAN_POINT ( 'NONE',  ( -9.942044687070568543, 2.752095193409294982, 455.0000000000000568 ) ) ;
#63448=CARTESIAN_POINT ( 'NONE',  ( -8.513516549646713116, 11.29351654964659701, 195.0000000000000284 ) ) ;
#63453=DIRECTION ( 'NONE',  ( 1.836970198721029934E-16, -1.836970198721036344E-16, 1.000000000000000000 ) ) ;
#63454=CARTESIAN_POINT ( 'NONE',  ( -8.393516549646792058, -7.616533956692236096, 455.0000000000000568 ) ) ;
#63457=FACE_OUTER_BOUND ( 'NONE', #66592, .T. ) ;
#63459=CYLINDRICAL_SURFACE ( 'NONE', #7236, 0.2000000000000005107 ) ;
#63464=DIRECTION ( 'NONE',  ( 8.673617379884087537E-15, 1.000000000000000000, 0.000000000000000000 ) ) ;
#63482=ADVANCED_FACE ( 'NONE', ( #59941 ), #53269, .T. ) ;
#63487=ORIENTED_EDGE ( 'NONE', *, *, #28109, .F. ) ;
#63495=EDGE_CURVE ( 'NONE', #66935, #3246, #872, .T. ) ;
#63504=CARTESIAN_POINT ( 'NONE',  ( 9.417013320880792904, -1.866219381641561315, 455.0000000000000568 ) ) ;
#63512=EDGE_CURVE ( 'NONE', #51301, #45555, #42641, .T. ) ;
#63514=ORIENTED_EDGE ( 'NONE', *, *, #28525, .F. ) ;
#63515=ORIENTED_EDGE ( 'NONE', *, *, #18726, .F. ) ;
#63518=EDGE_CURVE ( 'NONE', #1406, #8462, #26734, .T. ) ;
#63528=CARTESIAN_POINT ( 'NONE',  ( -10.08346604330787777, 9.093516549646603053, 455.0000000000000568 ) ) ;
#63535=FACE_OUTER_BOUND ( 'NONE', #6691, .T. ) ;
#63546=DIRECTION ( 'NONE',  ( -1.000000000000000000, 0.000000000000000000, 0.000000000000000000 ) ) ;
#63555=VERTEX_POINT ( 'NONE', #42986 ) ;
#63564=ORIENTED_EDGE ( 'NONE', *, *, #49640, .T. ) ;
#63570=DIRECTION ( 'NONE',  ( -0.7071067811865503483, -0.7071067811865446862, 0.000000000000000000 ) ) ;
#63571=ORIENTED_EDGE ( 'NONE', *, *, #7343, .F. ) ;
#63573=CARTESIAN_POINT ( 'NONE',  ( 9.804883450353379715, -11.08848345035349325, 455.0000000000000568 ) ) ;
#63577=CARTESIAN_POINT ( 'NONE',  ( -7.393516549646710345, 5.993516549646603409, 455.0000000000000568 ) ) ;
#63579=CARTESIAN_POINT ( 'NONE',  ( -5.655420232009250370, 8.393516549646600211, 195.0000000000000284 ) ) ;
#63587=LINE ( 'NONE', #16534, #42392 ) ;
#63593=ORIENTED_EDGE ( 'NONE', *, *, #27414, .T. ) ;
#63594=ORIENTED_EDGE ( 'NONE', *, *, #40978, .F. ) ;
#63597=ORIENTED_EDGE ( 'NONE', *, *, #37452, .F. ) ;
#63601=ADVANCED_FACE ( 'NONE', ( #13145 ), #50634, .F. ) ;
#63613=DIRECTION ( 'NONE',  ( 3.717264591378875951E-15, 1.000000000000000000, 0.000000000000000000 ) ) ;
#63618=VECTOR ( 'NONE', #43072, 999.9999999999998863 ) ;
#63626=ORIENTED_EDGE ( 'NONE', *, *, #5352, .F. ) ;
#63627=CARTESIAN_POINT ( 'NONE',  ( -4.393516549646784952, -11.32648345035339510, 195.0000000000000284 ) ) ;
#63645=ORIENTED_EDGE ( 'NONE', *, *, #58817, .T. ) ;
#63652=PLANE ( 'NONE',  #57000 ) ;
#63653=ORIENTED_EDGE ( 'NONE', *, *, #56120, .T. ) ;
#63655=VERTEX_POINT ( 'NONE', #35056 ) ;
#63656=EDGE_CURVE ( 'NONE', #13045, #36255, #6662, .T. ) ;
#63664=LINE ( 'NONE', #14868, #19667 ) ;
#63679=CARTESIAN_POINT ( 'NONE',  ( 11.32648345035340576, 7.793516549646564151, 455.0000000000000568 ) ) ;
#63700=PLANE ( 'NONE',  #33518 ) ;
#63702=EDGE_CURVE ( 'NONE', #25592, #40341, #18097, .T. ) ;
#63708=ORIENTED_EDGE ( 'NONE', *, *, #27174, .F. ) ;
#63710=VECTOR ( 'NONE', #14838, 1000.000000000000000 ) ;
#63716=ORIENTED_EDGE ( 'NONE', *, *, #43010, .F. ) ;
#63737=EDGE_CURVE ( 'NONE', #67553, #68804, #47774, .T. ) ;
#63743=EDGE_CURVE ( 'NONE', #64507, #49054, #25523, .T. ) ;
#63744=CARTESIAN_POINT ( 'NONE',  ( 10.09643294401454661, -9.106483450353398013, 195.0000000000000284 ) ) ;
#63745=AXIS2_PLACEMENT_3D ( 'NONE', #28059, #59544, #493 ) ;
#63751=ORIENTED_EDGE ( 'NONE', *, *, #61457, .F. ) ;
#63752=VERTEX_POINT ( 'NONE', #53443 ) ;
#63754=LINE ( 'NONE', #24521, #3891 ) ;
#63757=VECTOR ( 'NONE', #27448, 1000.000000000000000 ) ;
#63762=ORIENTED_EDGE ( 'NONE', *, *, #31898, .T. ) ;
#63772=DIRECTION ( 'NONE',  ( -1.280238727658158235E-15, -1.000000000000000000, 0.000000000000000000 ) ) ;
#63773=ORIENTED_EDGE ( 'NONE', *, *, #57970, .T. ) ;
#63783=DIRECTION ( 'NONE',  ( 0.000000000000000000, 1.000000000000000000, 0.000000000000000000 ) ) ;
#63784=CARTESIAN_POINT ( 'NONE',  ( 6.006483450353379716, -8.211283450353491276, 455.0000000000000568 ) ) ;
#63787=DIRECTION ( 'NONE',  ( -0.7071067811865515695, -0.7071067811865435759, 0.000000000000000000 ) ) ;
#63789=FACE_OUTER_BOUND ( 'NONE', #32877, .T. ) ;
#63792=CARTESIAN_POINT ( 'NONE',  ( 9.247904806590689475, -9.955011587777349291, 455.0000000000000568 ) ) ;
#63798=EDGE_CURVE ( 'NONE', #29489, #29928, #30464, .T. ) ;
#63801=VECTOR ( 'NONE', #9972, 1000.000000000000000 ) ;
#63818=EDGE_LOOP ( 'NONE', ( #34323, #64613, #35747, #27589 ) ) ;
#63842=VECTOR ( 'NONE', #53554, 1000.000000000000000 ) ;
#63853=VECTOR ( 'NONE', #48710, 1000.000000000000000 ) ;
#63870=CARTESIAN_POINT ( 'NONE',  ( 9.841277389592701041, 2.277516549646538824, 455.0000000000000568 ) ) ;
#63871=LINE ( 'NONE', #38054, #18870 ) ;
#63885=PLANE ( 'NONE',  #34649 ) ;
#63891=CIRCLE ( 'NONE', #62713, 0.5999999999999998668 ) ;
#63906=VERTEX_POINT ( 'NONE', #17327 ) ;
#63916=CARTESIAN_POINT ( 'NONE',  ( -11.29351654964668583, 8.513516549646642062, 194.9999952000000292 ) ) ;
#63927=LINE ( 'NONE', #15491, #68450 ) ;
#63929=CARTESIAN_POINT ( 'NONE',  ( -10.91351654964670637, 2.693516549646604030, 455.0000000000000568 ) ) ;
#63931=EDGE_CURVE ( 'NONE', #28029, #20859, #6041, .T. ) ;
#63939=DIRECTION ( 'NONE',  ( -1.000000000000000000, 0.000000000000000000, 0.000000000000000000 ) ) ;
#63940=ORIENTED_EDGE ( 'NONE', *, *, #33156, .F. ) ;
#63941=VECTOR ( 'NONE', #42567, 1000.000000000000114 ) ;
#63946=EDGE_CURVE ( 'NONE', #4452, #43025, #49856, .T. ) ;
#63950=CARTESIAN_POINT ( 'NONE',  ( 4.186483450353337687, -11.78648345035347589, 455.0000000000000568 ) ) ;
#63962=ADVANCED_FACE ( 'NONE', ( #49 ), #15958, .F. ) ;
#63963=DIRECTION ( 'NONE',  ( 0.7071067811865441310, -0.7071067811865510144, -2.597868168706485034E-16 ) ) ;
#63969=CARTESIAN_POINT ( 'NONE',  ( 7.757955312929523117, -8.465062094116182934, 455.0000000000000568 ) ) ;
#63973=FACE_OUTER_BOUND ( 'NONE', #4948, .T. ) ;
#63977=DIRECTION ( 'NONE',  ( -0.5000000000000018874, -0.8660254037844374864, 0.000000000000000000 ) ) ;
#63980=AXIS2_PLACEMENT_3D ( 'NONE', #2973, #13924, #39737 ) ;
#64000=ORIENTED_EDGE ( 'NONE', *, *, #909, .F. ) ;
#64003=AXIS2_PLACEMENT_3D ( 'NONE', #67958, #4326, #57343 ) ;
#64013=DIRECTION ( 'NONE',  ( -0.000000000000000000, -0.000000000000000000, -1.000000000000000000 ) ) ;
#64014=EDGE_CURVE ( 'NONE', #38597, #7366, #6713, .T. ) ;
#64027=AXIS2_PLACEMENT_3D ( 'NONE', #54020, #6607, #11543 ) ;
#64028=FACE_OUTER_BOUND ( 'NONE', #3232, .T. ) ;
#64032=VERTEX_POINT ( 'NONE', #56888 ) ;
#64033=VERTEX_POINT ( 'NONE', #67523 ) ;
#64039=CARTESIAN_POINT ( 'NONE',  ( -5.655420232009250370, 8.393516549646600211, 455.0000000000000568 ) ) ;
#64044=CARTESIAN_POINT ( 'NONE',  ( -9.234937905884020637, 9.942044687070460185, 455.0000000000000568 ) ) ;
#64051=CIRCLE ( 'NONE', #23391, 2.204799999999997429 ) ;
#64053=ORIENTED_EDGE ( 'NONE', *, *, #65055, .F. ) ;
#64054=CARTESIAN_POINT ( 'NONE',  ( -11.33351654964663879, -1.090483450353281425, 195.0000000000000284 ) ) ;
#64057=CARTESIAN_POINT ( 'NONE',  ( -5.993516549646776603, -6.006483450353426790, 455.0000000000000568 ) ) ;
#64059=EDGE_CURVE ( 'NONE', #44826, #5610, #34266, .T. ) ;
#64099=CARTESIAN_POINT ( 'NONE',  ( 4.201500623656039934, 7.259684009079806266, 455.0000000000000568 ) ) ;
#64100=ORIENTED_EDGE ( 'NONE', *, *, #32385, .T. ) ;
#64107=EDGE_CURVE ( 'NONE', #59237, #8340, #18716, .T. ) ;
#64108=PLANE ( 'NONE',  #61550 ) ;
#64109=DIRECTION ( 'NONE',  ( -0.000000000000000000, -0.000000000000000000, -1.000000000000000000 ) ) ;
#64121=VECTOR ( 'NONE', #52837, 1000.000000000000000 ) ;
#64124=ORIENTED_EDGE ( 'NONE', *, *, #36659, .F. ) ;
#64126=ORIENTED_EDGE ( 'NONE', *, *, #66934, .F. ) ;
#64137=VERTEX_POINT ( 'NONE', #40285 ) ;
#64139=EDGE_CURVE ( 'NONE', #48487, #19877, #52250, .T. ) ;
#64145=DIRECTION ( 'NONE',  ( 1.836970198721029934E-16, 1.836970198721010706E-16, -1.000000000000000000 ) ) ;
#64148=FACE_OUTER_BOUND ( 'NONE', #32018, .T. ) ;
#64149=DIRECTION ( 'NONE',  ( 0.6414496315691445849, 0.7671651518153106419, -0.000000000000000000 ) ) ;
#64154=FACE_BOUND ( 'NONE', #19005, .T. ) ;
#64161=PLANE ( 'NONE',  #28360 ) ;
#64162=CARTESIAN_POINT ( 'NONE',  ( -7.793516549646712477, 11.11351654964660085, 455.0000000000000568 ) ) ;
#64166=EDGE_LOOP ( 'NONE', ( #232, #11016, #10097, #44244 ) ) ;
#64172=VECTOR ( 'NONE', #46857, 1000.000000000000000 ) ;
#64186=FACE_OUTER_BOUND ( 'NONE', #39280, .T. ) ;
#64190=ADVANCED_FACE ( 'NONE', ( #47342 ), #15177, .F. ) ;
#64191=LINE ( 'NONE', #37655, #17191 ) ;
#64200=ORIENTED_EDGE ( 'NONE', *, *, #28877, .F. ) ;
#64205=VERTEX_POINT ( 'NONE', #31089 ) ;
#64219=EDGE_CURVE ( 'NONE', #31408, #16734, #36743, .T. ) ;
#64223=ADVANCED_FACE ( 'NONE', ( #63973 ), #4227, .F. ) ;
#64234=VERTEX_POINT ( 'NONE', #20471 ) ;
#64238=ADVANCED_FACE ( 'NONE', ( #62910 ), #19417, .F. ) ;
#64242=CARTESIAN_POINT ( 'NONE',  ( 5.393625297349900372, -7.265214908726231435, 455.0000000000000568 ) ) ;
#64244=LINE ( 'NONE', #41613, #53392 ) ;
#64252=AXIS2_PLACEMENT_3D ( 'NONE', #50239, #16697, #11709 ) ;
#64258=LINE ( 'NONE', #58946, #24665 ) ;
#64263=CARTESIAN_POINT ( 'NONE',  ( -11.99351654964671354, 4.173516549646604901, 455.0000000000000568 ) ) ;
#64268=LINE ( 'NONE', #8854, #51160 ) ;
#64278=LINE ( 'NONE', #4185, #10750 ) ;
#64283=EDGE_CURVE ( 'NONE', #8396, #61131, #7054, .T. ) ;
#64284=LINE ( 'NONE', #10528, #53712 ) ;
#64292=ADVANCED_FACE ( 'NONE', ( #31792 ), #9878, .F. ) ;
#64293=VERTEX_POINT ( 'NONE', #3865 ) ;
#64296=CARTESIAN_POINT ( 'NONE',  ( 4.747751991980625696, -6.619341603356940773, 455.0000000000000568 ) ) ;
#64297=DIRECTION ( 'NONE',  ( -1.000000000000000000, 0.000000000000000000, 0.000000000000000000 ) ) ;
#64300=DIRECTION ( 'NONE',  ( 1.836970198721029934E-16, 1.836970198721010706E-16, -1.000000000000000000 ) ) ;
#64301=DIRECTION ( 'NONE',  ( 8.802523127157697409E-15, 1.000000000000000000, 0.000000000000000000 ) ) ;
#64305=ORIENTED_EDGE ( 'NONE', *, *, #43279, .T. ) ;
#64307=AXIS2_PLACEMENT_3D ( 'NONE', #8817, #30385, #39922 ) ;
#64308=DIRECTION ( 'NONE',  ( -1.000000000000000000, 0.000000000000000000, 0.000000000000000000 ) ) ;
#64314=ORIENTED_EDGE ( 'NONE', *, *, #56800, .T. ) ;
#64319=VECTOR ( 'NONE', #4418, 1000.000000000000000 ) ;
#64334=CARTESIAN_POINT ( 'NONE',  ( 3.606483450353406006, 7.415254214038213831, 455.0000000000000568 ) ) ;
#64337=FACE_OUTER_BOUND ( 'NONE', #39244, .T. ) ;
#64339=ORIENTED_EDGE ( 'NONE', *, *, #31643, .F. ) ;
#64347=CYLINDRICAL_SURFACE ( 'NONE', #6992, 0.2000000000000005107 ) ;
#64348=VECTOR ( 'NONE', #23802, 1000.000000000000000 ) ;
#64353=CARTESIAN_POINT ( 'NONE',  ( -9.293516549646710700, 10.08346604330776941, 195.0000000000000284 ) ) ;
#64371=VERTEX_POINT ( 'NONE', #4915 ) ;
#64373=EDGE_CURVE ( 'NONE', #19531, #35354, #60169, .T. ) ;
#64375=AXIS2_PLACEMENT_3D ( 'NONE', #3049, #7279, #34147 ) ;
#64384=DIRECTION ( 'NONE',  ( -1.836970198721029934E-16, 1.836970198721036344E-16, -1.000000000000000000 ) ) ;
#64387=EDGE_CURVE ( 'NONE', #30360, #43706, #64647, .T. ) ;
#64388=FACE_OUTER_BOUND ( 'NONE', #32874, .T. ) ;
#64392=FACE_OUTER_BOUND ( 'NONE', #67273, .T. ) ;
#64394=LINE ( 'NONE', #36827, #32303 ) ;
#64396=LINE ( 'NONE', #64732, #40702 ) ;
#64403=ORIENTED_EDGE ( 'NONE', *, *, #3846, .F. ) ;
#64407=EDGE_CURVE ( 'NONE', #57399, #40401, #54739, .T. ) ;
#64411=AXIS2_PLACEMENT_3D ( 'NONE', #57875, #9443, #31009 ) ;
#64417=CARTESIAN_POINT ( 'NONE',  ( -4.188533722949335569, 7.259684009079808931, 455.0000000000000568 ) ) ;
#64420=CARTESIAN_POINT ( 'NONE',  ( -10.19191654964671301, 11.07551654964660415, 195.0000000000000284 ) ) ;
#64421=AXIS2_PLACEMENT_3D ( 'NONE', #52460, #13568, #35123 ) ;
#64425=EDGE_LOOP ( 'NONE', ( #5924, #1203, #5913, #53679 ) ) ;
#64440=DIRECTION ( 'NONE',  ( 1.836970198721029934E-16, 1.836970198721010706E-16, -1.000000000000000000 ) ) ;
#64443=FACE_OUTER_BOUND ( 'NONE', #32702, .T. ) ;
#64448=ORIENTED_EDGE ( 'NONE', *, *, #66858, .F. ) ;
#64450=ORIENTED_EDGE ( 'NONE', *, *, #16728, .T. ) ;
#64465=DIRECTION ( 'NONE',  ( -0.000000000000000000, -0.000000000000000000, -1.000000000000000000 ) ) ;
#64475=DIRECTION ( 'NONE',  ( 0.7671651518153006499, -0.6414496315691565753, -2.356647714346250026E-16 ) ) ;
#64480=DIRECTION ( 'NONE',  ( -0.000000000000000000, 3.673940397442059868E-16, -1.000000000000000000 ) ) ;
#64481=FACE_OUTER_BOUND ( 'NONE', #13132, .T. ) ;
#64487=CARTESIAN_POINT ( 'NONE',  ( -2.693516549646780334, -10.92648345035340895, 195.0000000000000284 ) ) ;
#64491=LINE ( 'NONE', #43947, #48144 ) ;
#64502=VECTOR ( 'NONE', #29396, 1000.000000000000000 ) ;
#64507=VERTEX_POINT ( 'NONE', #2026 ) ;
#64515=LINE ( 'NONE', #43637, #11401 ) ;
#64516=ORIENTED_EDGE ( 'NONE', *, *, #63702, .F. ) ;
#64521=VECTOR ( 'NONE', #24722, 1000.000000000000000 ) ;
#64526=EDGE_CURVE ( 'NONE', #51301, #4070, #12612, .T. ) ;
#64547=EDGE_LOOP ( 'NONE', ( #340, #15046, #17733, #20334 ) ) ;
#64551=CARTESIAN_POINT ( 'NONE',  ( 6.006483450353379716, -8.211283450353491276, 455.0000000000000568 ) ) ;
#64552=ORIENTED_EDGE ( 'NONE', *, *, #45135, .F. ) ;
#64560=LINE ( 'NONE', #31352, #50361 ) ;
#64568=FACE_OUTER_BOUND ( 'NONE', #58408, .T. ) ;
#64570=CARTESIAN_POINT ( 'NONE',  ( -11.99351654964671354, 7.813516549646603693, 195.0000000000000284 ) ) ;
#64575=PLANE ( 'NONE',  #22655 ) ;
#64595=EDGE_LOOP ( 'NONE', ( #4563, #31809, #68710, #56670 ) ) ;
#64600=AXIS2_PLACEMENT_3D ( 'NONE', #16595, #49108, #4939 ) ;
#64602=ORIENTED_EDGE ( 'NONE', *, *, #25580, .T. ) ;
#64607=VECTOR ( 'NONE', #44150, 1000.000000000000000 ) ;
#64613=ORIENTED_EDGE ( 'NONE', *, *, #909, .T. ) ;
#64616=LINE ( 'NONE', #38105, #66573 ) ;
#64621=LINE ( 'NONE', #10879, #63853 ) ;
#64623=CARTESIAN_POINT ( 'NONE',  ( -9.293516549646827940, -10.92648345035338764, 455.0000000000000568 ) ) ;
#64626=FACE_OUTER_BOUND ( 'NONE', #61553, .T. ) ;
#64632=LINE ( 'NONE', #10891, #34499 ) ;
#64638=VERTEX_POINT ( 'NONE', #47607 ) ;
#64639=ORIENTED_EDGE ( 'NONE', *, *, #66010, .T. ) ;
#64641=FACE_OUTER_BOUND ( 'NONE', #45570, .T. ) ;
#64647=LINE ( 'NONE', #1004, #47755 ) ;
#64651=LINE ( 'NONE', #37789, #7413 ) ;
#64652=PLANE ( 'NONE',  #28841 ) ;
#64654=VECTOR ( 'NONE', #52884, 999.9999999999998863 ) ;
#64655=LINE ( 'NONE', #37794, #22476 ) ;
#64656=DIRECTION ( 'NONE',  ( -0.000000000000000000, -0.000000000000000000, -1.000000000000000000 ) ) ;
#64661=ORIENTED_EDGE ( 'NONE', *, *, #58052, .F. ) ;
#64666=DIRECTION ( 'NONE',  ( 1.000000000000000000, 0.000000000000000000, 0.000000000000000000 ) ) ;
#64668=EDGE_CURVE ( 'NONE', #10176, #5167, #41952, .T. ) ;
#64680=DIRECTION ( 'NONE',  ( -0.000000000000000000, -0.000000000000000000, -1.000000000000000000 ) ) ;
#64681=DIRECTION ( 'NONE',  ( 0.000000000000000000, 0.000000000000000000, 1.000000000000000000 ) ) ;
#64684=AXIS2_PLACEMENT_3D ( 'NONE', #6564, #1581, #60972 ) ;
#64687=ORIENTED_EDGE ( 'NONE', *, *, #16397, .F. ) ;
#64701=DIRECTION ( 'NONE',  ( 1.000000000000000000, 0.000000000000000000, 0.000000000000000000 ) ) ;
#64708=ADVANCED_FACE ( 'NONE', ( #36296 ), #31370, .F. ) ;
#64711=VERTEX_POINT ( 'NONE', #19668 ) ;
#64712=ORIENTED_EDGE ( 'NONE', *, *, #36878, .F. ) ;
#64715=DIRECTION ( 'NONE',  ( -1.000000000000000000, 3.491481338843132961E-15, 1.836970198721036344E-16 ) ) ;
#64725=FACE_OUTER_BOUND ( 'NONE', #48394, .T. ) ;
#64732=CARTESIAN_POINT ( 'NONE',  ( -9.293516549646710700, 10.08346604330776941, 455.0000000000000568 ) ) ;
#64739=CARTESIAN_POINT ( 'NONE',  ( 6.006483450353379716, -3.606483450353394904, 195.0000000000000284 ) ) ;
#64745=DIRECTION ( 'NONE',  ( -1.062171939662868249E-14, -1.000000000000000000, 0.000000000000000000 ) ) ;
#64747=DIRECTION ( 'NONE',  ( -0.000000000000000000, -0.000000000000000000, -1.000000000000000000 ) ) ;
#64749=CARTESIAN_POINT ( 'NONE',  ( -8.333516549646715177, 11.11351654964659730, 455.0000000000000568 ) ) ;
#64751=LINE ( 'NONE', #21961, #6063 ) ;
#64753=VERTEX_POINT ( 'NONE', #14023 ) ;
#64759=ORIENTED_EDGE ( 'NONE', *, *, #16421, .F. ) ;
#64769=AXIS2_PLACEMENT_3D ( 'NONE', #23388, #66519, #32625 ) ;
#64773=FACE_OUTER_BOUND ( 'NONE', #57502, .T. ) ;
#64783=CARTESIAN_POINT ( 'NONE',  ( 7.826483450353380000, -12.00648345035339659, 195.0000000000000284 ) ) ;
#64784=CARTESIAN_POINT ( 'NONE',  ( 10.92648345035331303, 2.693516549646575609, 195.0000000000000284 ) ) ;
#64789=DIRECTION ( 'NONE',  ( 0.000000000000000000, -1.000000000000000000, 0.000000000000000000 ) ) ;
#64790=CARTESIAN_POINT ( 'NONE',  ( 7.852485183456931139, -3.430747519065418860, 455.0000000000000568 ) ) ;
#64793=VERTEX_POINT ( 'NONE', #32047 ) ;
#64797=CARTESIAN_POINT ( 'NONE',  ( 7.826483450353421745, 11.77351654964657257, 455.0000000000000568 ) ) ;
#64808=LINE ( 'NONE', #54548, #1562 ) ;
#64819=CARTESIAN_POINT ( 'NONE',  ( 7.272650909786598561, -7.811466277050764795, 195.0000000000000284 ) ) ;
#64824=DIRECTION ( 'NONE',  ( -1.836970198721029934E-16, -1.836970198721010706E-16, 1.000000000000000000 ) ) ;
#64828=CYLINDRICAL_SURFACE ( 'NONE', #17653, 0.5999999999999998668 ) ;
#64832=VECTOR ( 'NONE', #28909, 1000.000000000000114 ) ;
#64836=ORIENTED_EDGE ( 'NONE', *, *, #43279, .F. ) ;
#64838=CARTESIAN_POINT ( 'NONE',  ( 9.417013320880768035, 1.853252480934615809, 455.0000000000000568 ) ) ;
#64852=ORIENTED_EDGE ( 'NONE', *, *, #63518, .F. ) ;
#64859=DIRECTION ( 'NONE',  ( -1.000000000000000000, -1.671920889371702854E-15, -0.000000000000000000 ) ) ;
#64862=DIRECTION ( 'NONE',  ( 3.717264591378875951E-15, 1.000000000000000000, 0.000000000000000000 ) ) ;
#64864=CARTESIAN_POINT ( 'NONE',  ( -7.259684009079930611, 7.798499376343971612, 195.0000000000000284 ) ) ;
#64865=ORIENTED_EDGE ( 'NONE', *, *, #51136, .F. ) ;
#64873=VECTOR ( 'NONE', #61172, 1000.000000000000114 ) ;
#64876=ORIENTED_EDGE ( 'NONE', *, *, #19970, .F. ) ;
#64892=VERTEX_POINT ( 'NONE', #34105 ) ;
#64897=DIRECTION ( 'NONE',  ( 0.000000000000000000, -1.000000000000000000, 0.000000000000000000 ) ) ;
#64900=DIRECTION ( 'NONE',  ( -1.000000000000000000, -1.570596175624152290E-15, 0.000000000000000000 ) ) ;
#64901=CARTESIAN_POINT ( 'NONE',  ( 6.619341603356875936, 7.252248008019321901, 455.0000000000000568 ) ) ;
#64906=EDGE_LOOP ( 'NONE', ( #9303, #17365, #64053, #49977 ) ) ;
#64912=ORIENTED_EDGE ( 'NONE', *, *, #36058, .T. ) ;
#64922=EDGE_CURVE ( 'NONE', #57392, #41573, #12195, .T. ) ;
#64923=CARTESIAN_POINT ( 'NONE',  ( 4.396432944014527777, -8.406483450353382736, 195.0000000000000284 ) ) ;
#64927=CARTESIAN_POINT ( 'NONE',  ( -11.18071654964682615, -12.00648345035337350, 455.0000000000000568 ) ) ;
#64929=ORIENTED_EDGE ( 'NONE', *, *, #1835, .T. ) ;
#64933=DIRECTION ( 'NONE',  ( 0.000000000000000000, 3.673940397442059868E-16, -1.000000000000000000 ) ) ;
#64936=CARTESIAN_POINT ( 'NONE',  ( 7.811466277050736373, -4.740315990920255906, 455.0000000000000568 ) ) ;
#64952=CARTESIAN_POINT ( 'NONE',  ( 9.306483450353379538, -10.92648345035348534, 455.0000000000000568 ) ) ;
#64955=DIRECTION ( 'NONE',  ( 0.7071067811865446862, -0.7071067811865503483, 0.000000000000000000 ) ) ;
#64962=CIRCLE ( 'NONE', #34433, 0.1999999999999992339 ) ;
#64970=CIRCLE ( 'NONE', #55380, 0.8128000000000145109 ) ;
#64977=CARTESIAN_POINT ( 'NONE',  ( -8.593516549646793123, -7.616533956692233431, 455.0000000000000568 ) ) ;
#64988=DIRECTION ( 'NONE',  ( -1.836970198721029934E-16, -1.836970198721010706E-16, 1.000000000000000000 ) ) ;
#64993=DIRECTION ( 'NONE',  ( -1.000000000000000000, 2.309061475090597584E-14, 0.000000000000000000 ) ) ;
#64997=VERTEX_POINT ( 'NONE', #37940 ) ;
#65008=EDGE_CURVE ( 'NONE', #10322, #9609, #38288, .T. ) ;
#65009=FACE_OUTER_BOUND ( 'NONE', #18353, .T. ) ;
#65010=LINE ( 'NONE', #36387, #35605 ) ;
#65021=CARTESIAN_POINT ( 'NONE',  ( 11.48848345035334617, -10.20488345035352928, 455.0000000000000568 ) ) ;
#65027=DIRECTION ( 'NONE',  ( 1.836970198721029934E-16, 1.836970198721010706E-16, -1.000000000000000000 ) ) ;
#65028=DIRECTION ( 'NONE',  ( 1.000000000000000000, -1.610765207321970913E-14, 0.000000000000000000 ) ) ;
#65029=DIRECTION ( 'NONE',  ( -1.836970198721029934E-16, 1.836970198721036344E-16, -1.000000000000000000 ) ) ;
#65037=ORIENTED_EDGE ( 'NONE', *, *, #66103, .F. ) ;
#65042=VERTEX_POINT ( 'NONE', #26629 ) ;
#65043=VERTEX_POINT ( 'NONE', #53508 ) ;
#65054=CARTESIAN_POINT ( 'NONE',  ( 10.20488345035345290, 9.791916549646566992, 455.0000000000000568 ) ) ;
#65055=EDGE_CURVE ( 'NONE', #54865, #33821, #64808, .T. ) ;
#65058=ORIENTED_EDGE ( 'NONE', *, *, #44602, .T. ) ;
#65078=CARTESIAN_POINT ( 'NONE',  ( 11.78648345035340839, 7.813516549646560172, 455.0000000000000568 ) ) ;
#65081=VERTEX_POINT ( 'NONE', #44257 ) ;
#65085=CYLINDRICAL_SURFACE ( 'NONE', #4741, 0.2000000000000005107 ) ;
#65086=ORIENTED_EDGE ( 'NONE', *, *, #45587, .F. ) ;
#65087=CARTESIAN_POINT ( 'NONE',  ( -11.77351654964674132, -4.186483450353323477, 455.0000000000000568 ) ) ;
#65094=CARTESIAN_POINT ( 'NONE',  ( 7.272650909786554152, 4.188533722949247640, 195.0000000000000284 ) ) ;
#65096=LINE ( 'NONE', #11331, #20283 ) ;
#65097=EDGE_CURVE ( 'NONE', #12559, #40641, #69315, .T. ) ;
#65103=EDGE_CURVE ( 'NONE', #3828, #20214, #54205, .T. ) ;
#65125=ORIENTED_EDGE ( 'NONE', *, *, #16892, .T. ) ;
#65127=DIRECTION ( 'NONE',  ( -0.000000000000000000, -0.000000000000000000, -1.000000000000000000 ) ) ;
#65133=CARTESIAN_POINT ( 'NONE',  ( 4.201500623656003519, -7.272650909786698037, 455.0000000000000568 ) ) ;
#65141=CARTESIAN_POINT ( 'NONE',  ( -8.593516549646711411, 7.603567055985436696, 195.0000000000000284 ) ) ;
#65144=DIRECTION ( 'NONE',  ( 0.7071067811865527908, 0.7071067811865422437, 2.597868168706460875E-16 ) ) ;
#65155=ORIENTED_EDGE ( 'NONE', *, *, #13835, .F. ) ;
#65160=ADVANCED_FACE ( 'NONE', ( #54898 ), #11729, .F. ) ;
#65167=AXIS2_PLACEMENT_3D ( 'NONE', #60446, #60792, #13039 ) ;
#65176=ADVANCED_FACE ( 'NONE', ( #66180 ), #35032, .F. ) ;
#65181=AXIS2_PLACEMENT_3D ( 'NONE', #20552, #30462, #9252 ) ;
#65182=CARTESIAN_POINT ( 'NONE',  ( 1.866219381641426533, -9.417013320880776917, 195.0000000000000284 ) ) ;
#65184=CARTESIAN_POINT ( 'NONE',  ( 7.811466277050736373, -7.272650909786632312, 195.0000000000000284 ) ) ;
#65185=EDGE_CURVE ( 'NONE', #58876, #17214, #55231, .T. ) ;
#65192=AXIS2_PLACEMENT_3D ( 'NONE', #40633, #61134, #50885 ) ;
#65194=DIRECTION ( 'NONE',  ( -0.000000000000000000, 3.673940397442059868E-16, -1.000000000000000000 ) ) ;
#65203=ORIENTED_EDGE ( 'NONE', *, *, #46229, .T. ) ;
#65204=CARTESIAN_POINT ( 'NONE',  ( -5.993516549646728642, -6.006483450353378828, 195.0000000000000284 ) ) ;
#65213=LINE ( 'NONE', #43969, #16498 ) ;
#65218=DIRECTION ( 'NONE',  ( 0.000000000000000000, 1.000000000000000000, 0.000000000000000000 ) ) ;
#65221=ORIENTED_EDGE ( 'NONE', *, *, #18031, .F. ) ;
#65225=DIRECTION ( 'NONE',  ( -1.836970198721029934E-16, 1.836970198721036344E-16, -1.000000000000000000 ) ) ;
#65226=DIRECTION ( 'NONE',  ( -3.491481338843132961E-15, -1.000000000000000000, -1.836970198721029934E-16 ) ) ;
#65230=LINE ( 'NONE', #16778, #39009 ) ;
#65236=DIRECTION ( 'NONE',  ( -1.836970198721029934E-16, 1.836970198721036344E-16, -1.000000000000000000 ) ) ;
#65239=CARTESIAN_POINT ( 'NONE',  ( 9.955011587777175208, 2.752095193409277218, 195.0000000000000284 ) ) ;
#65243=ORIENTED_EDGE ( 'NONE', *, *, #38103, .F. ) ;
#65249=ORIENTED_EDGE ( 'NONE', *, *, #20020, .F. ) ;
#65254=LINE ( 'NONE', #11477, #11883 ) ;
#65266=VERTEX_POINT ( 'NONE', #57663 ) ;
#65272=CARTESIAN_POINT ( 'NONE',  ( 2.290483450353350658, -9.841277389592804070, 455.0000000000000568 ) ) ;
#65281=DIRECTION ( 'NONE',  ( 8.359604446858499085E-15, 1.000000000000000000, 0.000000000000000000 ) ) ;
#65289=LINE ( 'NONE', #66312, #33062 ) ;
#65290=DIRECTION ( 'NONE',  ( 0.7071067811865446862, -0.7071067811865503483, 0.000000000000000000 ) ) ;
#65297=DIRECTION ( 'NONE',  ( -1.000000000000000000, 0.000000000000000000, 0.000000000000000000 ) ) ;
#65302=CARTESIAN_POINT ( 'NONE',  ( -11.47551654964682122, -10.20488345035336941, 455.0000000000000568 ) ) ;
#65303=CARTESIAN_POINT ( 'NONE',  ( -9.942044687070568543, 9.234937905883914055, 455.0000000000000568 ) ) ;
#65312=ORIENTED_EDGE ( 'NONE', *, *, #32892, .F. ) ;
#65314=AXIS2_PLACEMENT_3D ( 'NONE', #12296, #67096, #39188 ) ;
#65323=CARTESIAN_POINT ( 'NONE',  ( 1.690483450353418959, 10.73351654964659652, 455.0000000000000568 ) ) ;
#65326=ORIENTED_EDGE ( 'NONE', *, *, #52374, .F. ) ;
#65343=CARTESIAN_POINT ( 'NONE',  ( -10.73351654964669599, -1.690483450353341910, 455.0000000000000568 ) ) ;
#65344=FACE_OUTER_BOUND ( 'NONE', #26352, .T. ) ;
#65348=CARTESIAN_POINT ( 'NONE',  ( 7.806483450353372433, 11.11351654964662039, 195.0000000000000284 ) ) ;
#65358=VECTOR ( 'NONE', #49968, 1000.000000000000000 ) ;
#65364=FACE_OUTER_BOUND ( 'NONE', #66994, .T. ) ;
#65375=CARTESIAN_POINT ( 'NONE',  ( -11.77351654964674310, -4.406483450353321452, 455.0000000000000568 ) ) ;
#65389=CARTESIAN_POINT ( 'NONE',  ( 8.465062094116069247, -4.255011587777349114, 455.0000000000000568 ) ) ;
#65390=ORIENTED_EDGE ( 'NONE', *, *, #44937, .T. ) ;
#65393=DIRECTION ( 'NONE',  ( 8.673617379884013384E-15, 1.000000000000000000, 0.000000000000000000 ) ) ;
#65398=CARTESIAN_POINT ( 'NONE',  ( 7.616533956692244978, 8.593516549646574632, 455.0000000000000568 ) ) ;
#65403=VERTEX_POINT ( 'NONE', #42098 ) ;
#65408=EDGE_CURVE ( 'NONE', #54829, #29989, #25142, .T. ) ;
#65414=ORIENTED_EDGE ( 'NONE', *, *, #49773, .T. ) ;
#65415=VECTOR ( 'NONE', #68301, 1000.000000000000000 ) ;
#65416=DIRECTION ( 'NONE',  ( -0.7671651518153006499, -0.6414496315691565753, -2.356647714346250026E-16 ) ) ;
#65419=DIRECTION ( 'NONE',  ( 1.836970198721029934E-16, -1.836970198721036344E-16, 1.000000000000000000 ) ) ;
#65420=CARTESIAN_POINT ( 'NONE',  ( 8.606483450353360709, 7.603567055985452683, 195.0000000000000284 ) ) ;
#65422=VERTEX_POINT ( 'NONE', #50999 ) ;
#65430=FACE_OUTER_BOUND ( 'NONE', #60138, .T. ) ;
#65440=ORIENTED_EDGE ( 'NONE', *, *, #48662, .T. ) ;
#65442=EDGE_LOOP ( 'NONE', ( #57453, #57932, #60735, #37935 ) ) ;
#65443=FACE_OUTER_BOUND ( 'NONE', #17413, .T. ) ;
#65452=CARTESIAN_POINT ( 'NONE',  ( -1.853252480934834967, -9.417013320880835536, 195.0000000000000284 ) ) ;
#65462=ORIENTED_EDGE ( 'NONE', *, *, #9945, .F. ) ;
#65469=ORIENTED_EDGE ( 'NONE', *, *, #57008, .T. ) ;
#65470=ORIENTED_EDGE ( 'NONE', *, *, #32241, .F. ) ;
#65474=AXIS2_PLACEMENT_3D ( 'NONE', #65204, #5101, #27706 ) ;
#65475=DIRECTION ( 'NONE',  ( 1.836970198721029934E-16, 1.836970198721010706E-16, -1.000000000000000000 ) ) ;
#65493=VECTOR ( 'NONE', #58188, 1000.000000000000000 ) ;
#65500=ORIENTED_EDGE ( 'NONE', *, *, #17982, .F. ) ;
#65502=PLANE ( 'NONE',  #54272 ) ;
#65507=ORIENTED_EDGE ( 'NONE', *, *, #38237, .F. ) ;
#65510=CARTESIAN_POINT ( 'NONE',  ( -8.333516549646715177, 11.11351654964659907, 195.0000000000000284 ) ) ;
#65511=CARTESIAN_POINT ( 'NONE',  ( 10.92648345035337520, -9.106483450353492159, 455.0000000000000568 ) ) ;
#65512=ORIENTED_EDGE ( 'NONE', *, *, #42189, .F. ) ;
#65516=DIRECTION ( 'NONE',  ( 1.000000000000000000, 0.000000000000000000, 0.000000000000000000 ) ) ;
#65529=CIRCLE ( 'NONE', #2275, 1.399999999999998579 ) ;
#65540=DIRECTION ( 'NONE',  ( 1.000000000000000000, 0.000000000000000000, 0.000000000000000000 ) ) ;
#65542=EDGE_CURVE ( 'NONE', #38948, #41197, #29776, .T. ) ;
#65552=ORIENTED_EDGE ( 'NONE', *, *, #14109, .T. ) ;
#65561=ORIENTED_EDGE ( 'NONE', *, *, #54951, .T. ) ;
#65566=DIRECTION ( 'NONE',  ( 0.8660254037844510311, 0.4999999999999785727, 1.836970198720951294E-16 ) ) ;
#65571=ORIENTED_EDGE ( 'NONE', *, *, #22843, .T. ) ;
#65574=ORIENTED_EDGE ( 'NONE', *, *, #2759, .F. ) ;
#65575=VECTOR ( 'NONE', #9254, 1000.000000000000000 ) ;
#65583=EDGE_CURVE ( 'NONE', #50762, #67938, #15281, .T. ) ;
#65592=LINE ( 'NONE', #21765, #45818 ) ;
#65600=ADVANCED_FACE ( 'NONE', ( #52412 ), #41085, .F. ) ;
#65605=FACE_OUTER_BOUND ( 'NONE', #8190, .T. ) ;
#65611=ADVANCED_FACE ( 'NONE', ( #58430 ), #20574, .F. ) ;
#65619=DIRECTION ( 'NONE',  ( -1.836970198721029934E-16, -1.836970198721010706E-16, 1.000000000000000000 ) ) ;
#65624=CARTESIAN_POINT ( 'NONE',  ( 2.706483450353371900, 10.91351654964663354, 195.0000000000000284 ) ) ;
#65626=LINE ( 'NONE', #38750, #18149 ) ;
#65628=ORIENTED_EDGE ( 'NONE', *, *, #39600, .T. ) ;
#65638=EDGE_CURVE ( 'NONE', #11892, #13193, #37204, .T. ) ;
#65648=LINE ( 'NONE', #16866, #20328 ) ;
#65650=VECTOR ( 'NONE', #42895, 1000.000000000000114 ) ;
#65655=EDGE_CURVE ( 'NONE', #35824, #51349, #12631, .T. ) ;
#65656=DIRECTION ( 'NONE',  ( -4.268512490100335178E-15, -1.000000000000000000, 0.000000000000000000 ) ) ;
#65680=ORIENTED_EDGE ( 'NONE', *, *, #58977, .F. ) ;
#65689=CARTESIAN_POINT ( 'NONE',  ( -11.33351654964671162, 1.077516549646603483, 455.0000000000000568 ) ) ;
#65693=EDGE_CURVE ( 'NONE', #67098, #63196, #66039, .T. ) ;
#65700=CARTESIAN_POINT ( 'NONE',  ( -11.07551654964667520, 9.791916549646639822, 195.0000000000000284 ) ) ;
#65705=ORIENTED_EDGE ( 'NONE', *, *, #62944, .F. ) ;
#65707=VECTOR ( 'NONE', #10083, 1000.000000000000000 ) ;
#65708=CIRCLE ( 'NONE', #64600, 0.5999999999999989786 ) ;
#65709=LINE ( 'NONE', #60384, #45753 ) ;
#65710=CARTESIAN_POINT ( 'NONE',  ( -11.77351654964670935, 7.813516549646603693, 455.0000000000000568 ) ) ;
#65714=AXIS2_PLACEMENT_3D ( 'NONE', #50591, #66495, #50926 ) ;
#65716=ORIENTED_EDGE ( 'NONE', *, *, #5070, .F. ) ;
#65720=VECTOR ( 'NONE', #14834, 1000.000000000000114 ) ;
#65721=EDGE_CURVE ( 'NONE', #59671, #6649, #17262, .T. ) ;
#65722=LINE ( 'NONE', #15902, #1644 ) ;
#65724=ORIENTED_EDGE ( 'NONE', *, *, #34275, .T. ) ;
#65726=EDGE_LOOP ( 'NONE', ( #62145, #32772, #21186, #44771 ) ) ;
#65738=ORIENTED_EDGE ( 'NONE', *, *, #65721, .F. ) ;
#65745=EDGE_CURVE ( 'NONE', #60571, #52360, #39513, .T. ) ;
#65746=CARTESIAN_POINT ( 'NONE',  ( -5.655420232009311654, -8.406483450353382736, 195.0000000000000284 ) ) ;
#65747=ORIENTED_EDGE ( 'NONE', *, *, #66858, .T. ) ;
#65753=VERTEX_POINT ( 'NONE', #16927 ) ;
#65764=AXIS2_PLACEMENT_3D ( 'NONE', #62113, #62829, #25352 ) ;
#65773=DIRECTION ( 'NONE',  ( 0.7071067811865474617, 0.7071067811865474617, 0.000000000000000000 ) ) ;
#65774=VERTEX_POINT ( 'NONE', #672 ) ;
#65775=EDGE_CURVE ( 'NONE', #11613, #144, #22241, .T. ) ;
#65790=DIRECTION ( 'NONE',  ( -1.836970198721029934E-16, 1.836970198721036344E-16, -1.000000000000000000 ) ) ;
#65800=ORIENTED_EDGE ( 'NONE', *, *, #8381, .F. ) ;
#65801=PLANE ( 'NONE',  #34749 ) ;
#65802=CARTESIAN_POINT ( 'NONE',  ( -4.609516549646713202, 3.593516549646603941, 455.0000000000000568 ) ) ;
#65818=ORIENTED_EDGE ( 'NONE', *, *, #40759, .T. ) ;
#65820=VERTEX_POINT ( 'NONE', #3791 ) ;
#65824=VECTOR ( 'NONE', #53702, 1000.000000000000000 ) ;
#65830=ORIENTED_EDGE ( 'NONE', *, *, #55938, .T. ) ;
#65837=EDGE_CURVE ( 'NONE', #33774, #8876, #57531, .T. ) ;
#65838=VERTEX_POINT ( 'NONE', #62124 ) ;
#65841=VECTOR ( 'NONE', #34322, 1000.000000000000000 ) ;
#65845=LINE ( 'NONE', #27678, #41927 ) ;
#65849=CARTESIAN_POINT ( 'NONE',  ( -11.99351654964674729, -7.826483450353316051, 195.0000000000000284 ) ) ;
#65858=VECTOR ( 'NONE', #48520, 1000.000000000000000 ) ;
#65866=EDGE_LOOP ( 'NONE', ( #56415, #24767, #38665, #60786 ) ) ;
#65874=ORIENTED_EDGE ( 'NONE', *, *, #32693, .F. ) ;
#65879=CARTESIAN_POINT ( 'NONE',  ( 9.804883450353408136, 10.19191654964661531, 195.0000000000000284 ) ) ;
#65883=ORIENTED_EDGE ( 'NONE', *, *, #65775, .F. ) ;
#65891=DIRECTION ( 'NONE',  ( -0.6414496315691619044, 0.7671651518152962090, 0.000000000000000000 ) ) ;
#65897=CARTESIAN_POINT ( 'NONE',  ( -2.893516549646681035, 10.08346604330774632, 195.0000000000000284 ) ) ;
#65934=LINE ( 'NONE', #50721, #20098 ) ;
#65947=DIRECTION ( 'NONE',  ( -0.000000000000000000, -0.000000000000000000, -1.000000000000000000 ) ) ;
#65949=DIRECTION ( 'NONE',  ( 0.000000000000000000, 0.000000000000000000, 1.000000000000000000 ) ) ;
#65952=VECTOR ( 'NONE', #44283, 1000.000000000000000 ) ;
#65962=DIRECTION ( 'NONE',  ( -1.836970198721029934E-16, 1.836970198721036344E-16, -1.000000000000000000 ) ) ;
#65966=DIRECTION ( 'NONE',  ( -8.903847840905249551E-15, -1.000000000000000000, -1.836970198721027222E-16 ) ) ;
#65977=LINE ( 'NONE', #55729, #6736 ) ;
#65983=CARTESIAN_POINT ( 'NONE',  ( -11.77351654964670935, 4.393516549646602876, 195.0000000000000284 ) ) ;
#65986=ORIENTED_EDGE ( 'NONE', *, *, #68110, .F. ) ;
#65988=ORIENTED_EDGE ( 'NONE', *, *, #38116, .F. ) ;
#65994=CIRCLE ( 'NONE', #35502, 0.1999999999999996503 ) ;
#65995=LINE ( 'NONE', #6617, #18173 ) ;
#65998=ORIENTED_EDGE ( 'NONE', *, *, #26974, .T. ) ;
#66010=EDGE_CURVE ( 'NONE', #14045, #44953, #60209, .T. ) ;
#66012=EDGE_LOOP ( 'NONE', ( #45878, #26829, #199, #12756 ) ) ;
#66023=CARTESIAN_POINT ( 'NONE',  ( 10.92648345035335922, 2.693516549646528091, 455.0000000000000568 ) ) ;
#66032=CYLINDRICAL_SURFACE ( 'NONE', #2697, 0.1999999999999987899 ) ;
#66033=FACE_OUTER_BOUND ( 'NONE', #51318, .T. ) ;
#66034=AXIS2_PLACEMENT_3D ( 'NONE', #8658, #51798, #30929 ) ;
#66039=LINE ( 'NONE', #17609, #38759 ) ;
#66042=EDGE_CURVE ( 'NONE', #66404, #12559, #59968, .T. ) ;
#66046=AXIS2_PLACEMENT_3D ( 'NONE', #47046, #13108, #8858 ) ;
#66053=VECTOR ( 'NONE', #57613, 1000.000000000000000 ) ;
#66057=CARTESIAN_POINT ( 'NONE',  ( -7.252248008019455128, 5.380658396643134722, 455.0000000000000568 ) ) ;
#66061=DIRECTION ( 'NONE',  ( 1.000000000000000000, -1.952517519553884087E-14, 1.836970198720994435E-16 ) ) ;
#66064=DIRECTION ( 'NONE',  ( -0.000000000000000000, 1.000000000000000000, 3.673940397442059868E-16 ) ) ;
#66094=VECTOR ( 'NONE', #32492, 1000.000000000000000 ) ;
#66097=DIRECTION ( 'NONE',  ( -0.7071067811865398012, 0.7071067811865552333, 2.597868168706484541E-16 ) ) ;
#66098=EDGE_CURVE ( 'NONE', #64032, #64371, #41027, .T. ) ;
#66103=EDGE_CURVE ( 'NONE', #35248, #35896, #28141, .T. ) ;
#66118=ADVANCED_FACE ( 'NONE', ( #38082 ), #61339, .F. ) ;
#66127=DIRECTION ( 'NONE',  ( -0.8660254037844528074, -0.4999999999999755751, 6.723777587269133212E-17 ) ) ;
#66139=DIRECTION ( 'NONE',  ( 1.000000000000000000, 0.000000000000000000, 0.000000000000000000 ) ) ;
#66140=ORIENTED_EDGE ( 'NONE', *, *, #59125, .T. ) ;
#66144=DIRECTION ( 'NONE',  ( 1.836970198721029934E-16, 1.836970198721010706E-16, -1.000000000000000000 ) ) ;
#66162=VECTOR ( 'NONE', #19460, 1000.000000000000000 ) ;
#66165=ORIENTED_EDGE ( 'NONE', *, *, #33770, .F. ) ;
#66175=CARTESIAN_POINT ( 'NONE',  ( 3.006483450353359732, 7.415254214038262681, 195.0000000000000284 ) ) ;
#66178=AXIS2_PLACEMENT_3D ( 'NONE', #10913, #48397, #63977 ) ;
#66180=FACE_OUTER_BOUND ( 'NONE', #58747, .T. ) ;
#66185=ORIENTED_EDGE ( 'NONE', *, *, #48728, .T. ) ;
#66187=ADVANCED_FACE ( 'NONE', ( #51094 ), #68062, .F. ) ;
#66194=EDGE_LOOP ( 'NONE', ( #12002, #66165, #4401, #50429 ) ) ;
#66199=PLANE ( 'NONE',  #61076 ) ;
#66206=FACE_OUTER_BOUND ( 'NONE', #59471, .T. ) ;
#66229=ORIENTED_EDGE ( 'NONE', *, *, #22610, .F. ) ;
#66237=DIRECTION ( 'NONE',  ( -1.000000000000000000, 0.000000000000000000, 0.000000000000000000 ) ) ;
#66256=DIRECTION ( 'NONE',  ( 1.000000000000000000, 0.000000000000000000, 0.000000000000000000 ) ) ;
#66257=CARTESIAN_POINT ( 'NONE',  ( -7.813516549646839948, -12.00648345035340903, 455.0000000000000568 ) ) ;
#66271=EDGE_CURVE ( 'NONE', #6262, #45635, #58155, .T. ) ;
#66286=ORIENTED_EDGE ( 'NONE', *, *, #47764, .T. ) ;
#66288=DIRECTION ( 'NONE',  ( 1.000000000000000000, 5.013651664672856055E-16, 0.000000000000000000 ) ) ;
#66289=CARTESIAN_POINT ( 'NONE',  ( -4.393516549646667713, 11.77351654964658856, 455.0000000000000568 ) ) ;
#66299=DIRECTION ( 'NONE',  ( -1.000000000000000000, 0.000000000000000000, 0.000000000000000000 ) ) ;
#66304=CARTESIAN_POINT ( 'NONE',  ( -11.11351654964671098, 7.793516549646603231, 455.0000000000000568 ) ) ;
#66309=ORIENTED_EDGE ( 'NONE', *, *, #23998, .F. ) ;
#66312=CARTESIAN_POINT ( 'NONE',  ( -11.11351654964670921, 8.333516549646663663, 455.0000000000000568 ) ) ;
#66314=EDGE_CURVE ( 'NONE', #66510, #38207, #47207, .T. ) ;
#66321=DIRECTION ( 'NONE',  ( -9.050731179009442381E-15, -1.000000000000000000, 0.000000000000000000 ) ) ;
#66323=CARTESIAN_POINT ( 'NONE',  ( -5.993516549646728642, -6.006483450353378828, 195.0000000000000284 ) ) ;
#66329=AXIS2_PLACEMENT_3D ( 'NONE', #55091, #39159, #16208 ) ;
#66330=FACE_OUTER_BOUND ( 'NONE', #59230, .T. ) ;
#66331=FACE_OUTER_BOUND ( 'NONE', #69765, .T. ) ;
#66342=ORIENTED_EDGE ( 'NONE', *, *, #56800, .F. ) ;
#66347=VERTEX_POINT ( 'NONE', #16072 ) ;
#66353=CARTESIAN_POINT ( 'NONE',  ( 7.606483450353424658, 11.77351654964657435, 455.0000000000000568 ) ) ;
#66356=VECTOR ( 'NONE', #53473, 1000.000000000000000 ) ;
#66357=AXIS2_PLACEMENT_3D ( 'NONE', #13127, #2875, #49923 ) ;
#66358=CARTESIAN_POINT ( 'NONE',  ( -8.393516549646768965, -5.668387132715940524, 455.0000000000000568 ) ) ;
#66359=CARTESIAN_POINT ( 'NONE',  ( 2.706483450353350584, -10.09643294401463365, 455.0000000000000568 ) ) ;
#66360=ADVANCED_FACE ( 'NONE', ( #39014 ), #6149, .T. ) ;
#66368=FACE_OUTER_BOUND ( 'NONE', #46885, .T. ) ;
#66381=DIRECTION ( 'NONE',  ( 1.000000000000000000, 0.000000000000000000, 0.000000000000000000 ) ) ;
#66395=EDGE_LOOP ( 'NONE', ( #47008, #30104, #26967, #31120 ) ) ;
#66402=VECTOR ( 'NONE', #45170, 1000.000000000000000 ) ;
#66404=VERTEX_POINT ( 'NONE', #11783 ) ;
#66418=ORIENTED_EDGE ( 'NONE', *, *, #50774, .T. ) ;
#66420=VECTOR ( 'NONE', #32659, 1000.000000000000114 ) ;
#66424=VERTEX_POINT ( 'NONE', #504 ) ;
#66437=FACE_OUTER_BOUND ( 'NONE', #13593, .T. ) ;
#66441=DIRECTION ( 'NONE',  ( -1.000000000000000000, 0.000000000000000000, 0.000000000000000000 ) ) ;
#66442=DIRECTION ( 'NONE',  ( -1.214636490590110115E-14, -1.000000000000000000, 0.000000000000000000 ) ) ;
#66450=AXIS2_PLACEMENT_3D ( 'NONE', #46757, #13536, #14249 ) ;
#66452=CARTESIAN_POINT ( 'NONE',  ( 7.606483450353424658, 11.77351654964657435, 455.0000000000000568 ) ) ;
#66455=LINE ( 'NONE', #18006, #3017 ) ;
#66464=CARTESIAN_POINT ( 'NONE',  ( -10.19191654964685156, -9.804883450353383267, 455.0000000000000568 ) ) ;
#66467=CIRCLE ( 'NONE', #17468, 0.1999999999999987899 ) ;
#66468=CARTESIAN_POINT ( 'NONE',  ( 11.78648345035340661, 7.593516549646560421, 455.0000000000000568 ) ) ;
#66470=CARTESIAN_POINT ( 'NONE',  ( 11.19368345035336532, -11.19368345035347723, 455.0000000000000568 ) ) ;
#66471=CARTESIAN_POINT ( 'NONE',  ( 10.20488345035340494, 10.19191654964661531, 195.0000000000000284 ) ) ;
#66474=DIRECTION ( 'NONE',  ( 1.000000000000000000, 0.000000000000000000, 0.000000000000000000 ) ) ;
#66495=DIRECTION ( 'NONE',  ( -1.836970198721029934E-16, 1.836970198721036344E-16, -1.000000000000000000 ) ) ;
#66497=CARTESIAN_POINT ( 'NONE',  ( 12.00648345035337883, -11.19368345035347900, 455.0000000000000568 ) ) ;
#66504=DIRECTION ( 'NONE',  ( 1.819560449471430698E-15, 1.000000000000000000, 1.836970198721032892E-16 ) ) ;
#66505=CARTESIAN_POINT ( 'NONE',  ( -7.259684009079983902, -7.811466277050722162, 195.0000000000000284 ) ) ;
#66510=VERTEX_POINT ( 'NONE', #29790 ) ;
#66518=AXIS2_PLACEMENT_3D ( 'NONE', #62084, #13658, #35209 ) ;
#66519=DIRECTION ( 'NONE',  ( 1.836970198721029934E-16, 1.836970198721010706E-16, -1.000000000000000000 ) ) ;
#66523=EDGE_LOOP ( 'NONE', ( #37829, #40544, #67761, #67613 ) ) ;
#66524=EDGE_CURVE ( 'NONE', #66935, #18339, #2223, .T. ) ;
#66525=VECTOR ( 'NONE', #22308, 1000.000000000000000 ) ;
#66536=DIRECTION ( 'NONE',  ( -0.7671651518153087546, -0.6414496315691469164, 2.309356642089053889E-17 ) ) ;
#66544=VECTOR ( 'NONE', #12585, 1000.000000000000000 ) ;
#66545=CYLINDRICAL_SURFACE ( 'NONE', #63256, 0.1999999999999987899 ) ;
#66547=ORIENTED_EDGE ( 'NONE', *, *, #2696, .T. ) ;
#66549=VECTOR ( 'NONE', #65966, 1000.000000000000000 ) ;
#66552=ORIENTED_EDGE ( 'NONE', *, *, #40628, .F. ) ;
#66560=VERTEX_POINT ( 'NONE', #18835 ) ;
#66567=ORIENTED_EDGE ( 'NONE', *, *, #26858, .F. ) ;
#66571=ORIENTED_EDGE ( 'NONE', *, *, #26637, .T. ) ;
#66573=VECTOR ( 'NONE', #16175, 1000.000000000000000 ) ;
#66584=DIRECTION ( 'NONE',  ( -0.000000000000000000, -0.000000000000000000, -1.000000000000000000 ) ) ;
#66586=FACE_OUTER_BOUND ( 'NONE', #41021, .T. ) ;
#66590=DIRECTION ( 'NONE',  ( -1.000000000000000000, 0.000000000000000000, 0.000000000000000000 ) ) ;
#66592=EDGE_LOOP ( 'NONE', ( #36067, #51580, #30952, #68404 ) ) ;
#66596=DIRECTION ( 'NONE',  ( 2.135044278125299371E-15, 1.000000000000000000, 0.000000000000000000 ) ) ;
#66598=VECTOR ( 'NONE', #31035, 1000.000000000000000 ) ;
#66606=AXIS2_PLACEMENT_3D ( 'NONE', #54742, #59697, #54399 ) ;
#66607=EDGE_LOOP ( 'NONE', ( #10388, #50238, #41818, #3038 ) ) ;
#66617=DIRECTION ( 'NONE',  ( 1.836970198721029934E-16, 1.836970198721010706E-16, -1.000000000000000000 ) ) ;
#66624=ORIENTED_EDGE ( 'NONE', *, *, #332, .F. ) ;
#66625=VECTOR ( 'NONE', #24552, 1000.000000000000000 ) ;
#66629=ORIENTED_EDGE ( 'NONE', *, *, #69683, .F. ) ;
#66636=CARTESIAN_POINT ( 'NONE',  ( 11.78648345035333378, 4.393516549646564684, 195.0000000000000284 ) ) ;
#66641=DIRECTION ( 'NONE',  ( -1.000000000000000000, 1.047444401652939849E-14, -1.836970198721010706E-16 ) ) ;
#66642=DIRECTION ( 'NONE',  ( 3.491481338843133355E-15, 1.000000000000000000, 1.836970198721029934E-16 ) ) ;
#66644=VECTOR ( 'NONE', #3013, 1000.000000000000000 ) ;
#66653=ORIENTED_EDGE ( 'NONE', *, *, #51278, .T. ) ;
#66654=DIRECTION ( 'NONE',  ( -1.828336019306068379E-14, -1.000000000000000000, -1.836970198721044232E-16 ) ) ;
#66655=CARTESIAN_POINT ( 'NONE',  ( -11.18071654964669648, 11.18071654964658812, 455.0000000000000568 ) ) ;
#66658=DIRECTION ( 'NONE',  ( -1.836970198721029934E-16, -1.836970198721010706E-16, 1.000000000000000000 ) ) ;
#66659=CIRCLE ( 'NONE', #17009, 0.1999999999999996503 ) ;
#66670=ORIENTED_EDGE ( 'NONE', *, *, #36265, .F. ) ;
#66671=VECTOR ( 'NONE', #43163, 1000.000000000000000 ) ;
#66674=ORIENTED_EDGE ( 'NONE', *, *, #8631, .T. ) ;
#66677=ORIENTED_EDGE ( 'NONE', *, *, #23665, .F. ) ;
#66691=DIRECTION ( 'NONE',  ( -0.000000000000000000, -0.000000000000000000, -1.000000000000000000 ) ) ;
#66698=CIRCLE ( 'NONE', #47540, 1.399999999999999245 ) ;
#66703=VECTOR ( 'NONE', #13365, 1000.000000000000000 ) ;
#66706=CARTESIAN_POINT ( 'NONE',  ( 11.78648345035337996, 4.173516549646518747, 455.0000000000000568 ) ) ;
#66711=VERTEX_POINT ( 'NONE', #27297 ) ;
#66715=DIRECTION ( 'NONE',  ( -1.836970198721029934E-16, 1.836970198721036344E-16, -1.000000000000000000 ) ) ;
#66728=DIRECTION ( 'NONE',  ( -1.836970198721029934E-16, 1.836970198721036344E-16, -1.000000000000000000 ) ) ;
#66735=DIRECTION ( 'NONE',  ( 0.6414496315691526895, 0.7671651518153038696, 2.587583378555111534E-16 ) ) ;
#66745=AXIS2_PLACEMENT_3D ( 'NONE', #2040, #1349, #44124 ) ;
#66758=EDGE_CURVE ( 'NONE', #8276, #46298, #60144, .T. ) ;
#66762=ORIENTED_EDGE ( 'NONE', *, *, #46700, .T. ) ;
#66765=LINE ( 'NONE', #61445, #29968 ) ;
#66768=VERTEX_POINT ( 'NONE', #54858 ) ;
#66776=ORIENTED_EDGE ( 'NONE', *, *, #66890, .T. ) ;
#66789=CYLINDRICAL_SURFACE ( 'NONE', #44234, 2.204799999999999649 ) ;
#66793=CARTESIAN_POINT ( 'NONE',  ( 4.622483450353394474, 3.593516549646586622, 455.0000000000000568 ) ) ;
#66820=CARTESIAN_POINT ( 'NONE',  ( -9.404046420174113408, -1.866219381641437636, 455.0000000000000568 ) ) ;
#66825=ORIENTED_EDGE ( 'NONE', *, *, #57355, .T. ) ;
#66836=ADVANCED_FACE ( 'NONE', ( #64773 ), #60491, .T. ) ;
#66843=CARTESIAN_POINT ( 'NONE',  ( -11.07551654964676935, -9.804883450353326424, 195.0000000000000284 ) ) ;
#66846=LINE ( 'NONE', #2498, #10800 ) ;
#66850=DIRECTION ( 'NONE',  ( 1.836970198721029934E-16, 1.836970198721010706E-16, -1.000000000000000000 ) ) ;
#66855=CARTESIAN_POINT ( 'NONE',  ( -5.380658396643234198, 4.734785091273867152, 455.0000000000000568 ) ) ;
#66858=EDGE_CURVE ( 'NONE', #46196, #19320, #24759, .T. ) ;
#66871=CARTESIAN_POINT ( 'NONE',  ( 6.006483450353409914, 8.198316549646580853, 455.0000000000000568 ) ) ;
#66887=VERTEX_POINT ( 'NONE', #60833 ) ;
#66890=EDGE_CURVE ( 'NONE', #48961, #13793, #39951, .T. ) ;
#66910=EDGE_CURVE ( 'NONE', #62095, #3656, #44926, .T. ) ;
#66913=CARTESIAN_POINT ( 'NONE',  ( -4.173516549646792306, -12.00648345035339837, 195.0000000000000284 ) ) ;
#66915=LINE ( 'NONE', #13175, #26542 ) ;
#66921=ORIENTED_EDGE ( 'NONE', *, *, #8042, .T. ) ;
#66922=CARTESIAN_POINT ( 'NONE',  ( -1.077516549646670541, 11.33351654964656596, 455.0000000000000568 ) ) ;
#66934=EDGE_CURVE ( 'NONE', #3912, #65820, #58691, .T. ) ;
#66935=VERTEX_POINT ( 'NONE', #9913 ) ;
#66940=FACE_OUTER_BOUND ( 'NONE', #34379, .T. ) ;
#66944=VERTEX_POINT ( 'NONE', #68241 ) ;
#66950=EDGE_LOOP ( 'NONE', ( #48538, #57812, #45134, #9970 ) ) ;
#66954=FACE_OUTER_BOUND ( 'NONE', #69434, .T. ) ;
#66960=DIRECTION ( 'NONE',  ( -0.000000000000000000, 3.673940397442059868E-16, -1.000000000000000000 ) ) ;
#66961=ADVANCED_FACE ( 'NONE', ( #31480 ), #15211, .F. ) ;
#66962=LINE ( 'NONE', #34082, #2990 ) ;
#66968=CARTESIAN_POINT ( 'NONE',  ( -11.77351654964670935, 4.393516549646602876, 455.0000000000000568 ) ) ;
#66972=VECTOR ( 'NONE', #28204, 1000.000000000000000 ) ;
#66974=ORIENTED_EDGE ( 'NONE', *, *, #42728, .F. ) ;
#66975=DIRECTION ( 'NONE',  ( 1.261617073437657577E-14, 1.000000000000000000, 0.000000000000000000 ) ) ;
#66991=CARTESIAN_POINT ( 'NONE',  ( -1.853252480934882707, -9.417013320880883498, 455.0000000000000568 ) ) ;
#66994=EDGE_LOOP ( 'NONE', ( #7160, #36318, #62998, #69914 ) ) ;
#67003=CARTESIAN_POINT ( 'NONE',  ( 10.20488345035338007, -11.08848345035349325, 455.0000000000000568 ) ) ;
#67011=VECTOR ( 'NONE', #11013, 1000.000000000000000 ) ;
#67013=DIRECTION ( 'NONE',  ( -1.000000000000000000, 0.000000000000000000, 0.000000000000000000 ) ) ;
#67019=VECTOR ( 'NONE', #69050, 1000.000000000000000 ) ;
#67020=ORIENTED_EDGE ( 'NONE', *, *, #28026, .F. ) ;
#67028=DIRECTION ( 'NONE',  ( -0.7671651518153128624, -0.6414496315691420314, 2.309356642089219057E-17 ) ) ;
#67034=EDGE_LOOP ( 'NONE', ( #9983, #66624, #44993, #55977 ) ) ;
#67036=EDGE_LOOP ( 'NONE', ( #49809, #39452, #37423, #21569 ) ) ;
#67041=EDGE_CURVE ( 'NONE', #17336, #29997, #43453, .T. ) ;
#67042=DIRECTION ( 'NONE',  ( -0.000000000000000000, -0.000000000000000000, -1.000000000000000000 ) ) ;
#67050=DIRECTION ( 'NONE',  ( 0.000000000000000000, -3.673940397442059868E-16, 1.000000000000000000 ) ) ;
#67053=EDGE_CURVE ( 'NONE', #9740, #58374, #54431, .T. ) ;
#67057=EDGE_CURVE ( 'NONE', #33142, #41637, #32160, .T. ) ;
#67060=DIRECTION ( 'NONE',  ( -0.6414496315691484707, 0.7671651518153074223, 2.309356642088893343E-17 ) ) ;
#67063=LINE ( 'NONE', #35577, #8367 ) ;
#67067=DIRECTION ( 'NONE',  ( -0.7671651518153073113, -0.6414496315691485817, -2.587583378555112027E-16 ) ) ;
#67075=DIRECTION ( 'NONE',  ( -0.000000000000000000, -0.000000000000000000, -1.000000000000000000 ) ) ;
#67079=ORIENTED_EDGE ( 'NONE', *, *, #2195, .F. ) ;
#67087=CARTESIAN_POINT ( 'NONE',  ( -5.993516549646711766, 5.993516549646603409, 455.0000000000000568 ) ) ;
#67089=CARTESIAN_POINT ( 'NONE',  ( -4.173516549646669738, 11.77351654964658678, 195.0000000000000284 ) ) ;
#67090=EDGE_CURVE ( 'NONE', #54514, #38741, #65722, .T. ) ;
#67093=ORIENTED_EDGE ( 'NONE', *, *, #5489, .T. ) ;
#67096=DIRECTION ( 'NONE',  ( 0.000000000000000000, 0.000000000000000000, 1.000000000000000000 ) ) ;
#67098=VERTEX_POINT ( 'NONE', #11611 ) ;
#67101=CARTESIAN_POINT ( 'NONE',  ( -8.393516549646733438, -6.344579767990798480, 195.0000000000000284 ) ) ;
#67102=FACE_OUTER_BOUND ( 'NONE', #67509, .T. ) ;
#67109=LINE ( 'NONE', #13006, #58420 ) ;
#67130=LINE ( 'NONE', #41305, #31687 ) ;
#67144=CARTESIAN_POINT ( 'NONE',  ( -8.452095193409402185, 4.242044687070461784, 195.0000000000000284 ) ) ;
#67145=LINE ( 'NONE', #23658, #7695 ) ;
#67160=CARTESIAN_POINT ( 'NONE',  ( -6.606374702650211539, -4.747751991980665665, 455.0000000000000568 ) ) ;
#67167=AXIS2_PLACEMENT_3D ( 'NONE', #61087, #12645, #49802 ) ;
#67172=DIRECTION ( 'NONE',  ( -0.7071067811865401342, 0.7071067811865550112, 1.355854680848613865E-30 ) ) ;
#67175=DIRECTION ( 'NONE',  ( 1.000000000000000000, 0.000000000000000000, 0.000000000000000000 ) ) ;
#67197=LINE ( 'NONE', #29709, #59171 ) ;
#67203=VERTEX_POINT ( 'NONE', #1703 ) ;
#67204=CARTESIAN_POINT ( 'NONE',  ( -11.07551654964678178, -11.08848345035329075, 195.0000000000000284 ) ) ;
#67208=ORIENTED_EDGE ( 'NONE', *, *, #45719, .F. ) ;
#67218=ORIENTED_EDGE ( 'NONE', *, *, #15929, .F. ) ;
#67226=VECTOR ( 'NONE', #67650, 1000.000000000000000 ) ;
#67229=EDGE_CURVE ( 'NONE', #21914, #1362, #45524, .T. ) ;
#67231=EDGE_CURVE ( 'NONE', #31922, #43306, #60751, .T. ) ;
#67233=DIRECTION ( 'NONE',  ( -1.000000000000000000, 3.491481338843133355E-15, 1.836970198721036344E-16 ) ) ;
#67246=CARTESIAN_POINT ( 'NONE',  ( 11.08848345035334404, -11.48848345035349183, 455.0000000000000568 ) ) ;
#67247=ADVANCED_FACE ( 'NONE', ( #46848 ), #29612, .F. ) ;
#67255=DIRECTION ( 'NONE',  ( -0.000000000000000000, 3.673940397442059868E-16, -1.000000000000000000 ) ) ;
#67268=VECTOR ( 'NONE', #17060, 1000.000000000000000 ) ;
#67269=AXIS2_PLACEMENT_3D ( 'NONE', #34109, #44370, #55355 ) ;
#67271=ORIENTED_EDGE ( 'NONE', *, *, #43223, .F. ) ;
#67273=EDGE_LOOP ( 'NONE', ( #68736, #5410, #11558, #19952 ) ) ;
#67290=VECTOR ( 'NONE', #34730, 1000.000000000000000 ) ;
#67292=DIRECTION ( 'NONE',  ( 1.836970198721029934E-16, 1.836970198721010706E-16, -1.000000000000000000 ) ) ;
#67298=ORIENTED_EDGE ( 'NONE', *, *, #4315, .T. ) ;
#67306=VERTEX_POINT ( 'NONE', #18302 ) ;
#67318=EDGE_LOOP ( 'NONE', ( #29019, #32665, #9714, #3045 ) ) ;
#67326=CIRCLE ( 'NONE', #5258, 0.8128000000000145109 ) ;
#67328=CYLINDRICAL_SURFACE ( 'NONE', #3607, 0.8128000000000145109 ) ;
#67334=AXIS2_PLACEMENT_3D ( 'NONE', #25926, #58793, #26963 ) ;
#67336=DIRECTION ( 'NONE',  ( 0.000000000000000000, -0.000000000000000000, -1.000000000000000000 ) ) ;
#67344=AXIS2_PLACEMENT_3D ( 'NONE', #62464, #46213, #57183 ) ;
#67350=CARTESIAN_POINT ( 'NONE',  ( 6.619341603356837744, -7.265214908726146170, 195.0000000000000284 ) ) ;
#67362=DIRECTION ( 'NONE',  ( 1.000000000000000000, -1.828336019306068379E-14, 0.000000000000000000 ) ) ;
#67364=VECTOR ( 'NONE', #40841, 1000.000000000000000 ) ;
#67366=EDGE_CURVE ( 'NONE', #41078, #37589, #4442, .T. ) ;
#67368=VECTOR ( 'NONE', #46708, 1000.000000000000000 ) ;
#67369=DIRECTION ( 'NONE',  ( -1.000000000000000000, 0.000000000000000000, 0.000000000000000000 ) ) ;
#67370=LINE ( 'NONE', #12556, #44097 ) ;
#67373=ORIENTED_EDGE ( 'NONE', *, *, #20675, .F. ) ;
#67376=CIRCLE ( 'NONE', #43488, 0.2000000000000005107 ) ;
#67379=LINE ( 'NONE', #35176, #59401 ) ;
#67382=AXIS2_PLACEMENT_3D ( 'NONE', #43506, #21608, #60458 ) ;
#67384=ADVANCED_FACE ( 'NONE', ( #36971 ), #53926, .F. ) ;
#67389=EDGE_CURVE ( 'NONE', #46286, #30523, #1702, .T. ) ;
#67402=VERTEX_POINT ( 'NONE', #44318 ) ;
#67405=ADVANCED_FACE ( 'NONE', ( #33033 ), #27387, .T. ) ;
#67409=CARTESIAN_POINT ( 'NONE',  ( -7.393516549646776070, -6.006483450353401921, 455.0000000000000568 ) ) ;
#67410=ORIENTED_EDGE ( 'NONE', *, *, #20304, .F. ) ;
#67411=ADVANCED_FACE ( 'NONE', ( #48957 ), #50328, .F. ) ;
#67412=LINE ( 'NONE', #2002, #51433 ) ;
#67422=DIRECTION ( 'NONE',  ( -1.836970198721029934E-16, -1.836970198721010706E-16, 1.000000000000000000 ) ) ;
#67432=CARTESIAN_POINT ( 'NONE',  ( -4.727349090213552429, -4.201500623656063915, 455.0000000000000568 ) ) ;
#67433=AXIS2_PLACEMENT_3D ( 'NONE', #16122, #27078, #47260 ) ;
#67434=DIRECTION ( 'NONE',  ( -0.000000000000000000, -0.000000000000000000, -1.000000000000000000 ) ) ;
#67440=DIRECTION ( 'NONE',  ( 0.7071067811865464625, -0.7071067811865486830, -2.597868168706483555E-16 ) ) ;
#67442=CIRCLE ( 'NONE', #66329, 0.1999999999999996503 ) ;
#67453=DIRECTION ( 'NONE',  ( -1.000000000000000000, 0.000000000000000000, 0.000000000000000000 ) ) ;
#67456=ORIENTED_EDGE ( 'NONE', *, *, #55111, .F. ) ;
#67457=ADVANCED_FACE ( 'NONE', ( #27731 ), #22085, .T. ) ;
#67458=CYLINDRICAL_SURFACE ( 'NONE', #45405, 0.4000000000000010214 ) ;
#67460=LINE ( 'NONE', #67799, #35381 ) ;
#67463=VERTEX_POINT ( 'NONE', #43648 ) ;
#67466=EDGE_CURVE ( 'NONE', #31830, #23630, #65230, .T. ) ;
#67467=VERTEX_POINT ( 'NONE', #43980 ) ;
#67470=FACE_OUTER_BOUND ( 'NONE', #33320, .T. ) ;
#67473=ORIENTED_EDGE ( 'NONE', *, *, #22320, .T. ) ;
#67475=ORIENTED_EDGE ( 'NONE', *, *, #60274, .T. ) ;
#67477=VECTOR ( 'NONE', #2480, 1000.000000000000000 ) ;
#67488=DIRECTION ( 'NONE',  ( -1.000000000000000000, 1.261617073437657577E-14, 4.635105932205237132E-30 ) ) ;
#67495=FACE_OUTER_BOUND ( 'NONE', #10690, .T. ) ;
#67501=ORIENTED_EDGE ( 'NONE', *, *, #16929, .F. ) ;
#67505=DIRECTION ( 'NONE',  ( -0.7071067811865500152, -0.7071067811865451302, 4.683861624749757595E-31 ) ) ;
#67509=EDGE_LOOP ( 'NONE', ( #45823, #35921, #9843, #31835 ) ) ;
#67512=CARTESIAN_POINT ( 'NONE',  ( -8.693516549646711056, 11.11351654964659730, 455.0000000000000568 ) ) ;
#67516=ORIENTED_EDGE ( 'NONE', *, *, #58265, .T. ) ;
#67519=CARTESIAN_POINT ( 'NONE',  ( -9.791916549646712653, 10.19191654964664018, 455.0000000000000568 ) ) ;
#67523=CARTESIAN_POINT ( 'NONE',  ( -4.393516549646835578, -11.78648345035344214, 455.0000000000000568 ) ) ;
#67526=DIRECTION ( 'NONE',  ( 3.016910393003147986E-15, 1.000000000000000000, -0.000000000000000000 ) ) ;
#67527=CARTESIAN_POINT ( 'NONE',  ( -11.99351654964671354, 7.813516549646603693, 455.0000000000000568 ) ) ;
#67528=VECTOR ( 'NONE', #43808, 1000.000000000000000 ) ;
#67529=CARTESIAN_POINT ( 'NONE',  ( 2.706483450353371900, 10.91351654964663354, 195.0000000000000284 ) ) ;
#67536=ORIENTED_EDGE ( 'NONE', *, *, #17978, .T. ) ;
#67538=DIRECTION ( 'NONE',  ( -0.000000000000000000, 3.673940397442059868E-16, -1.000000000000000000 ) ) ;
#67543=CARTESIAN_POINT ( 'NONE',  ( 11.78648345035340839, 7.813516549646560172, 455.0000000000000568 ) ) ;
#67544=ORIENTED_EDGE ( 'NONE', *, *, #12131, .T. ) ;
#67549=EDGE_CURVE ( 'NONE', #54840, #13233, #45709, .T. ) ;
#67553=VERTEX_POINT ( 'NONE', #8933 ) ;
#67556=EDGE_CURVE ( 'NONE', #28277, #1362, #2237, .T. ) ;
#67562=CARTESIAN_POINT ( 'NONE',  ( 12.00648345035341968, 11.18071654964654726, 455.0000000000000568 ) ) ;
#67563=EDGE_CURVE ( 'NONE', #3872, #41995, #12993, .T. ) ;
#67564=DIRECTION ( 'NONE',  ( -0.7671651518152998728, 0.6414496315691574635, 0.000000000000000000 ) ) ;
#67569=VERTEX_POINT ( 'NONE', #19542 ) ;
#67575=AXIS2_PLACEMENT_3D ( 'NONE', #35612, #31395, #57196 ) ;
#67578=VERTEX_POINT ( 'NONE', #51371 ) ;
#67583=ORIENTED_EDGE ( 'NONE', *, *, #7818, .T. ) ;
#67589=DIRECTION ( 'NONE',  ( -3.491481338843133355E-15, -1.000000000000000000, -1.836970198721029934E-16 ) ) ;
#67594=ORIENTED_EDGE ( 'NONE', *, *, #25331, .T. ) ;
#67596=FACE_OUTER_BOUND ( 'NONE', #48625, .T. ) ;
#67607=ORIENTED_EDGE ( 'NONE', *, *, #66890, .F. ) ;
#67613=ORIENTED_EDGE ( 'NONE', *, *, #57437, .T. ) ;
#67616=ORIENTED_EDGE ( 'NONE', *, *, #10163, .T. ) ;
#67623=VERTEX_POINT ( 'NONE', #36884 ) ;
#67627=DIRECTION ( 'NONE',  ( 1.836970198721029934E-16, 1.836970198721010706E-16, -1.000000000000000000 ) ) ;
#67638=FACE_OUTER_BOUND ( 'NONE', #8693, .T. ) ;
#67641=DIRECTION ( 'NONE',  ( -1.000000000000000000, 0.000000000000000000, 0.000000000000000000 ) ) ;
#67650=DIRECTION ( 'NONE',  ( -2.990116172375847553E-15, -1.000000000000000000, -1.836970198721030920E-16 ) ) ;
#67654=VERTEX_POINT ( 'NONE', #63040 ) ;
#67658=ORIENTED_EDGE ( 'NONE', *, *, #62383, .T. ) ;
#67664=DIRECTION ( 'NONE',  ( 1.836970198721029934E-16, 1.836970198721010706E-16, -1.000000000000000000 ) ) ;
#67666=ORIENTED_EDGE ( 'NONE', *, *, #60901, .F. ) ;
#67670=CARTESIAN_POINT ( 'NONE',  ( -2.693516549646675529, 10.91351654964657314, 195.0000000000000284 ) ) ;
#67672=CARTESIAN_POINT ( 'NONE',  ( -7.259684009079930611, 7.798499376343971612, 455.0000000000000568 ) ) ;
#67692=ADVANCED_FACE ( 'NONE', ( #63391 ), #64108, .F. ) ;
#67702=FACE_OUTER_BOUND ( 'NONE', #29074, .T. ) ;
#67707=ORIENTED_EDGE ( 'NONE', *, *, #49236, .F. ) ;
#67712=ADVANCED_FACE ( 'NONE', ( #14953 ), #37225, .F. ) ;
#67719=CIRCLE ( 'NONE', #64307, 0.1999999999999987899 ) ;
#67720=DIRECTION ( 'NONE',  ( 1.836970198721029934E-16, 1.836970198721010706E-16, -1.000000000000000000 ) ) ;
#67733=ORIENTED_EDGE ( 'NONE', *, *, #57477, .T. ) ;
#67743=ORIENTED_EDGE ( 'NONE', *, *, #17771, .T. ) ;
#67753=CIRCLE ( 'NONE', #9060, 0.6000000000000006439 ) ;
#67757=VECTOR ( 'NONE', #9001, 1000.000000000000000 ) ;
#67761=ORIENTED_EDGE ( 'NONE', *, *, #43069, .F. ) ;
#67768=EDGE_CURVE ( 'NONE', #25046, #46850, #21995, .T. ) ;
#67769=DIRECTION ( 'NONE',  ( 1.000000000000000000, -1.254221251785257574E-14, 0.000000000000000000 ) ) ;
#67772=PLANE ( 'NONE',  #33835 ) ;
#67775=AXIS2_PLACEMENT_3D ( 'NONE', #23007, #2476, #50227 ) ;
#67784=DIRECTION ( 'NONE',  ( 1.000000000000000000, -8.903847840905249551E-15, 1.836970198721013664E-16 ) ) ;
#67787=ORIENTED_EDGE ( 'NONE', *, *, #52638, .F. ) ;
#67789=EDGE_CURVE ( 'NONE', #30559, #27705, #6433, .T. ) ;
#67796=EDGE_CURVE ( 'NONE', #44324, #30449, #27996, .T. ) ;
#67799=CARTESIAN_POINT ( 'NONE',  ( -4.188533722949417282, -4.740315990920197287, 455.0000000000000568 ) ) ;
#67801=AXIS2_PLACEMENT_3D ( 'NONE', #14271, #42178, #3660 ) ;
#67803=DIRECTION ( 'NONE',  ( -0.7071067811865486830, -0.7071067811865464625, 0.000000000000000000 ) ) ;
#67809=CARTESIAN_POINT ( 'NONE',  ( -5.993516549646776603, -6.006483450353426790, 455.0000000000000568 ) ) ;
#67814=AXIS2_PLACEMENT_3D ( 'NONE', #55237, #60532, #60870 ) ;
#67818=DIRECTION ( 'NONE',  ( -0.000000000000000000, -0.000000000000000000, -1.000000000000000000 ) ) ;
#67820=VECTOR ( 'NONE', #18425, 1000.000000000000000 ) ;
#67824=CARTESIAN_POINT ( 'NONE',  ( -8.198316549646712303, 5.993516549646603409, 455.0000000000000568 ) ) ;
#67826=DIRECTION ( 'NONE',  ( -0.000000000000000000, 3.673940397442059868E-16, -1.000000000000000000 ) ) ;
#67827=ORIENTED_EDGE ( 'NONE', *, *, #55981, .F. ) ;
#67845=LINE ( 'NONE', #46613, #39111 ) ;
#67855=EDGE_CURVE ( 'NONE', #26901, #30052, #66846, .T. ) ;
#67867=DIRECTION ( 'NONE',  ( 0.000000000000000000, -1.000000000000000000, -3.673940397442059868E-16 ) ) ;
#67871=AXIS2_PLACEMENT_3D ( 'NONE', #24455, #23751, #61562 ) ;
#67874=VECTOR ( 'NONE', #16223, 1000.000000000000000 ) ;
#67875=VERTEX_POINT ( 'NONE', #34310 ) ;
#67879=VERTEX_POINT ( 'NONE', #13103 ) ;
#67880=VECTOR ( 'NONE', #61255, 1000.000000000000000 ) ;
#67887=CARTESIAN_POINT ( 'NONE',  ( 10.92648345035337343, -2.706483450353395437, 195.0000000000000284 ) ) ;
#67888=ORIENTED_EDGE ( 'NONE', *, *, #43364, .T. ) ;
#67893=CARTESIAN_POINT ( 'NONE',  ( 10.92648345035337343, -9.306483450353395526, 195.0000000000000284 ) ) ;
#67894=VECTOR ( 'NONE', #25623, 1000.000000000000000 ) ;
#67902=VERTEX_POINT ( 'NONE', #35357 ) ;
#67916=ORIENTED_EDGE ( 'NONE', *, *, #49236, .T. ) ;
#67920=CARTESIAN_POINT ( 'NONE',  ( -10.19191654964671301, 9.791916549646639822, 455.0000000000000568 ) ) ;
#67921=CIRCLE ( 'NONE', #37448, 0.1999999999999987899 ) ;
#67927=VECTOR ( 'NONE', #11367, 1000.000000000000000 ) ;
#67932=ORIENTED_EDGE ( 'NONE', *, *, #37497, .T. ) ;
#67938=VERTEX_POINT ( 'NONE', #23717 ) ;
#67948=DIRECTION ( 'NONE',  ( -1.000000000000000000, 0.000000000000000000, 0.000000000000000000 ) ) ;
#67950=EDGE_CURVE ( 'NONE', #14058, #48542, #24777, .T. ) ;
#67954=LINE ( 'NONE', #14201, #65415 ) ;
#67958=CARTESIAN_POINT ( 'NONE',  ( 6.006483450353379716, -6.006483450353490738, 455.0000000000000568 ) ) ;
#67961=DIRECTION ( 'NONE',  ( 1.000000000000000000, 0.000000000000000000, 0.000000000000000000 ) ) ;
#67962=CARTESIAN_POINT ( 'NONE',  ( -10.08346604330788132, -2.706483450353354581, 455.0000000000000568 ) ) ;
#67967=CYLINDRICAL_SURFACE ( 'NONE', #51663, 0.2000000000000005107 ) ;
#67975=DIRECTION ( 'NONE',  ( 1.000000000000000000, -1.883404846338789915E-14, 1.836970198720995421E-16 ) ) ;
#67982=ORIENTED_EDGE ( 'NONE', *, *, #22610, .T. ) ;
#67991=FACE_BOUND ( 'NONE', #19466, .T. ) ;
#67997=ORIENTED_EDGE ( 'NONE', *, *, #10358, .T. ) ;
#68006=VERTEX_POINT ( 'NONE', #4276 ) ;
#68007=ORIENTED_EDGE ( 'NONE', *, *, #38153, .T. ) ;
#68013=ORIENTED_EDGE ( 'NONE', *, *, #44666, .F. ) ;
#68023=FACE_OUTER_BOUND ( 'NONE', #15922, .T. ) ;
#68025=ORIENTED_EDGE ( 'NONE', *, *, #2560, .F. ) ;
#68026=ORIENTED_EDGE ( 'NONE', *, *, #4014, .T. ) ;
#68027=CARTESIAN_POINT ( 'NONE',  ( -1.853252480934882707, -9.417013320880883498, 455.0000000000000568 ) ) ;
#68029=VECTOR ( 'NONE', #54267, 1000.000000000000000 ) ;
#68031=PLANE ( 'NONE',  #31625 ) ;
#68035=CARTESIAN_POINT ( 'NONE',  ( -4.173516549646839380, -12.00648345035344811, 455.0000000000000568 ) ) ;
#68048=DIRECTION ( 'NONE',  ( -1.047444401652939849E-14, -1.000000000000000000, -1.836970198721029934E-16 ) ) ;
#68053=FACE_OUTER_BOUND ( 'NONE', #19521, .T. ) ;
#68061=CARTESIAN_POINT ( 'NONE',  ( 12.00648345035338238, 4.173516549646515195, 455.0000000000000568 ) ) ;
#68062=CYLINDRICAL_SURFACE ( 'NONE', #28604, 1.399999999999998579 ) ;
#68077=ORIENTED_EDGE ( 'NONE', *, *, #7997, .T. ) ;
#68082=CIRCLE ( 'NONE', #33101, 2.204799999999999205 ) ;
#68085=CARTESIAN_POINT ( 'NONE',  ( -8.452095193409387974, -4.255011587777191906, 195.0000000000000284 ) ) ;
#68086=VECTOR ( 'NONE', #55026, 1000.000000000000000 ) ;
#68087=CARTESIAN_POINT ( 'NONE',  ( -8.452095193409402185, 7.744988412222746810, 195.0000000000000284 ) ) ;
#68090=EDGE_LOOP ( 'NONE', ( #21150, #59250, #10244, #54477 ) ) ;
#68096=DIRECTION ( 'NONE',  ( 2.135044278125301343E-15, -1.000000000000000000, -3.673940397442059868E-16 ) ) ;
#68098=CARTESIAN_POINT ( 'NONE',  ( 4.747751991980625696, -5.393625297349947445, 195.0000000000000284 ) ) ;
#68100=CARTESIAN_POINT ( 'NONE',  ( 4.206483450353373676, 11.11351654964663282, 195.0000000000000284 ) ) ;
#68110=EDGE_CURVE ( 'NONE', #65403, #4106, #26182, .T. ) ;
#68111=EDGE_CURVE ( 'NONE', #24412, #44389, #33461, .T. ) ;
#68118=CARTESIAN_POINT ( 'NONE',  ( 5.393625297349900372, -7.265214908726231435, 455.0000000000000568 ) ) ;
#68122=EDGE_CURVE ( 'NONE', #21711, #33281, #54443, .T. ) ;
#68124=CARTESIAN_POINT ( 'NONE',  ( -4.193516549646782998, -11.12648345035339581, 195.0000000000000284 ) ) ;
#68127=CARTESIAN_POINT ( 'NONE',  ( 6.344579767990823349, -8.406483450353396947, 195.0000000000000284 ) ) ;
#68131=DIRECTION ( 'NONE',  ( 0.7671651518153065341, -0.6414496315691495809, 0.000000000000000000 ) ) ;
#68132=CYLINDRICAL_SURFACE ( 'NONE', #5316, 0.2000000000000000944 ) ;
#68145=VECTOR ( 'NONE', #55016, 1000.000000000000000 ) ;
#68146=CYLINDRICAL_SURFACE ( 'NONE', #21498, 1.399999999999998579 ) ;
#68153=CARTESIAN_POINT ( 'NONE',  ( 10.09643294401453240, 9.293516549646613001, 195.0000000000000284 ) ) ;
#68155=DIRECTION ( 'NONE',  ( 1.000000000000000000, -1.671920889371702854E-15, 0.000000000000000000 ) ) ;
#68156=ORIENTED_EDGE ( 'NONE', *, *, #9189, .T. ) ;
#68164=ORIENTED_EDGE ( 'NONE', *, *, #19176, .T. ) ;
#68166=DIRECTION ( 'NONE',  ( -0.000000000000000000, 3.673940397442059868E-16, -1.000000000000000000 ) ) ;
#68172=ORIENTED_EDGE ( 'NONE', *, *, #26533, .T. ) ;
#68173=EDGE_LOOP ( 'NONE', ( #29378, #38089, #64759, #6026 ) ) ;
#68196=VERTEX_POINT ( 'NONE', #5661 ) ;
#68198=EDGE_CURVE ( 'NONE', #68881, #48598, #32177, .T. ) ;
#68201=ORIENTED_EDGE ( 'NONE', *, *, #45345, .F. ) ;
#68203=ORIENTED_EDGE ( 'NONE', *, *, #34361, .T. ) ;
#68214=CYLINDRICAL_SURFACE ( 'NONE', #60351, 0.3999999999999993006 ) ;
#68217=ORIENTED_EDGE ( 'NONE', *, *, #29728, .F. ) ;
#68221=LINE ( 'NONE', #69637, #28647 ) ;
#68225=ORIENTED_EDGE ( 'NONE', *, *, #43282, .T. ) ;
#68228=DIRECTION ( 'NONE',  ( 0.5000000000000068834, 0.8660254037844345998, 6.723777587268309839E-17 ) ) ;
#68239=AXIS2_PLACEMENT_3D ( 'NONE', #42211, #9700, #25618 ) ;
#68241=CARTESIAN_POINT ( 'NONE',  ( 10.09643294401454661, -9.306483450353395526, 195.0000000000000284 ) ) ;
#68259=DIRECTION ( 'NONE',  ( -0.8660254037844400399, -0.4999999999999973910, 6.723777587268495961E-17 ) ) ;
#68262=CARTESIAN_POINT ( 'NONE',  ( -10.91351654964675610, -9.306483450353326248, 195.0000000000000284 ) ) ;
#68285=AXIS2_PLACEMENT_3D ( 'NONE', #34235, #28947, #50521 ) ;
#68291=LINE ( 'NONE', #50974, #68934 ) ;
#68301=DIRECTION ( 'NONE',  ( -1.836970198721029934E-16, 1.836970198721036344E-16, -1.000000000000000000 ) ) ;
#68313=VERTEX_POINT ( 'NONE', #67824 ) ;
#68318=LINE ( 'NONE', #58432, #37269 ) ;
#68323=DIRECTION ( 'NONE',  ( -1.671920889371702657E-15, -1.000000000000000000, -3.673940397442059868E-16 ) ) ;
#68324=EDGE_CURVE ( 'NONE', #12404, #4257, #45864, .T. ) ;
#68329=EDGE_LOOP ( 'NONE', ( #52834, #37657, #28701, #29354 ) ) ;
#68336=DIRECTION ( 'NONE',  ( 9.050731179009442381E-15, 1.000000000000000000, 3.673940397442060361E-16 ) ) ;
#68340=CARTESIAN_POINT ( 'NONE',  ( -8.593516549646711411, 4.383466043307770121, 195.0000000000000284 ) ) ;
#68343=VECTOR ( 'NONE', #17901, 1000.000000000000000 ) ;
#68345=DIRECTION ( 'NONE',  ( -1.836970198721029934E-16, 1.836970198721036344E-16, -1.000000000000000000 ) ) ;
#68352=EDGE_LOOP ( 'NONE', ( #66571, #42413, #18345, #52685 ) ) ;
#68360=VERTEX_POINT ( 'NONE', #2758 ) ;
#68378=CARTESIAN_POINT ( 'NONE',  ( -11.18071654964669825, 11.99351654964660341, 455.0000000000000568 ) ) ;
#68380=CARTESIAN_POINT ( 'NONE',  ( -8.393516549646779623, -6.344579767990844665, 455.0000000000000568 ) ) ;
#68391=ORIENTED_EDGE ( 'NONE', *, *, #25503, .T. ) ;
#68395=AXIS2_PLACEMENT_3D ( 'NONE', #45837, #29919, #51499 ) ;
#68404=ORIENTED_EDGE ( 'NONE', *, *, #27642, .T. ) ;
#68416=DIRECTION ( 'NONE',  ( -0.8660254037844383745, -0.5000000000000005551, -1.836970198721031660E-16 ) ) ;
#68417=VERTEX_POINT ( 'NONE', #63577 ) ;
#68426=LINE ( 'NONE', #25659, #35194 ) ;
#68429=ORIENTED_EDGE ( 'NONE', *, *, #53604, .F. ) ;
#68430=ORIENTED_EDGE ( 'NONE', *, *, #43364, .F. ) ;
#68436=ADVANCED_FACE ( 'NONE', ( #42347 ), #9126, .F. ) ;
#68450=VECTOR ( 'NONE', #4183, 1000.000000000000000 ) ;
#68451=ORIENTED_EDGE ( 'NONE', *, *, #68110, .T. ) ;
#68461=AXIS2_PLACEMENT_3D ( 'NONE', #20976, #24888, #4393 ) ;
#68470=CARTESIAN_POINT ( 'NONE',  ( -6.331612867284154511, 8.393516549646601987, 455.0000000000000568 ) ) ;
#68472=EDGE_CURVE ( 'NONE', #39516, #40478, #63927, .T. ) ;
#68486=CARTESIAN_POINT ( 'NONE',  ( 4.396432944014576627, 8.393516549646587777, 455.0000000000000568 ) ) ;
#68488=AXIS2_PLACEMENT_3D ( 'NONE', #38977, #55245, #23416 ) ;
#68503=CIRCLE ( 'NONE', #7509, 1.399999999999999245 ) ;
#68504=DIRECTION ( 'NONE',  ( 0.5000000000000068834, 0.8660254037844345998, 6.723777587268309839E-17 ) ) ;
#68507=VECTOR ( 'NONE', #36189, 1000.000000000000000 ) ;
#68508=ORIENTED_EDGE ( 'NONE', *, *, #36414, .F. ) ;
#68512=DIRECTION ( 'NONE',  ( -3.491481338843132961E-15, -1.000000000000000000, -1.836970198721029934E-16 ) ) ;
#68515=PLANE ( 'NONE',  #14174 ) ;
#68518=CARTESIAN_POINT ( 'NONE',  ( -4.609516549646713202, 3.593516549646603941, 455.0000000000000568 ) ) ;
#68523=CARTESIAN_POINT ( 'NONE',  ( 11.78648345035337819, -7.826483450353491023, 455.0000000000000568 ) ) ;
#68526=ADVANCED_FACE ( 'NONE', ( #62494 ), #8773, .F. ) ;
#68531=DIRECTION ( 'NONE',  ( -0.8660254037844510311, -0.4999999999999785727, 0.000000000000000000 ) ) ;
#68533=LINE ( 'NONE', #57561, #12771 ) ;
#68540=EDGE_CURVE ( 'NONE', #39563, #67875, #26438, .T. ) ;
#68547=CARTESIAN_POINT ( 'NONE',  ( 11.78648345035333378, 4.393516549646564684, 195.0000000000000284 ) ) ;
#68550=VECTOR ( 'NONE', #3764, 1000.000000000000000 ) ;
#68567=CARTESIAN_POINT ( 'NONE',  ( -7.813516549646711162, 11.99351654964660341, 455.0000000000000568 ) ) ;
#68572=DIRECTION ( 'NONE',  ( -1.836970198721029934E-16, 1.836970198721036344E-16, -1.000000000000000000 ) ) ;
#68574=CYLINDRICAL_SURFACE ( 'NONE', #8584, 0.3999999999999993006 ) ;
#68581=LINE ( 'NONE', #21528, #44648 ) ;
#68582=ORIENTED_EDGE ( 'NONE', *, *, #14016, .T. ) ;
#68589=AXIS2_PLACEMENT_3D ( 'NONE', #69868, #42995, #27433 ) ;
#68597=VERTEX_POINT ( 'NONE', #16174 ) ;
#68617=VERTEX_POINT ( 'NONE', #5570 ) ;
#68635=ORIENTED_EDGE ( 'NONE', *, *, #65583, .T. ) ;
#68640=ORIENTED_EDGE ( 'NONE', *, *, #33110, .T. ) ;
#68651=VECTOR ( 'NONE', #4744, 1000.000000000000114 ) ;
#68661=ADVANCED_FACE ( 'NONE', ( #38444 ), #59991, .F. ) ;
#68664=AXIS2_PLACEMENT_3D ( 'NONE', #29505, #23153, #55348 ) ;
#68667=DIRECTION ( 'NONE',  ( -1.000000000000000000, 1.221996412923863792E-14, 1.836970198721052367E-16 ) ) ;
#68671=VERTEX_POINT ( 'NONE', #49406 ) ;
#68680=CARTESIAN_POINT ( 'NONE',  ( -9.093516549646826874, -10.92648345035338941, 455.0000000000000568 ) ) ;
#68697=EDGE_CURVE ( 'NONE', #41134, #14927, #62069, .T. ) ;
#68701=CARTESIAN_POINT ( 'NONE',  ( -4.727349090213504468, -4.201500623656015065, 195.0000000000000284 ) ) ;
#68706=DIRECTION ( 'NONE',  ( 0.8660254037844311581, -0.5000000000000129896, 6.723777587268175486E-17 ) ) ;
#68710=ORIENTED_EDGE ( 'NONE', *, *, #54639, .F. ) ;
#68711=ORIENTED_EDGE ( 'NONE', *, *, #28258, .T. ) ;
#68718=DIRECTION ( 'NONE',  ( -0.000000000000000000, -0.000000000000000000, -1.000000000000000000 ) ) ;
#68722=CARTESIAN_POINT ( 'NONE',  ( 7.811466277050736373, -4.740315990920159983, 195.0000000000000284 ) ) ;
#68724=ORIENTED_EDGE ( 'NONE', *, *, #32425, .F. ) ;
#68728=LINE ( 'NONE', #13218, #57585 ) ;
#68735=ORIENTED_EDGE ( 'NONE', *, *, #28125, .F. ) ;
#68736=ORIENTED_EDGE ( 'NONE', *, *, #55111, .T. ) ;
#68739=CARTESIAN_POINT ( 'NONE',  ( -5.380658396643315022, -4.747751991980679875, 455.0000000000000568 ) ) ;
#68740=DIRECTION ( 'NONE',  ( -1.000000000000000000, 1.115702204244422993E-14, 0.000000000000000000 ) ) ;
#68743=AXIS2_PLACEMENT_3D ( 'NONE', #35803, #45704, #46066 ) ;
#68745=DIRECTION ( 'NONE',  ( 0.7671651518153006499, 0.6414496315691565753, 0.000000000000000000 ) ) ;
#68746=ORIENTED_EDGE ( 'NONE', *, *, #8208, .T. ) ;
#68751=DIRECTION ( 'NONE',  ( -0.000000000000000000, 3.673940397442059868E-16, -1.000000000000000000 ) ) ;
#68755=EDGE_CURVE ( 'NONE', #58374, #20073, #45111, .T. ) ;
#68776=LINE ( 'NONE', #41189, #69654 ) ;
#68783=CIRCLE ( 'NONE', #15696, 0.6000000000000006439 ) ;
#68786=CARTESIAN_POINT ( 'NONE',  ( -8.513516549646713116, 11.29351654964659701, 194.9999952000000292 ) ) ;
#68794=PLANE ( 'NONE',  #18816 ) ;
#68800=VECTOR ( 'NONE', #49757, 1000.000000000000114 ) ;
#68801=VERTEX_POINT ( 'NONE', #57824 ) ;
#68802=DIRECTION ( 'NONE',  ( -0.000000000000000000, 3.673940397442059868E-16, -1.000000000000000000 ) ) ;
#68803=DIRECTION ( 'NONE',  ( -1.047444401652940007E-14, -1.000000000000000000, -1.836970198721029934E-16 ) ) ;
#68804=VERTEX_POINT ( 'NONE', #68085 ) ;
#68806=CIRCLE ( 'NONE', #39407, 2.204799999999997429 ) ;
#68811=ORIENTED_EDGE ( 'NONE', *, *, #24048, .T. ) ;
#68813=CARTESIAN_POINT ( 'NONE',  ( -11.07551654964682797, -11.08848345035333693, 455.0000000000000568 ) ) ;
#68814=CARTESIAN_POINT ( 'NONE',  ( 4.740315990920129785, -4.201500623656049704, 195.0000000000000284 ) ) ;
#68815=ORIENTED_EDGE ( 'NONE', *, *, #19789, .F. ) ;
#68824=DIRECTION ( 'NONE',  ( -1.000000000000000000, 0.000000000000000000, 0.000000000000000000 ) ) ;
#68825=DIRECTION ( 'NONE',  ( -0.000000000000000000, -0.000000000000000000, -1.000000000000000000 ) ) ;
#68827=ADVANCED_FACE ( 'NONE', ( #63132 ), #68794, .F. ) ;
#68833=LINE ( 'NONE', #69527, #46363 ) ;
#68842=CARTESIAN_POINT ( 'NONE',  ( -2.752095193409373586, 9.942044687070435316, 455.0000000000000568 ) ) ;
#68843=LINE ( 'NONE', #52945, #30766 ) ;
#68844=ORIENTED_EDGE ( 'NONE', *, *, #42707, .F. ) ;
#68849=AXIS2_PLACEMENT_3D ( 'NONE', #51790, #24914, #46474 ) ;
#68855=ORIENTED_EDGE ( 'NONE', *, *, #52727, .F. ) ;
#68867=ORIENTED_EDGE ( 'NONE', *, *, #36418, .F. ) ;
#68868=DIRECTION ( 'NONE',  ( 5.626525616968433120E-15, 1.000000000000000000, 1.836970198721026236E-16 ) ) ;
#68869=LINE ( 'NONE', #63573, #7604 ) ;
#68872=AXIS2_PLACEMENT_3D ( 'NONE', #42621, #194, #58552 ) ;
#68876=EDGE_CURVE ( 'NONE', #37589, #14927, #51997, .T. ) ;
#68880=ORIENTED_EDGE ( 'NONE', *, *, #42312, .F. ) ;
#68881=VERTEX_POINT ( 'NONE', #8491 ) ;
#68886=CIRCLE ( 'NONE', #38395, 0.1999999999999987899 ) ;
#68895=VECTOR ( 'NONE', #51869, 1000.000000000000000 ) ;
#68900=LINE ( 'NONE', #284, #37920 ) ;
#68901=DIRECTION ( 'NONE',  ( -0.000000000000000000, 3.673940397442059868E-16, -1.000000000000000000 ) ) ;
#68907=DIRECTION ( 'NONE',  ( 0.000000000000000000, -1.000000000000000000, 0.000000000000000000 ) ) ;
#68913=LINE ( 'NONE', #68567, #8735 ) ;
#68919=CARTESIAN_POINT ( 'NONE',  ( 1.690483450353344352, -10.74648345035345720, 455.0000000000000568 ) ) ;
#68920=DIRECTION ( 'NONE',  ( -0.000000000000000000, 3.673940397442059868E-16, -1.000000000000000000 ) ) ;
#68923=ADVANCED_FACE ( 'NONE', ( #46328 ), #45985, .F. ) ;
#68934=VECTOR ( 'NONE', #45654, 1000.000000000000000 ) ;
#68955=DIRECTION ( 'NONE',  ( -0.000000000000000000, 3.673940397442059868E-16, -1.000000000000000000 ) ) ;
#68964=DIRECTION ( 'NONE',  ( -1.000000000000000000, 0.000000000000000000, 0.000000000000000000 ) ) ;
#68965=VERTEX_POINT ( 'NONE', #47038 ) ;
#68968=ORIENTED_EDGE ( 'NONE', *, *, #44947, .T. ) ;
#68977=FACE_OUTER_BOUND ( 'NONE', #41623, .T. ) ;
#68992=FACE_OUTER_BOUND ( 'NONE', #54277, .T. ) ;
#68993=PLANE ( 'NONE',  #65181 ) ;
#69017=ORIENTED_EDGE ( 'NONE', *, *, #56592, .T. ) ;
#69020=VERTEX_POINT ( 'NONE', #64353 ) ;
#69021=ORIENTED_EDGE ( 'NONE', *, *, #43061, .T. ) ;
#69023=FACE_OUTER_BOUND ( 'NONE', #55759, .T. ) ;
#69027=EDGE_LOOP ( 'NONE', ( #23624, #11120, #11679, #59294 ) ) ;
#69032=ORIENTED_EDGE ( 'NONE', *, *, #50299, .T. ) ;
#69039=DIRECTION ( 'NONE',  ( 0.000000000000000000, 0.000000000000000000, 1.000000000000000000 ) ) ;
#69041=ORIENTED_EDGE ( 'NONE', *, *, #14926, .T. ) ;
#69048=DIRECTION ( 'NONE',  ( -0.000000000000000000, 3.673940397442059868E-16, -1.000000000000000000 ) ) ;
#69050=DIRECTION ( 'NONE',  ( 1.836970198721029934E-16, 1.836970198721010706E-16, -1.000000000000000000 ) ) ;
#69061=LINE ( 'NONE', #41837, #20389 ) ;
#69062=EDGE_CURVE ( 'NONE', #23669, #59475, #9563, .T. ) ;
#69068=CARTESIAN_POINT ( 'NONE',  ( -5.993516549646776603, -6.006483450353426790, 455.0000000000000568 ) ) ;
#69072=ORIENTED_EDGE ( 'NONE', *, *, #7188, .T. ) ;
#69078=DIRECTION ( 'NONE',  ( 1.836970198721029934E-16, 1.836970198721010706E-16, -1.000000000000000000 ) ) ;
#69083=EDGE_CURVE ( 'NONE', #28648, #43815, #25830, .T. ) ;
#69084=ORIENTED_EDGE ( 'NONE', *, *, #26533, .F. ) ;
#69085=FACE_OUTER_BOUND ( 'NONE', #51398, .T. ) ;
#69101=PLANE ( 'NONE',  #68849 ) ;
#69105=DIRECTION ( 'NONE',  ( -0.000000000000000000, 3.673940397442059868E-16, -1.000000000000000000 ) ) ;
#69118=EDGE_LOOP ( 'NONE', ( #1094, #39040, #37673, #13822 ) ) ;
#69135=EDGE_LOOP ( 'NONE', ( #12324, #4779, #29016, #24596 ) ) ;
#69136=ORIENTED_EDGE ( 'NONE', *, *, #8887, .F. ) ;
#69144=ORIENTED_EDGE ( 'NONE', *, *, #32827, .F. ) ;
#69149=ORIENTED_EDGE ( 'NONE', *, *, #18686, .T. ) ;
#69155=EDGE_CURVE ( 'NONE', #57399, #44650, #1377, .T. ) ;
#69157=ADVANCED_FACE ( 'NONE', ( #27553 ), #43821, .T. ) ;
#69160=EDGE_CURVE ( 'NONE', #144, #41828, #44489, .T. ) ;
#69168=ORIENTED_EDGE ( 'NONE', *, *, #59021, .T. ) ;
#69171=DIRECTION ( 'NONE',  ( 0.000000000000000000, 0.000000000000000000, 1.000000000000000000 ) ) ;
#69176=LINE ( 'NONE', #57510, #38113 ) ;
#69181=CARTESIAN_POINT ( 'NONE',  ( 8.406483450353359643, 7.603567055985454459, 195.0000000000000284 ) ) ;
#69184=CARTESIAN_POINT ( 'NONE',  ( -11.07551654964667520, 10.19191654964664018, 455.0000000000000568 ) ) ;
#69188=CARTESIAN_POINT ( 'NONE',  ( 11.12648345035337982, 4.193516549646526315, 455.0000000000000568 ) ) ;
#69190=DIRECTION ( 'NONE',  ( -0.000000000000000000, 3.673940397442059868E-16, -1.000000000000000000 ) ) ;
#69210=ORIENTED_EDGE ( 'NONE', *, *, #30353, .F. ) ;
#69214=LINE ( 'NONE', #9472, #66598 ) ;
#69216=DIRECTION ( 'NONE',  ( 3.717264591378875951E-15, 1.000000000000000000, 0.000000000000000000 ) ) ;
#69223=ORIENTED_EDGE ( 'NONE', *, *, #63334, .F. ) ;
#69227=EDGE_CURVE ( 'NONE', #10176, #28585, #54779, .T. ) ;
#69236=LINE ( 'NONE', #9486, #18715 ) ;
#69237=DIRECTION ( 'NONE',  ( -0.7671651518153038696, 0.6414496315691526895, -2.309356642089023690E-17 ) ) ;
#69245=DIRECTION ( 'NONE',  ( 1.000000000000000000, -1.047444401652940007E-14, 1.836970198721010706E-16 ) ) ;
#69247=CIRCLE ( 'NONE', #45499, 0.5999999999999998668 ) ;
#69261=VECTOR ( 'NONE', #27164, 1000.000000000000000 ) ;
#69266=DIRECTION ( 'NONE',  ( 1.836970198721029934E-16, 1.836970198721010706E-16, -1.000000000000000000 ) ) ;
#69270=CYLINDRICAL_SURFACE ( 'NONE', #59545, 0.5999999999999998668 ) ;
#69287=ORIENTED_EDGE ( 'NONE', *, *, #12480, .F. ) ;
#69290=LINE ( 'NONE', #20846, #13352 ) ;
#69296=ORIENTED_EDGE ( 'NONE', *, *, #162, .F. ) ;
#69302=VECTOR ( 'NONE', #46158, 1000.000000000000000 ) ;
#69304=ORIENTED_EDGE ( 'NONE', *, *, #23235, .F. ) ;
#69305=CARTESIAN_POINT ( 'NONE',  ( -5.993516549646711766, 5.993516549646603409, 195.0000000000000284 ) ) ;
#69310=ORIENTED_EDGE ( 'NONE', *, *, #5620, .T. ) ;
#69314=VECTOR ( 'NONE', #57722, 1000.000000000000000 ) ;
#69315=CIRCLE ( 'NONE', #59172, 0.2000000000000005107 ) ;
#69333=DIRECTION ( 'NONE',  ( 0.6414496315691617934, -0.7671651518152962090, -2.818519042763987834E-16 ) ) ;
#69337=CARTESIAN_POINT ( 'NONE',  ( 12.00648345035338060, -4.186483450353396307, 195.0000000000000284 ) ) ;
#69340=FACE_OUTER_BOUND ( 'NONE', #64166, .T. ) ;
#69341=CARTESIAN_POINT ( 'NONE',  ( -7.259684009079916400, -4.201500623655988420, 195.0000000000000284 ) ) ;
#69346=CARTESIAN_POINT ( 'NONE',  ( 12.00648345035333620, 4.173516549646563156, 195.0000000000000284 ) ) ;
#69352=EDGE_CURVE ( 'NONE', #1336, #62698, #67109, .T. ) ;
#69355=ADVANCED_FACE ( 'NONE', ( #18666 ), #35264, .F. ) ;
#69364=DIRECTION ( 'NONE',  ( 1.836970198721029934E-16, 1.836970198721010706E-16, -1.000000000000000000 ) ) ;
#69374=LINE ( 'NONE', #21978, #11662 ) ;
#69389=VERTEX_POINT ( 'NONE', #29622 ) ;
#69393=ORIENTED_EDGE ( 'NONE', *, *, #9616, .T. ) ;
#69400=CARTESIAN_POINT ( 'NONE',  ( 8.465062094116069247, -7.757955312929539105, 195.0000000000000284 ) ) ;
#69415=DIRECTION ( 'NONE',  ( -0.5000000000000019984, -0.8660254037844375974, -0.000000000000000000 ) ) ;
#69428=VERTEX_POINT ( 'NONE', #24686 ) ;
#69430=DIRECTION ( 'NONE',  ( 1.836970198721029934E-16, 1.836970198721010706E-16, -1.000000000000000000 ) ) ;
#69434=EDGE_LOOP ( 'NONE', ( #17860, #60420, #29257, #6786 ) ) ;
#69435=FACE_BOUND ( 'NONE', #29843, .T. ) ;
#69439=PLANE ( 'NONE',  #21217 ) ;
#69445=CARTESIAN_POINT ( 'NONE',  ( 4.186483450353423841, 11.99351654964658742, 455.0000000000000568 ) ) ;
#69447=VECTOR ( 'NONE', #19722, 1000.000000000000000 ) ;
#69449=ORIENTED_EDGE ( 'NONE', *, *, #59040, .F. ) ;
#69455=AXIS2_PLACEMENT_3D ( 'NONE', #45190, #67488, #25045 ) ;
#69463=EDGE_CURVE ( 'NONE', #24415, #354, #51909, .T. ) ;
#69474=DIRECTION ( 'NONE',  ( 1.000000000000000000, 0.000000000000000000, 0.000000000000000000 ) ) ;
#69489=ORIENTED_EDGE ( 'NONE', *, *, #25621, .F. ) ;
#69500=VECTOR ( 'NONE', #60727, 1000.000000000000000 ) ;
#69511=FACE_OUTER_BOUND ( 'NONE', #3661, .T. ) ;
#69513=VECTOR ( 'NONE', #11094, 1000.000000000000000 ) ;
#69516=LINE ( 'NONE', #4477, #27680 ) ;
#69527=CARTESIAN_POINT ( 'NONE',  ( -8.452095193409402185, 7.744988412222746810, 455.0000000000000568 ) ) ;
#69528=CARTESIAN_POINT ( 'NONE',  ( -11.47551654964667733, 11.07551654964660237, 195.0000000000000284 ) ) ;
#69529=EDGE_CURVE ( 'NONE', #27000, #61399, #21472, .T. ) ;
#69530=LINE ( 'NONE', #41958, #52598 ) ;
#69538=ORIENTED_EDGE ( 'NONE', *, *, #3253, .F. ) ;
#69540=EDGE_CURVE ( 'NONE', #36372, #34655, #68869, .T. ) ;
#69542=VECTOR ( 'NONE', #3106, 1000.000000000000000 ) ;
#69548=LINE ( 'NONE', #4160, #65 ) ;
#69556=ADVANCED_FACE ( 'NONE', ( #10167 ), #36337, .F. ) ;
#69559=EDGE_CURVE ( 'NONE', #21746, #23316, #39255, .T. ) ;
#69560=AXIS2_PLACEMENT_3D ( 'NONE', #36629, #26729, #9413 ) ;
#69569=LINE ( 'NONE', #46579, #8511 ) ;
#69572=CARTESIAN_POINT ( 'NONE',  ( 12.00648345035338060, -7.826483450353491023, 455.0000000000000568 ) ) ;
#69573=ORIENTED_EDGE ( 'NONE', *, *, #12826, .F. ) ;
#69592=EDGE_CURVE ( 'NONE', #33832, #35182, #27129, .T. ) ;
#69593=CARTESIAN_POINT ( 'NONE',  ( 6.006483450353353959, 5.993516549646629166, 195.0000000000000284 ) ) ;
#69596=AXIS2_PLACEMENT_3D ( 'NONE', #5791, #16748, #27005 ) ;
#69605=ORIENTED_EDGE ( 'NONE', *, *, #26313, .F. ) ;
#69610=DIRECTION ( 'NONE',  ( -1.000000000000000000, 1.813998472013049822E-14, -1.836970198720996654E-16 ) ) ;
#69615=VECTOR ( 'NONE', #60510, 1000.000000000000000 ) ;
#69635=DIRECTION ( 'NONE',  ( -0.000000000000000000, 3.673940397442059868E-16, -1.000000000000000000 ) ) ;
#69636=ORIENTED_EDGE ( 'NONE', *, *, #58924, .T. ) ;
#69637=CARTESIAN_POINT ( 'NONE',  ( -3.593516549646790015, -7.428221114745077180, 455.0000000000000568 ) ) ;
#69638=ADVANCED_FACE ( 'NONE', ( #33472 ), #38100, .T. ) ;
#69641=DIRECTION ( 'NONE',  ( 1.000000000000000000, -1.356437060717834379E-15, -1.836970198721032646E-16 ) ) ;
#69654=VECTOR ( 'NONE', #41896, 1000.000000000000000 ) ;
#69665=AXIS2_PLACEMENT_3D ( 'NONE', #43345, #64933, #53291 ) ;
#69666=CIRCLE ( 'NONE', #47036, 0.1999999999999987899 ) ;
#69675=DIRECTION ( 'NONE',  ( -1.000000000000000000, 4.745709458399858621E-16, 1.836970198721030920E-16 ) ) ;
#69683=EDGE_CURVE ( 'NONE', #56927, #53423, #11882, .T. ) ;
#69684=AXIS2_PLACEMENT_3D ( 'NONE', #69705, #21266, #48477 ) ;
#69695=ORIENTED_EDGE ( 'NONE', *, *, #37875, .F. ) ;
#69705=CARTESIAN_POINT ( 'NONE',  ( 6.006483450353401921, 5.993516549646582092, 455.0000000000000568 ) ) ;
#69708=AXIS2_PLACEMENT_3D ( 'NONE', #29650, #35290, #8429 ) ;
#69710=CARTESIAN_POINT ( 'NONE',  ( 7.806483450353372433, 11.11351654964662039, 195.0000000000000284 ) ) ;
#69713=DIRECTION ( 'NONE',  ( 0.7071067811865475727, -0.7071067811865475727, -2.597868168706480597E-16 ) ) ;
#69716=ADVANCED_FACE ( 'NONE', ( #22857 ), #967, .F. ) ;
#69724=DIRECTION ( 'NONE',  ( -0.000000000000000000, -0.000000000000000000, -1.000000000000000000 ) ) ;
#69726=ORIENTED_EDGE ( 'NONE', *, *, #39753, .T. ) ;
#69746=CARTESIAN_POINT ( 'NONE',  ( -4.727349090213559535, -7.811466277050794993, 455.0000000000000568 ) ) ;
#69748=DIRECTION ( 'NONE',  ( -1.920292680692490463E-14, -1.000000000000000000, -1.836970198721045958E-16 ) ) ;
#69754=LINE ( 'NONE', #4092, #5897 ) ;
#69758=CIRCLE ( 'NONE', #17793, 2.204799999999997873 ) ;
#69764=LINE ( 'NONE', #4375, #67019 ) ;
#69765=EDGE_LOOP ( 'NONE', ( #42198, #42873, #43444, #17182 ) ) ;
#69766=ORIENTED_EDGE ( 'NONE', *, *, #25215, .T. ) ;
#69767=EDGE_LOOP ( 'NONE', ( #41625, #14817, #15230, #25224 ) ) ;
#69777=EDGE_LOOP ( 'NONE', ( #62622, #8809, #35739, #51250 ) ) ;
#69784=DIRECTION ( 'NONE',  ( 0.000000000000000000, 0.000000000000000000, 1.000000000000000000 ) ) ;
#69786=ORIENTED_EDGE ( 'NONE', *, *, #48956, .F. ) ;
#69789=CARTESIAN_POINT ( 'NONE',  ( 1.090483450353372907, 11.33351654964664590, 195.0000000000000284 ) ) ;
#69791=DIRECTION ( 'NONE',  ( -1.836970198721029934E-16, 1.836970198721036344E-16, -1.000000000000000000 ) ) ;
#69795=ORIENTED_EDGE ( 'NONE', *, *, #65542, .T. ) ;
#69799=CARTESIAN_POINT ( 'NONE',  ( 4.206483450353421638, 11.11351654964658486, 455.0000000000000568 ) ) ;
#69806=EDGE_CURVE ( 'NONE', #44389, #803, #12920, .T. ) ;
#69817=LINE ( 'NONE', #54598, #63842 ) ;
#69820=EDGE_LOOP ( 'NONE', ( #17474, #20439, #13389, #20169 ) ) ;
#69828=EDGE_LOOP ( 'NONE', ( #18086, #58465, #8780, #62081 ) ) ;
#69834=CARTESIAN_POINT ( 'NONE',  ( -9.828310488886039309, -1.690483450353358119, 455.0000000000000568 ) ) ;
#69839=ORIENTED_EDGE ( 'NONE', *, *, #25580, .F. ) ;
#69841=ADVANCED_FACE ( 'NONE', ( #40145 ), #57120, .T. ) ;
#69843=ORIENTED_EDGE ( 'NONE', *, *, #62348, .F. ) ;
#69854=EDGE_CURVE ( 'NONE', #8876, #13060, #13308, .T. ) ;
#69857=CARTESIAN_POINT ( 'NONE',  ( 4.206483450353421638, 11.11351654964658486, 455.0000000000000568 ) ) ;
#69860=VECTOR ( 'NONE', #42744, 1000.000000000000000 ) ;
#69865=FACE_OUTER_BOUND ( 'NONE', #61008, .T. ) ;
#69866=CYLINDRICAL_SURFACE ( 'NONE', #5478, 0.1999999999999996503 ) ;
#69868=CARTESIAN_POINT ( 'NONE',  ( -5.993516549646711766, 5.993516549646603409, 455.0000000000000568 ) ) ;
#69875=DIRECTION ( 'NONE',  ( -0.6414496315691617934, 0.7671651518152962090, 0.000000000000000000 ) ) ;
#69877=DIRECTION ( 'NONE',  ( -0.000000000000000000, 3.673940397442059868E-16, -1.000000000000000000 ) ) ;
#69892=EDGE_CURVE ( 'NONE', #29989, #62095, #37061, .T. ) ;
#69897=DIRECTION ( 'NONE',  ( -0.7071067811865401342, 0.7071067811865550112, 1.355854680848613865E-30 ) ) ;
#69900=ORIENTED_EDGE ( 'NONE', *, *, #39946, .F. ) ;
#69908=AXIS2_PLACEMENT_3D ( 'NONE', #60037, #38152, #55438 ) ;
#69913=ORIENTED_EDGE ( 'NONE', *, *, #64373, .F. ) ;
#69914=ORIENTED_EDGE ( 'NONE', *, *, #41654, .T. ) ;
#69919=ORIENTED_EDGE ( 'NONE', *, *, #5312, .F. ) ;
#69930=ORIENTED_EDGE ( 'NONE', *, *, #1300, .F. ) ;
#69936=EDGE_CURVE ( 'NONE', #48542, #46263, #28014, .T. ) ;
#69938=AXIS2_PLACEMENT_3D ( 'NONE', #17881, #10844, #60672 ) ;
#69941=DIRECTION ( 'NONE',  ( 1.000000000000000000, -8.802523127157697409E-15, 1.836970198721013664E-16 ) ) ;
#69945=ORIENTED_EDGE ( 'NONE', *, *, #17736, .F. ) ;
#69947=CARTESIAN_POINT ( 'NONE',  ( -7.259684009080030975, -7.811466277050769236, 455.0000000000000568 ) ) ;
#69948=AXIS2_PLACEMENT_3D ( 'NONE', #48485, #51, #49518 ) ;
#69950=EDGE_CURVE ( 'NONE', #37762, #53071, #25671, .T. ) ;
#69954=DIRECTION ( 'NONE',  ( -4.336808689942006692E-15, -1.000000000000000000, 0.000000000000000000 ) ) ;
#69976=LINE ( 'NONE', #5288, #35625 ) ;
ENDSEC;
END-ISO-10303-21;
